ISO-10303-21;
HEADER;
/* Generated by software containing ST-Developer
 * from STEP Tools, Inc. (www.steptools.com) 
 */

FILE_DESCRIPTION(
/* description */ ('Independent compact industrial fixture table, bolted aluminum worktop
 on connected adjustable support base. Whole-mm nominal dimensions. No
 load rating assigned.'),
/* implementation_level */ '2;1');

FILE_NAME(
/* name */ 'Socket head cap screw M8x25.step',
/* time_stamp */ '2026-11-07T17:47:58-08:00',
/* author */ (''),
/* organization */ (''),
/* preprocessor_version */ 'ST-DEVELOPER v20.2',
/* originating_system */ 'Autodesk Translation Framework v15.17.0.0',
/* authorisation */ '');

FILE_SCHEMA (('AUTOMOTIVE_DESIGN { 1 0 10303 214 3 1 1 }'));
ENDSEC;

DATA;
#10=MECHANICAL_DESIGN_GEOMETRIC_PRESENTATION_REPRESENTATION('',(#2253),#97475);
#330=CONICAL_SURFACE('',#22228,3.5,0.785398163397448);
#342=B_SPLINE_SURFACE_WITH_KNOTS('',3,3,((#35708,#35709,#35710,#35711,#35712,
#35713,#35714,#35715,#35716,#35717,#35718,#35719,#35720,#35721,#35722,#35723,
#35724,#35725,#35726,#35727,#35728,#35729,#35730,#35731,#35732,#35733,#35734,
#35735,#35736,#35737,#35738,#35739,#35740,#35741,#35742,#35743,#35744,#35745,
#35746,#35747,#35748,#35749,#35750,#35751,#35752,#35753,#35754,#35755,#35756,
#35757,#35758,#35759,#35760,#35761,#35762,#35763,#35764,#35765,#35766,#35767,
#35768,#35769,#35770,#35771,#35772,#35773,#35774,#35775,#35776,#35777,#35778,
#35779,#35780,#35781,#35782,#35783,#35784,#35785,#35786,#35787,#35788,#35789,
#35790,#35791,#35792,#35793,#35794,#35795,#35796,#35797,#35798,#35799,#35800,
#35801,#35802,#35803,#35804,#35805,#35806,#35807,#35808,#35809,#35810,#35811,
#35812,#35813,#35814,#35815,#35816,#35817,#35818,#35819,#35820,#35821,#35822,
#35823,#35824,#35825,#35826,#35827,#35828,#35829,#35830,#35831,#35832,#35833,
#35834,#35835,#35836,#35837,#35838,#35839,#35840,#35841,#35842,#35843,#35844,
#35845,#35846,#35847,#35848,#35849,#35850,#35851,#35852,#35853,#35854,#35855,
#35856,#35857,#35858,#35859,#35860,#35861,#35862,#35863,#35864,#35865),
(#35866,#35867,#35868,#35869,#35870,#35871,#35872,#35873,#35874,#35875,
#35876,#35877,#35878,#35879,#35880,#35881,#35882,#35883,#35884,#35885,#35886,
#35887,#35888,#35889,#35890,#35891,#35892,#35893,#35894,#35895,#35896,#35897,
#35898,#35899,#35900,#35901,#35902,#35903,#35904,#35905,#35906,#35907,#35908,
#35909,#35910,#35911,#35912,#35913,#35914,#35915,#35916,#35917,#35918,#35919,
#35920,#35921,#35922,#35923,#35924,#35925,#35926,#35927,#35928,#35929,#35930,
#35931,#35932,#35933,#35934,#35935,#35936,#35937,#35938,#35939,#35940,#35941,
#35942,#35943,#35944,#35945,#35946,#35947,#35948,#35949,#35950,#35951,#35952,
#35953,#35954,#35955,#35956,#35957,#35958,#35959,#35960,#35961,#35962,#35963,
#35964,#35965,#35966,#35967,#35968,#35969,#35970,#35971,#35972,#35973,#35974,
#35975,#35976,#35977,#35978,#35979,#35980,#35981,#35982,#35983,#35984,#35985,
#35986,#35987,#35988,#35989,#35990,#35991,#35992,#35993,#35994,#35995,#35996,
#35997,#35998,#35999,#36000,#36001,#36002,#36003,#36004,#36005,#36006,#36007,
#36008,#36009,#36010,#36011,#36012,#36013,#36014,#36015,#36016,#36017,#36018,
#36019,#36020,#36021,#36022,#36023),(#36024,#36025,#36026,#36027,#36028,
#36029,#36030,#36031,#36032,#36033,#36034,#36035,#36036,#36037,#36038,#36039,
#36040,#36041,#36042,#36043,#36044,#36045,#36046,#36047,#36048,#36049,#36050,
#36051,#36052,#36053,#36054,#36055,#36056,#36057,#36058,#36059,#36060,#36061,
#36062,#36063,#36064,#36065,#36066,#36067,#36068,#36069,#36070,#36071,#36072,
#36073,#36074,#36075,#36076,#36077,#36078,#36079,#36080,#36081,#36082,#36083,
#36084,#36085,#36086,#36087,#36088,#36089,#36090,#36091,#36092,#36093,#36094,
#36095,#36096,#36097,#36098,#36099,#36100,#36101,#36102,#36103,#36104,#36105,
#36106,#36107,#36108,#36109,#36110,#36111,#36112,#36113,#36114,#36115,#36116,
#36117,#36118,#36119,#36120,#36121,#36122,#36123,#36124,#36125,#36126,#36127,
#36128,#36129,#36130,#36131,#36132,#36133,#36134,#36135,#36136,#36137,#36138,
#36139,#36140,#36141,#36142,#36143,#36144,#36145,#36146,#36147,#36148,#36149,
#36150,#36151,#36152,#36153,#36154,#36155,#36156,#36157,#36158,#36159,#36160,
#36161,#36162,#36163,#36164,#36165,#36166,#36167,#36168,#36169,#36170,#36171,
#36172,#36173,#36174,#36175,#36176,#36177,#36178,#36179,#36180,#36181),
(#36182,#36183,#36184,#36185,#36186,#36187,#36188,#36189,#36190,#36191,
#36192,#36193,#36194,#36195,#36196,#36197,#36198,#36199,#36200,#36201,#36202,
#36203,#36204,#36205,#36206,#36207,#36208,#36209,#36210,#36211,#36212,#36213,
#36214,#36215,#36216,#36217,#36218,#36219,#36220,#36221,#36222,#36223,#36224,
#36225,#36226,#36227,#36228,#36229,#36230,#36231,#36232,#36233,#36234,#36235,
#36236,#36237,#36238,#36239,#36240,#36241,#36242,#36243,#36244,#36245,#36246,
#36247,#36248,#36249,#36250,#36251,#36252,#36253,#36254,#36255,#36256,#36257,
#36258,#36259,#36260,#36261,#36262,#36263,#36264,#36265,#36266,#36267,#36268,
#36269,#36270,#36271,#36272,#36273,#36274,#36275,#36276,#36277,#36278,#36279,
#36280,#36281,#36282,#36283,#36284,#36285,#36286,#36287,#36288,#36289,#36290,
#36291,#36292,#36293,#36294,#36295,#36296,#36297,#36298,#36299,#36300,#36301,
#36302,#36303,#36304,#36305,#36306,#36307,#36308,#36309,#36310,#36311,#36312,
#36313,#36314,#36315,#36316,#36317,#36318,#36319,#36320,#36321,#36322,#36323,
#36324,#36325,#36326,#36327,#36328,#36329,#36330,#36331,#36332,#36333,#36334,
#36335,#36336,#36337,#36338,#36339)),.UNSPECIFIED.,.F.,.F.,.F.,(4,4),(4,
1,1,1,1,1,1,1,1,1,1,1,1,1,1,1,1,1,1,1,1,1,1,1,1,1,1,1,1,1,1,1,1,1,1,1,1,
1,1,1,1,1,1,1,1,1,1,1,1,1,1,1,1,1,1,1,1,1,1,1,1,1,1,1,1,1,1,1,1,1,1,1,1,
1,1,1,1,1,1,1,1,1,1,1,1,1,1,1,1,1,1,1,1,1,1,1,1,1,1,1,1,1,1,1,1,1,1,1,1,
1,1,1,1,1,1,1,1,1,1,1,1,1,1,1,1,1,1,1,1,1,1,1,1,1,1,1,1,1,1,1,1,1,1,1,1,
1,1,1,1,1,1,1,1,1,1,4),(0.,0.0658467982010769),(11.6150328478184,12.61338032228,
13.6117277967416,14.6100752712031,15.6084227456647,16.6067702201263,17.6051176945879,
18.6034651690495,19.6018126435111,20.6001601179726,21.5985075924342,22.5968550668958,
23.5952025413574,24.593550015819,25.5918974902806,26.5902449647422,27.5885924392037,
28.5869399136653,29.5852873881269,30.5836348625885,31.5819823370501,32.5803298115117,
33.5786772859732,34.5770247604348,35.5753722348964,36.573719709358,37.5720671838196,
38.5704146582812,39.5687621327428,40.5671096072043,41.5654570816659,42.5638045561275,
43.5621520305891,44.5604995050507,45.5588469795123,46.5571944539738,47.5555419284354,
48.553889402897,49.5522368773586,50.5505843518202,51.5489318262818,52.5472793007434,
53.545626775205,54.5439742496665,55.5423217241281,56.5406691985897,57.5390166730513,
58.5373641475129,59.5357116219745,60.534059096436,61.5324065708976,62.5307540453592,
63.5291015198208,64.5274489942824,65.525796468744,66.5241439432056,67.5224914176671,
68.5208388921287,69.5191863665903,70.5175338410519,71.5158813155135,72.5142287899751,
73.5125762644366,74.5109237388982,75.5092712133598,76.5076186878214,77.505966162283,
78.5043136367446,79.5026611112062,80.5010085856677,81.4993560601293,82.4977035345909,
83.4960510090525,84.4943984835141,85.4927459579757,86.4910934324373,87.4894409068988,
88.4877883813604,89.486135855822,90.4844833302836,91.4828308047452,92.4811782792068,
93.4795257536684,94.4778732281299,95.4762207025915,96.4745681770531,97.4729156515147,
98.4712631259763,99.4696106004379,100.467958074899,101.466305549361,102.464653023823,
103.463000498284,104.461347972746,105.459695447207,106.458042921669,107.456390396131,
108.454737870592,109.453085345054,110.451432819515,111.449780293977,112.448127768438,
113.4464752429,114.444822717362,115.443170191823,116.441517666285,117.439865140746,
118.438212615208,119.43656008967,120.434907564131,121.433255038593,122.431602513054,
123.429949987516,124.428297461977,125.426644936439,126.424992410901,127.423339885362,
128.421687359824,129.420034834285,130.418382308747,131.416729783209,132.41507725767,
133.413424732132,134.411772206593,135.410119681055,136.408467155516,137.406814629978,
138.40516210444,139.403509578901,140.401857053363,141.400204527824,142.398552002286,
143.396899476748,144.395246951209,145.393594425671,146.391941900132,147.390289374594,
148.388636849056,149.386984323517,150.385331797979,151.38367927244,152.382026746902,
153.380374221363,154.378721695825,155.377069170287,156.375416644748,157.37376411921,
158.372111593671,159.370459068133,160.368806542595,161.367154017056,162.365501491518,
163.363848965979,164.362196440441,165.360543914902,166.358891389364),
 .UNSPECIFIED.);
#343=B_SPLINE_SURFACE_WITH_KNOTS('',3,3,((#36477,#36478,#36479,#36480,#36481,
#36482,#36483,#36484,#36485,#36486,#36487,#36488,#36489,#36490,#36491,#36492,
#36493,#36494,#36495,#36496,#36497,#36498,#36499,#36500,#36501,#36502,#36503,
#36504,#36505,#36506,#36507,#36508,#36509,#36510,#36511,#36512,#36513,#36514,
#36515,#36516,#36517,#36518,#36519,#36520,#36521,#36522,#36523,#36524,#36525,
#36526,#36527,#36528,#36529,#36530,#36531,#36532,#36533,#36534,#36535,#36536,
#36537,#36538,#36539,#36540,#36541,#36542,#36543,#36544,#36545,#36546,#36547,
#36548,#36549,#36550,#36551,#36552,#36553,#36554,#36555,#36556,#36557,#36558,
#36559,#36560,#36561,#36562,#36563,#36564,#36565,#36566,#36567,#36568,#36569,
#36570,#36571,#36572,#36573,#36574,#36575,#36576,#36577,#36578,#36579,#36580,
#36581,#36582,#36583,#36584,#36585,#36586,#36587,#36588,#36589,#36590,#36591,
#36592,#36593,#36594,#36595,#36596,#36597,#36598,#36599,#36600,#36601,#36602,
#36603,#36604,#36605,#36606,#36607,#36608,#36609,#36610,#36611,#36612,#36613,
#36614,#36615,#36616,#36617,#36618,#36619,#36620,#36621,#36622,#36623,#36624,
#36625,#36626,#36627,#36628,#36629,#36630,#36631,#36632,#36633,#36634,#36635,
#36636),(#36637,#36638,#36639,#36640,#36641,#36642,#36643,#36644,#36645,
#36646,#36647,#36648,#36649,#36650,#36651,#36652,#36653,#36654,#36655,#36656,
#36657,#36658,#36659,#36660,#36661,#36662,#36663,#36664,#36665,#36666,#36667,
#36668,#36669,#36670,#36671,#36672,#36673,#36674,#36675,#36676,#36677,#36678,
#36679,#36680,#36681,#36682,#36683,#36684,#36685,#36686,#36687,#36688,#36689,
#36690,#36691,#36692,#36693,#36694,#36695,#36696,#36697,#36698,#36699,#36700,
#36701,#36702,#36703,#36704,#36705,#36706,#36707,#36708,#36709,#36710,#36711,
#36712,#36713,#36714,#36715,#36716,#36717,#36718,#36719,#36720,#36721,#36722,
#36723,#36724,#36725,#36726,#36727,#36728,#36729,#36730,#36731,#36732,#36733,
#36734,#36735,#36736,#36737,#36738,#36739,#36740,#36741,#36742,#36743,#36744,
#36745,#36746,#36747,#36748,#36749,#36750,#36751,#36752,#36753,#36754,#36755,
#36756,#36757,#36758,#36759,#36760,#36761,#36762,#36763,#36764,#36765,#36766,
#36767,#36768,#36769,#36770,#36771,#36772,#36773,#36774,#36775,#36776,#36777,
#36778,#36779,#36780,#36781,#36782,#36783,#36784,#36785,#36786,#36787,#36788,
#36789,#36790,#36791,#36792,#36793,#36794,#36795,#36796),(#36797,#36798,
#36799,#36800,#36801,#36802,#36803,#36804,#36805,#36806,#36807,#36808,#36809,
#36810,#36811,#36812,#36813,#36814,#36815,#36816,#36817,#36818,#36819,#36820,
#36821,#36822,#36823,#36824,#36825,#36826,#36827,#36828,#36829,#36830,#36831,
#36832,#36833,#36834,#36835,#36836,#36837,#36838,#36839,#36840,#36841,#36842,
#36843,#36844,#36845,#36846,#36847,#36848,#36849,#36850,#36851,#36852,#36853,
#36854,#36855,#36856,#36857,#36858,#36859,#36860,#36861,#36862,#36863,#36864,
#36865,#36866,#36867,#36868,#36869,#36870,#36871,#36872,#36873,#36874,#36875,
#36876,#36877,#36878,#36879,#36880,#36881,#36882,#36883,#36884,#36885,#36886,
#36887,#36888,#36889,#36890,#36891,#36892,#36893,#36894,#36895,#36896,#36897,
#36898,#36899,#36900,#36901,#36902,#36903,#36904,#36905,#36906,#36907,#36908,
#36909,#36910,#36911,#36912,#36913,#36914,#36915,#36916,#36917,#36918,#36919,
#36920,#36921,#36922,#36923,#36924,#36925,#36926,#36927,#36928,#36929,#36930,
#36931,#36932,#36933,#36934,#36935,#36936,#36937,#36938,#36939,#36940,#36941,
#36942,#36943,#36944,#36945,#36946,#36947,#36948,#36949,#36950,#36951,#36952,
#36953,#36954,#36955,#36956),(#36957,#36958,#36959,#36960,#36961,#36962,
#36963,#36964,#36965,#36966,#36967,#36968,#36969,#36970,#36971,#36972,#36973,
#36974,#36975,#36976,#36977,#36978,#36979,#36980,#36981,#36982,#36983,#36984,
#36985,#36986,#36987,#36988,#36989,#36990,#36991,#36992,#36993,#36994,#36995,
#36996,#36997,#36998,#36999,#37000,#37001,#37002,#37003,#37004,#37005,#37006,
#37007,#37008,#37009,#37010,#37011,#37012,#37013,#37014,#37015,#37016,#37017,
#37018,#37019,#37020,#37021,#37022,#37023,#37024,#37025,#37026,#37027,#37028,
#37029,#37030,#37031,#37032,#37033,#37034,#37035,#37036,#37037,#37038,#37039,
#37040,#37041,#37042,#37043,#37044,#37045,#37046,#37047,#37048,#37049,#37050,
#37051,#37052,#37053,#37054,#37055,#37056,#37057,#37058,#37059,#37060,#37061,
#37062,#37063,#37064,#37065,#37066,#37067,#37068,#37069,#37070,#37071,#37072,
#37073,#37074,#37075,#37076,#37077,#37078,#37079,#37080,#37081,#37082,#37083,
#37084,#37085,#37086,#37087,#37088,#37089,#37090,#37091,#37092,#37093,#37094,
#37095,#37096,#37097,#37098,#37099,#37100,#37101,#37102,#37103,#37104,#37105,
#37106,#37107,#37108,#37109,#37110,#37111,#37112,#37113,#37114,#37115,#37116)),
 .UNSPECIFIED.,.F.,.F.,.F.,(4,4),(4,1,1,1,1,1,1,1,1,1,1,1,1,1,1,1,1,1,1,
1,1,1,1,1,1,1,1,1,1,1,1,1,1,1,1,1,1,1,1,1,1,1,1,1,1,1,1,1,1,1,1,1,1,1,1,
1,1,1,1,1,1,1,1,1,1,1,1,1,1,1,1,1,1,1,1,1,1,1,1,1,1,1,1,1,1,1,1,1,1,1,1,
1,1,1,1,1,1,1,1,1,1,1,1,1,1,1,1,1,1,1,1,1,1,1,1,1,1,1,1,1,1,1,1,1,1,1,1,
1,1,1,1,1,1,1,1,1,1,1,1,1,1,1,1,1,1,1,1,1,1,1,1,1,1,1,1,1,1,4),(0.,0.0658467982010769),
(8.30747755240114,9.30628326397092,10.3050889755407,11.3038946871105,12.3027003986802,
13.30150611025,14.3003118218198,15.2991175333896,16.2979232449593,17.2967289565291,
18.2955346680989,19.2943403796687,20.2931460912385,21.2919518028082,22.290757514378,
23.2895632259478,24.2883689375176,25.2871746490873,26.2859803606571,27.2847860722269,
28.2835917837967,29.2823974953664,30.2812032069362,31.280008918506,32.2788146300758,
33.2776203416455,34.2764260532153,35.2752317647851,36.2740374763549,37.2728431879246,
38.2716488994944,39.2704546110642,40.269260322634,41.2680660342037,42.2668717457735,
43.2656774573433,44.2644831689131,45.2632888804829,46.2620945920526,47.2609003036224,
48.2597060151922,49.258511726762,50.2573174383317,51.2561231499015,52.2549288614713,
53.2537345730411,54.2525402846108,55.2513459961806,56.2501517077504,57.2489574193202,
58.2477631308899,59.2465688424597,60.2453745540295,61.2441802655993,62.242985977169,
63.2417916887388,64.2405974003086,65.2394031118784,66.2382088234481,67.2370145350179,
68.2358202465877,69.2346259581575,70.2334316697272,71.232237381297,72.2310430928668,
73.2298488044366,74.2286545160063,75.2274602275761,76.2262659391459,77.2250716507157,
78.2238773622854,79.2226830738552,80.221488785425,81.2202944969948,82.2191002085646,
83.2179059201343,84.2167116317041,85.2155173432739,86.2143230548436,87.2131287664134,
88.2119344779832,89.210740189553,90.2095459011228,91.2083516126925,92.2071573242623,
93.2059630358321,94.2047687474019,95.2035744589716,96.2023801705414,97.2011858821112,
98.199991593681,99.1987973052507,100.197603016821,101.19640872839,102.19521443996,
103.19402015153,104.1928258631,105.191631574669,106.190437286239,107.189242997809,
108.188048709379,109.186854420948,110.185660132518,111.184465844088,112.183271555658,
113.182077267228,114.180882978797,115.179688690367,116.178494401937,117.177300113507,
118.176105825076,119.174911536646,120.173717248216,121.172522959786,122.171328671356,
123.170134382925,124.168940094495,125.167745806065,126.166551517635,127.165357229204,
128.164162940774,129.162968652344,130.161774363914,131.160580075484,132.159385787053,
133.158191498623,134.156997210193,135.155802921763,136.154608633332,137.153414344902,
138.152220056472,139.151025768042,140.149831479612,141.148637191181,142.147442902751,
143.146248614321,144.145054325891,145.14386003746,146.14266574903,147.1414714606,
148.14027717217,149.13908288374,150.137888595309,151.136694306879,152.135500018449,
153.134305730019,154.133111441588,155.131917153158,156.130722864728,157.129528576298,
158.128334287868,159.127139999437,160.125945711007,161.124751422577,162.123557134147,
163.122362845716,164.121168557286,165.119974268856),.UNSPECIFIED.);
#536=B_SPLINE_CURVE_WITH_KNOTS('',3,(#33621,#33622,#33623,#33624,#33625,
#33626,#33627,#33628,#33629,#33630),.UNSPECIFIED.,.F.,.F.,(4,3,3,4),(-4.09293042013064,
-3.99338989784634,-2.99504242338475,-2.06863817490912),.UNSPECIFIED.);
#537=B_SPLINE_CURVE_WITH_KNOTS('',3,(#33633,#33634,#33635,#33636,#33637,
#33638,#33639),.UNSPECIFIED.,.F.,.F.,(4,3,4),(0.,0.998805711569778,1.11730040836826),
 .UNSPECIFIED.);
#538=B_SPLINE_CURVE_WITH_KNOTS('',3,(#33644,#33645,#33646,#33647,#33648,
#33649,#33650,#33651,#33652,#33653,#33654,#33655,#33656,#33657,#33658,#33659,
#33660,#33661,#33662,#33663,#33664,#33665),.UNSPECIFIED.,.F.,.F.,(4,3,3,
3,3,3,3,4),(-10.3761157273102,-9.98347474461585,-8.98512727015427,-7.98677979569268,
-6.98843232123109,-5.99008484676951,-4.99173737230793,-4.09293042013064),
 .UNSPECIFIED.);
#539=B_SPLINE_CURVE_WITH_KNOTS('',3,(#33666,#33667,#33668,#33669,#33670,
#33671,#33672,#33673,#33674,#33675,#33676,#33677,#33678,#33679,#33680,#33681,
#33682,#33683,#33684,#33685,#33686,#33687),.UNSPECIFIED.,.F.,.F.,(4,3,3,
3,3,3,3,4),(1.11730040836826,1.99761142313956,2.99641713470934,3.99522284627912,
4.99402855784889,5.99283426941867,6.99163998098846,7.40048571554784),
 .UNSPECIFIED.);
#540=B_SPLINE_CURVE_WITH_KNOTS('',3,(#33692,#33693,#33694,#33695,#33696,
#33697,#33698,#33699,#33700,#33701,#33702,#33703,#33704,#33705,#33706,#33707,
#33708,#33709,#33710,#33711,#33712,#33713),.UNSPECIFIED.,.F.,.F.,(4,3,3,
3,3,3,3,4),(-16.6593010344898,-15.9735595913854,-14.9752121169238,-13.9768646424622,
-12.9785171680006,-11.980169693539,-10.9818222190774,-10.3761157273102),
 .UNSPECIFIED.);
#541=B_SPLINE_CURVE_WITH_KNOTS('',3,(#33714,#33715,#33716,#33717,#33718,
#33719,#33720,#33721,#33722,#33723,#33724,#33725,#33726,#33727,#33728,#33729,
#33730,#33731,#33732,#33733,#33734,#33735),.UNSPECIFIED.,.F.,.F.,(4,3,3,
3,3,3,3,4),(7.40048571554784,7.99044569255823,8.989251404128,9.98805711569777,
10.9868628272675,11.9856685388373,12.9844742504071,13.6836710227274),
 .UNSPECIFIED.);
#542=B_SPLINE_CURVE_WITH_KNOTS('',3,(#33740,#33741,#33742,#33743,#33744,
#33745,#33746,#33747,#33748,#33749,#33750,#33751,#33752,#33753,#33754,#33755,
#33756,#33757,#33758,#33759,#33760,#33761),.UNSPECIFIED.,.F.,.F.,(4,3,3,
3,3,3,3,4),(-22.9424863416694,-21.9636444381549,-20.9652969636933,-19.9669494892317,
-18.9686020147701,-17.9702545403085,-16.9719070658469,-16.6593010344898),
 .UNSPECIFIED.);
#543=B_SPLINE_CURVE_WITH_KNOTS('',3,(#33762,#33763,#33764,#33765,#33766,
#33767,#33768,#33769,#33770,#33771,#33772,#33773,#33774,#33775,#33776,#33777,
#33778,#33779,#33780,#33781,#33782,#33783),.UNSPECIFIED.,.F.,.F.,(4,3,3,
3,3,3,3,4),(13.6836710227274,13.9832799619769,14.9820856735466,15.9808913851164,
16.9796970966862,17.978502808256,18.9773085198257,19.966856329907),
 .UNSPECIFIED.);
#544=B_SPLINE_CURVE_WITH_KNOTS('',3,(#33788,#33789,#33790,#33791,#33792,
#33793,#33794,#33795,#33796,#33797,#33798,#33799,#33800,#33801,#33802,#33803,
#33804,#33805,#33806,#33807,#33808,#33809,#33810,#33811,#33812),
 .UNSPECIFIED.,.F.,.F.,(4,3,3,3,3,3,3,3,4),(-29.225671648849,-28.952076759386,
-27.9537292849244,-26.9553818104628,-25.9570343360012,-24.9586868615396,
-23.960339387078,-22.9619919126165,-22.9424863416694),.UNSPECIFIED.);
#545=B_SPLINE_CURVE_WITH_KNOTS('',3,(#33813,#33814,#33815,#33816,#33817,
#33818,#33819,#33820,#33821,#33822,#33823,#33824,#33825,#33826,#33827,#33828,
#33829,#33830,#33831,#33832,#33833,#33834,#33835,#33836,#33837),
 .UNSPECIFIED.,.F.,.F.,(4,3,3,3,3,3,3,3,4),(19.966856329907,19.9761142313955,
20.9749199429653,21.9737256545351,22.9725313661048,23.9713370776746,24.9701427892444,
25.9689485008142,26.2500416370866),.UNSPECIFIED.);
#546=B_SPLINE_CURVE_WITH_KNOTS('',3,(#33842,#33843,#33844,#33845,#33846,
#33847,#33848,#33849,#33850,#33851,#33852,#33853,#33854,#33855,#33856,#33857,
#33858,#33859,#33860,#33861,#33862,#33863),.UNSPECIFIED.,.F.,.F.,(4,3,3,
3,3,3,3,4),(-35.5088569560286,-34.9421616061555,-33.9438141316939,-32.9454666572323,
-31.9471191827707,-30.9487717083091,-29.9504242338475,-29.225671648849),
 .UNSPECIFIED.);
#547=B_SPLINE_CURVE_WITH_KNOTS('',3,(#33864,#33865,#33866,#33867,#33868,
#33869,#33870,#33871,#33872,#33873,#33874,#33875,#33876,#33877,#33878,#33879,
#33880,#33881,#33882,#33883,#33884,#33885),.UNSPECIFIED.,.F.,.F.,(4,3,3,
3,3,3,3,4),(26.2500416370866,26.9677542123839,27.9665599239537,28.9653656355235,
29.9641713470933,30.9629770586631,31.9617827702328,32.5332269442662),
 .UNSPECIFIED.);
#548=B_SPLINE_CURVE_WITH_KNOTS('',3,(#33890,#33891,#33892,#33893,#33894,
#33895,#33896,#33897,#33898,#33899,#33900,#33901,#33902,#33903,#33904,#33905,
#33906,#33907,#33908,#33909,#33910,#33911),.UNSPECIFIED.,.F.,.F.,(4,3,3,
3,3,3,3,4),(-41.7920422632082,-40.932246452925,-39.9338989784634,-38.9355515040018,
-37.9372040295402,-36.9388565550787,-35.9405090806171,-35.5088569560286),
 .UNSPECIFIED.);
#549=B_SPLINE_CURVE_WITH_KNOTS('',3,(#33912,#33913,#33914,#33915,#33916,
#33917,#33918,#33919,#33920,#33921,#33922,#33923,#33924,#33925,#33926,#33927,
#33928,#33929,#33930,#33931,#33932,#33933),.UNSPECIFIED.,.F.,.F.,(4,3,3,
3,3,3,3,4),(32.5332269442662,32.9605884818026,33.9593941933724,34.9581999049422,
35.9570056165119,36.9558113280817,37.9546170396515,38.8164122514458),
 .UNSPECIFIED.);
#550=B_SPLINE_CURVE_WITH_KNOTS('',3,(#33938,#33939,#33940,#33941,#33942,
#33943,#33944,#33945,#33946,#33947,#33948,#33949,#33950,#33951,#33952,#33953,
#33954,#33955,#33956,#33957,#33958,#33959,#33960,#33961,#33962),
 .UNSPECIFIED.,.F.,.F.,(4,3,3,3,3,3,3,3,4),(-48.0752275703878,-47.9206787741561,
-46.9223312996945,-45.9239838252329,-44.9256363507713,-43.9272888763097,
-42.9289414018482,-41.9305939273866,-41.7920422632082),.UNSPECIFIED.);
#551=B_SPLINE_CURVE_WITH_KNOTS('',3,(#33963,#33964,#33965,#33966,#33967,
#33968,#33969,#33970,#33971,#33972,#33973,#33974,#33975,#33976,#33977,#33978,
#33979,#33980,#33981,#33982,#33983,#33984,#33985,#33986,#33987),
 .UNSPECIFIED.,.F.,.F.,(4,3,3,3,3,3,3,3,4),(38.8164122514458,38.9534227512213,
39.952228462791,40.9510341743608,41.9498398859306,42.9486455975004,43.9474513090701,
44.9462570206399,45.0995975586254),.UNSPECIFIED.);
#552=B_SPLINE_CURVE_WITH_KNOTS('',3,(#33992,#33993,#33994,#33995,#33996,
#33997,#33998,#33999,#34000,#34001,#34002,#34003,#34004,#34005,#34006,#34007,
#34008,#34009,#34010,#34011,#34012,#34013),.UNSPECIFIED.,.F.,.F.,(4,3,3,
3,3,3,3,4),(-54.3584128775673,-53.9107636209256,-52.912416146464,-51.9140686720024,
-50.9157211975408,-49.9173737230793,-48.9190262486177,-48.0752275703878),
 .UNSPECIFIED.);
#553=B_SPLINE_CURVE_WITH_KNOTS('',3,(#34014,#34015,#34016,#34017,#34018,
#34019,#34020,#34021,#34022,#34023,#34024,#34025,#34026,#34027,#34028,#34029,
#34030,#34031,#34032,#34033,#34034,#34035),.UNSPECIFIED.,.F.,.F.,(4,3,3,
3,3,3,3,4),(45.0995975586254,45.9450627322097,46.9438684437795,47.9426741553493,
48.941479866919,49.9402855784888,50.9390912900586,51.382782865805),
 .UNSPECIFIED.);
#554=B_SPLINE_CURVE_WITH_KNOTS('',3,(#34040,#34041,#34042,#34043,#34044,
#34045,#34046,#34047,#34048,#34049,#34050,#34051,#34052,#34053,#34054,#34055,
#34056,#34057,#34058,#34059,#34060,#34061),.UNSPECIFIED.,.F.,.F.,(4,3,3,
3,3,3,3,4),(-60.6415981847469,-59.9008484676951,-58.9025009932335,-57.9041535187719,
-56.9058060443103,-55.9074585698488,-54.9091110953872,-54.3584128775673),
 .UNSPECIFIED.);
#555=B_SPLINE_CURVE_WITH_KNOTS('',3,(#34062,#34063,#34064,#34065,#34066,
#34067,#34068,#34069,#34070,#34071,#34072,#34073,#34074,#34075,#34076,#34077,
#34078,#34079,#34080,#34081,#34082,#34083),.UNSPECIFIED.,.F.,.F.,(4,3,3,
3,3,3,3,4),(51.382782865805,51.9378970016283,52.9367027131981,53.9355084247679,
54.9343141363377,55.9331198479074,56.9319255594772,57.6659681729846),
 .UNSPECIFIED.);
#556=B_SPLINE_CURVE_WITH_KNOTS('',3,(#34088,#34089,#34090,#34091,#34092,
#34093,#34094,#34095,#34096,#34097,#34098,#34099,#34100,#34101,#34102,#34103,
#34104,#34105,#34106,#34107,#34108,#34109,#34110,#34111,#34112),
 .UNSPECIFIED.,.F.,.F.,(4,3,3,3,3,3,3,3,4),(-66.9247834919265,-66.8892807889262,
-65.8909333144646,-64.892585840003,-63.8942383655414,-62.8958908910799,
-61.8975434166182,-60.8991959421567,-60.6415981847469),.UNSPECIFIED.);
#557=B_SPLINE_CURVE_WITH_KNOTS('',3,(#34113,#34114,#34115,#34116,#34117,
#34118,#34119,#34120,#34121,#34122,#34123,#34124,#34125,#34126,#34127,#34128,
#34129,#34130,#34131,#34132,#34133,#34134,#34135,#34136,#34137),
 .UNSPECIFIED.,.F.,.F.,(4,3,3,3,3,3,3,3,4),(57.6659681729846,57.930731271047,
58.9295369826168,59.9283426941866,60.9271484057563,61.9259541173261,62.9247598288959,
63.9235655404657,63.9491534801642),.UNSPECIFIED.);
#558=B_SPLINE_CURVE_WITH_KNOTS('',3,(#34142,#34143,#34144,#34145,#34146,
#34147,#34148,#34149,#34150,#34151,#34152,#34153,#34154,#34155,#34156,#34157,
#34158,#34159,#34160,#34161,#34162,#34163),.UNSPECIFIED.,.F.,.F.,(4,3,3,
3,3,3,3,4),(-73.2079687991061,-72.8793656356957,-71.8810181612341,-70.8826706867726,
-69.8843232123109,-68.8859757378494,-67.8876282633878,-66.9247834919265),
 .UNSPECIFIED.);
#559=B_SPLINE_CURVE_WITH_KNOTS('',3,(#34164,#34165,#34166,#34167,#34168,
#34169,#34170,#34171,#34172,#34173,#34174,#34175,#34176,#34177,#34178,#34179,
#34180,#34181,#34182,#34183,#34184,#34185),.UNSPECIFIED.,.F.,.F.,(4,3,3,
3,3,3,3,4),(63.9491534801642,64.9223712520354,65.9211769636052,66.919982675175,
67.9187883867447,68.9175940983145,69.9163998098843,70.2323387873437),
 .UNSPECIFIED.);
#560=B_SPLINE_CURVE_WITH_KNOTS('',3,(#34190,#34191,#34192,#34193,#34194,
#34195,#34196,#34197,#34198,#34199,#34200,#34201,#34202,#34203,#34204,#34205,
#34206,#34207,#34208,#34209,#34210,#34211),.UNSPECIFIED.,.F.,.F.,(4,3,3,
3,3,3,3,4),(-79.4911541062857,-78.8694504824652,-77.8711030080036,-76.8727555335421,
-75.8744080590805,-74.8760605846189,-73.8777131101573,-73.2079687991061),
 .UNSPECIFIED.);
#561=B_SPLINE_CURVE_WITH_KNOTS('',3,(#34212,#34213,#34214,#34215,#34216,
#34217,#34218,#34219,#34220,#34221,#34222,#34223,#34224,#34225,#34226,#34227,
#34228,#34229,#34230,#34231,#34232,#34233),.UNSPECIFIED.,.F.,.F.,(4,3,3,
3,3,3,3,4),(70.2323387873437,70.9152055214541,71.9140112330238,72.9128169445936,
73.9116226561634,74.9104283677332,75.909234079303,76.5155240945233),
 .UNSPECIFIED.);
#562=B_SPLINE_CURVE_WITH_KNOTS('',3,(#34238,#34239,#34240,#34241,#34242,
#34243,#34244,#34245,#34246,#34247,#34248,#34249,#34250,#34251,#34252,#34253,
#34254,#34255,#34256,#34257,#34258,#34259),.UNSPECIFIED.,.F.,.F.,(4,3,3,
3,3,3,3,4),(-85.7743394134653,-84.8595353292348,-83.8611878547731,-82.8628403803116,
-81.86449290585,-80.8661454313884,-79.8677979569268,-79.4911541062857),
 .UNSPECIFIED.);
#563=B_SPLINE_CURVE_WITH_KNOTS('',3,(#34260,#34261,#34262,#34263,#34264,
#34265,#34266,#34267,#34268,#34269,#34270,#34271,#34272,#34273,#34274,#34275,
#34276,#34277,#34278,#34279,#34280,#34281),.UNSPECIFIED.,.F.,.F.,(4,3,3,
3,3,3,3,4),(76.5155240945233,76.9080397908727,77.9068455024425,78.9056512140123,
79.9044569255821,80.9032626371518,81.9020683487216,82.7987094017029),
 .UNSPECIFIED.);
#564=B_SPLINE_CURVE_WITH_KNOTS('',3,(#34286,#34287,#34288,#34289,#34290,
#34291,#34292,#34293,#34294,#34295,#34296,#34297,#34298,#34299,#34300,#34301,
#34302,#34303,#34304,#34305,#34306,#34307,#34308,#34309,#34310),
 .UNSPECIFIED.,.F.,.F.,(4,3,3,3,3,3,3,3,4),(-92.0575247206449,-91.8479676504658,
-90.8496201760042,-89.8512727015427,-88.8529252270811,-87.8545777526195,
-86.8562302781579,-85.8578828036963,-85.7743394134653),.UNSPECIFIED.);
#565=B_SPLINE_CURVE_WITH_KNOTS('',3,(#34311,#34312,#34313,#34314,#34315,
#34316,#34317,#34318,#34319,#34320,#34321,#34322,#34323,#34324,#34325,#34326,
#34327,#34328,#34329,#34330,#34331,#34332,#34333,#34334,#34335),
 .UNSPECIFIED.,.F.,.F.,(4,3,3,3,3,3,3,3,4),(82.7987094017029,82.9008740602914,
83.8996797718612,84.8984854834309,85.8972911950007,86.8960969065705,87.8949026181403,
88.8937083297101,89.0818947088825),.UNSPECIFIED.);
#566=B_SPLINE_CURVE_WITH_KNOTS('',3,(#34340,#34341,#34342,#34343,#34344,
#34345,#34346,#34347,#34348,#34349,#34350,#34351,#34352,#34353,#34354,#34355,
#34356,#34357,#34358,#34359,#34360,#34361),.UNSPECIFIED.,.F.,.F.,(4,3,3,
3,3,3,3,4),(-98.3407100278245,-97.8380524972353,-96.8397050227737,-95.8413575483122,
-94.8430100738506,-93.844662599389,-92.8463151249274,-92.0575247206449),
 .UNSPECIFIED.);
#567=B_SPLINE_CURVE_WITH_KNOTS('',3,(#34362,#34363,#34364,#34365,#34366,
#34367,#34368,#34369,#34370,#34371,#34372,#34373,#34374,#34375,#34376,#34377,
#34378,#34379,#34380,#34381,#34382,#34383),.UNSPECIFIED.,.F.,.F.,(4,3,3,
3,3,3,3,4),(89.0818947088825,89.8925140412798,90.8913197528496,91.8901254644194,
92.8889311759891,93.8877368875589,94.8865425991287,95.3650800160621),
 .UNSPECIFIED.);
#568=B_SPLINE_CURVE_WITH_KNOTS('',3,(#34388,#34389,#34390,#34391,#34392,
#34393,#34394,#34395,#34396,#34397,#34398,#34399,#34400,#34401,#34402,#34403,
#34404,#34405,#34406,#34407,#34408,#34409),.UNSPECIFIED.,.F.,.F.,(4,3,3,
3,3,3,3,4),(-104.623895335004,-103.828137344005,-102.829789869543,-101.831442395082,
-100.83309492062,-99.8347474461585,-98.8363999716969,-98.3407100278245),
 .UNSPECIFIED.);
#569=B_SPLINE_CURVE_WITH_KNOTS('',3,(#34410,#34411,#34412,#34413,#34414,
#34415,#34416,#34417,#34418,#34419,#34420,#34421,#34422,#34423,#34424,#34425,
#34426,#34427,#34428,#34429,#34430,#34431),.UNSPECIFIED.,.F.,.F.,(4,3,3,
3,3,3,3,4),(95.3650800160621,95.8853483106984,96.8841540222682,97.882959733838,
98.8817654454078,99.8805711569776,100.879376868547,101.648265323242),
 .UNSPECIFIED.);
#570=B_SPLINE_CURVE_WITH_KNOTS('',3,(#34436,#34437,#34438,#34439,#34440,
#34441,#34442,#34443,#34444,#34445,#34446,#34447,#34448,#34449,#34450,#34451,
#34452,#34453,#34454,#34455,#34456,#34457,#34458,#34459,#34460),
 .UNSPECIFIED.,.F.,.F.,(4,3,3,3,3,3,3,3,4),(-110.907080642184,-110.816569665236,
-109.818222190774,-108.819874716313,-107.821527241851,-106.82317976739,
-105.824832292928,-104.826484818466,-104.623895335004),.UNSPECIFIED.);
#571=B_SPLINE_CURVE_WITH_KNOTS('',3,(#34461,#34462,#34463,#34464,#34465,
#34466,#34467,#34468,#34469,#34470,#34471,#34472,#34473,#34474,#34475,#34476,
#34477,#34478,#34479,#34480,#34481,#34482,#34483,#34484,#34485),
 .UNSPECIFIED.,.F.,.F.,(4,3,3,3,3,3,3,3,4),(101.648265323242,101.878182580117,
102.876988291687,103.875794003257,104.874599714826,105.873405426396,106.872211137966,
107.871016849536,107.931450630421),.UNSPECIFIED.);
#572=B_SPLINE_CURVE_WITH_KNOTS('',3,(#34490,#34491,#34492,#34493,#34494,
#34495,#34496,#34497,#34498,#34499,#34500,#34501,#34502,#34503,#34504,#34505,
#34506,#34507,#34508,#34509,#34510,#34511),.UNSPECIFIED.,.F.,.F.,(4,3,3,
3,3,3,3,4),(-117.190265949363,-116.806654512005,-115.808307037544,-114.809959563082,
-113.811612088621,-112.813264614159,-111.814917139698,-110.907080642184),
 .UNSPECIFIED.);
#573=B_SPLINE_CURVE_WITH_KNOTS('',3,(#34512,#34513,#34514,#34515,#34516,
#34517,#34518,#34519,#34520,#34521,#34522,#34523,#34524,#34525,#34526,#34527,
#34528,#34529,#34530,#34531,#34532,#34533),.UNSPECIFIED.,.F.,.F.,(4,3,3,
3,3,3,3,4),(107.931450630421,108.869822561106,109.868628272675,110.867433984245,
111.866239695815,112.865045407385,113.863851118954,114.214635937601),
 .UNSPECIFIED.);
#574=B_SPLINE_CURVE_WITH_KNOTS('',3,(#34538,#34539,#34540,#34541,#34542,
#34543,#34544,#34545,#34546,#34547,#34548,#34549,#34550,#34551,#34552,#34553,
#34554,#34555,#34556,#34557,#34558,#34559),.UNSPECIFIED.,.F.,.F.,(4,3,3,
3,3,3,3,4),(-123.473451256543,-122.796739358775,-121.798391884313,-120.800044409852,
-119.80169693539,-118.803349460929,-117.805001986467,-117.190265949363),
 .UNSPECIFIED.);
#575=B_SPLINE_CURVE_WITH_KNOTS('',3,(#34560,#34561,#34562,#34563,#34564,
#34565,#34566,#34567,#34568,#34569,#34570,#34571,#34572,#34573,#34574,#34575,
#34576,#34577,#34578,#34579,#34580,#34581),.UNSPECIFIED.,.F.,.F.,(4,3,3,
3,3,3,3,4),(114.214635937601,114.862656830524,115.861462542094,116.860268253664,
117.859073965234,118.857879676803,119.856685388373,120.49782124478),
 .UNSPECIFIED.);
#576=B_SPLINE_CURVE_WITH_KNOTS('',3,(#34586,#34587,#34588,#34589,#34590,
#34591,#34592,#34593,#34594,#34595,#34596,#34597,#34598,#34599,#34600,#34601,
#34602,#34603,#34604,#34605,#34606,#34607),.UNSPECIFIED.,.F.,.F.,(4,3,3,
3,3,3,3,4),(-129.756636563722,-128.786824205544,-127.788476731083,-126.790129256621,
-125.79178178216,-124.793434307698,-123.795086833237,-123.473451256543),
 .UNSPECIFIED.);
#577=B_SPLINE_CURVE_WITH_KNOTS('',3,(#34608,#34609,#34610,#34611,#34612,
#34613,#34614,#34615,#34616,#34617,#34618,#34619,#34620,#34621,#34622,#34623,
#34624,#34625,#34626,#34627,#34628,#34629),.UNSPECIFIED.,.F.,.F.,(4,3,3,
3,3,3,3,4),(120.49782124478,120.855491099943,121.854296811513,122.853102523082,
123.851908234652,124.850713946222,125.849519657792,126.78100655196),
 .UNSPECIFIED.);
#578=B_SPLINE_CURVE_WITH_KNOTS('',3,(#34634,#34635,#34636,#34637,#34638,
#34639,#34640,#34641,#34642,#34643,#34644,#34645,#34646,#34647,#34648,#34649,
#34650,#34651,#34652,#34653,#34654,#34655,#34656,#34657,#34658),
 .UNSPECIFIED.,.F.,.F.,(4,3,3,3,3,3,3,3,4),(-136.039821870902,-135.775256526776,
-134.776909052314,-133.778561577852,-132.780214103391,-131.781866628929,
-130.783519154468,-129.785171680006,-129.756636563722),.UNSPECIFIED.);
#579=B_SPLINE_CURVE_WITH_KNOTS('',3,(#34659,#34660,#34661,#34662,#34663,
#34664,#34665,#34666,#34667,#34668,#34669,#34670,#34671,#34672,#34673,#34674,
#34675,#34676,#34677,#34678,#34679,#34680,#34681,#34682,#34683),
 .UNSPECIFIED.,.F.,.F.,(4,3,3,3,3,3,3,3,4),(126.78100655196,126.848325369362,
127.847131080931,128.845936792501,129.844742504071,130.843548215641,131.84235392721,
132.84115963878,133.06419185914),.UNSPECIFIED.);
#580=B_SPLINE_CURVE_WITH_KNOTS('',3,(#34688,#34689,#34690,#34691,#34692,
#34693,#34694,#34695,#34696,#34697,#34698,#34699,#34700,#34701,#34702,#34703,
#34704,#34705,#34706,#34707,#34708,#34709),.UNSPECIFIED.,.F.,.F.,(4,3,3,
3,3,3,3,4),(-142.323007178082,-141.765341373545,-140.766993899083,-139.768646424622,
-138.77029895016,-137.771951475699,-136.773604001237,-136.039821870902),
 .UNSPECIFIED.);
#581=B_SPLINE_CURVE_WITH_KNOTS('',3,(#34710,#34711,#34712,#34713,#34714,
#34715,#34716,#34717,#34718,#34719,#34720,#34721,#34722,#34723,#34724,#34725,
#34726,#34727,#34728,#34729,#34730,#34731),.UNSPECIFIED.,.F.,.F.,(4,3,3,
3,3,3,3,4),(133.06419185914,133.83996535035,134.83877106192,135.83757677349,
136.836382485059,137.835188196629,138.833993908199,139.347377166319),
 .UNSPECIFIED.);
#582=B_SPLINE_CURVE_WITH_KNOTS('',3,(#34736,#34737,#34738,#34739,#34740,
#34741,#34742,#34743,#34744,#34745,#34746,#34747,#34748,#34749,#34750,#34751,
#34752,#34753,#34754,#34755,#34756,#34757),.UNSPECIFIED.,.F.,.F.,(4,3,3,
3,3,3,3,4),(-148.606192485261,-147.755426220315,-146.757078745853,-145.758731271391,
-144.76038379693,-143.762036322468,-142.763688848007,-142.323007178082),
 .UNSPECIFIED.);
#583=B_SPLINE_CURVE_WITH_KNOTS('',3,(#34758,#34759,#34760,#34761,#34762,
#34763,#34764,#34765,#34766,#34767,#34768,#34769,#34770,#34771,#34772,#34773,
#34774,#34775,#34776,#34777,#34778,#34779),.UNSPECIFIED.,.F.,.F.,(4,3,3,
3,3,3,3,4),(139.347377166319,139.832799619769,140.831605331338,141.830411042908,
142.829216754478,143.828022466048,144.826828177618,145.630562473499),
 .UNSPECIFIED.);
#584=B_SPLINE_CURVE_WITH_KNOTS('',3,(#34785,#34786,#34787,#34788,#34789,
#34790,#34791,#34792,#34793,#34794),.UNSPECIFIED.,.F.,.F.,(4,1,1,1,1,1,
1,4),(160.221225333079,160.368806542595,161.367154017056,162.365501491518,
163.363848965979,164.362196440441,165.360543914902,166.358891389364),
 .UNSPECIFIED.);
#585=B_SPLINE_CURVE_WITH_KNOTS('',3,(#34797,#34798,#34799,#34800,#34801,
#34802,#34803,#34804),.UNSPECIFIED.,.F.,.F.,(4,1,1,1,1,4),(160.221225333079,
161.124751422577,162.123557134147,163.122362845716,164.121168557286,165.119974268856),
 .UNSPECIFIED.);
#586=B_SPLINE_CURVE_WITH_KNOTS('',3,(#34809,#34810,#34811,#34812,#34813,
#34814,#34815,#34816,#34817,#34818),.UNSPECIFIED.,.F.,.F.,(4,1,1,1,1,1,
1,4),(153.9380400259,154.378721695825,155.377069170287,156.375416644748,
157.37376411921,158.372111593671,159.370459068133,160.221225333079),
 .UNSPECIFIED.);
#587=B_SPLINE_CURVE_WITH_KNOTS('',3,(#34819,#34820,#34821,#34822,#34823,
#34824,#34825,#34826,#34827,#34828,#34829),.UNSPECIFIED.,.F.,.F.,(4,1,1,
1,1,1,1,1,4),(153.9380400259,154.133111441588,155.131917153158,156.130722864728,
157.129528576298,158.128334287868,159.127139999437,160.125945711007,160.221225333079),
 .UNSPECIFIED.);
#588=B_SPLINE_CURVE_WITH_KNOTS('',3,(#34834,#34835,#34836,#34837,#34838,
#34839,#34840,#34841,#34842,#34843),.UNSPECIFIED.,.F.,.F.,(4,1,1,1,1,1,
1,4),(147.65485471872,148.388636849056,149.386984323517,150.385331797979,
151.38367927244,152.382026746902,153.380374221363,153.9380400259),
 .UNSPECIFIED.);
#589=B_SPLINE_CURVE_WITH_KNOTS('',3,(#34844,#34845,#34846,#34847,#34848,
#34849,#34850,#34851,#34852,#34853),.UNSPECIFIED.,.F.,.F.,(4,1,1,1,1,1,
1,4),(147.65485471872,148.14027717217,149.13908288374,150.137888595309,
151.136694306879,152.135500018449,153.134305730019,153.9380400259),
 .UNSPECIFIED.);
#590=B_SPLINE_CURVE_WITH_KNOTS('',3,(#34858,#34859,#34860,#34861,#34862,
#34863,#34864,#34865,#34866,#34867,#34868),.UNSPECIFIED.,.F.,.F.,(4,1,1,
1,1,1,1,1,4),(141.371669411541,141.400204527824,142.398552002286,143.396899476748,
144.395246951209,145.393594425671,146.391941900132,147.390289374594,147.65485471872),
 .UNSPECIFIED.);
#591=B_SPLINE_CURVE_WITH_KNOTS('',3,(#34869,#34870,#34871,#34872,#34873,
#34874,#34875,#34876,#34877,#34878),.UNSPECIFIED.,.F.,.F.,(4,1,1,1,1,1,
1,4),(141.371669411541,142.147442902751,143.146248614321,144.145054325891,
145.14386003746,146.14266574903,147.1414714606,147.65485471872),
 .UNSPECIFIED.);
#592=B_SPLINE_CURVE_WITH_KNOTS('',3,(#34883,#34884,#34885,#34886,#34887,
#34888,#34889,#34890,#34891,#34892),.UNSPECIFIED.,.F.,.F.,(4,1,1,1,1,1,
1,4),(135.088484104361,135.410119681055,136.408467155516,137.406814629978,
138.40516210444,139.403509578901,140.401857053363,141.371669411541),
 .UNSPECIFIED.);
#593=B_SPLINE_CURVE_WITH_KNOTS('',3,(#34893,#34894,#34895,#34896,#34897,
#34898,#34899,#34900,#34901,#34902,#34903),.UNSPECIFIED.,.F.,.F.,(4,1,1,
1,1,1,1,1,4),(135.088484104361,135.155802921763,136.154608633332,137.153414344902,
138.152220056472,139.151025768042,140.149831479612,141.148637191181,141.371669411541),
 .UNSPECIFIED.);
#594=B_SPLINE_CURVE_WITH_KNOTS('',3,(#34908,#34909,#34910,#34911,#34912,
#34913,#34914,#34915,#34916,#34917),.UNSPECIFIED.,.F.,.F.,(4,1,1,1,1,1,
1,4),(128.805298797182,129.420034834285,130.418382308747,131.416729783209,
132.41507725767,133.413424732132,134.411772206593,135.088484104361),
 .UNSPECIFIED.);
#595=B_SPLINE_CURVE_WITH_KNOTS('',3,(#34918,#34919,#34920,#34921,#34922,
#34923,#34924,#34925,#34926,#34927),.UNSPECIFIED.,.F.,.F.,(4,1,1,1,1,1,
1,4),(128.805298797182,129.162968652344,130.161774363914,131.160580075484,
132.159385787053,133.158191498623,134.156997210193,135.088484104361),
 .UNSPECIFIED.);
#596=B_SPLINE_CURVE_WITH_KNOTS('',3,(#34932,#34933,#34934,#34935,#34936,
#34937,#34938,#34939,#34940,#34941),.UNSPECIFIED.,.F.,.F.,(4,1,1,1,1,1,
1,4),(122.522113490002,123.429949987516,124.428297461977,125.426644936439,
126.424992410901,127.423339885362,128.421687359824,128.805298797182),
 .UNSPECIFIED.);
#597=B_SPLINE_CURVE_WITH_KNOTS('',3,(#34942,#34943,#34944,#34945,#34946,
#34947,#34948,#34949,#34950,#34951),.UNSPECIFIED.,.F.,.F.,(4,1,1,1,1,1,
1,4),(122.522113490002,123.170134382925,124.168940094495,125.167745806065,
126.166551517635,127.165357229204,128.164162940774,128.805298797182),
 .UNSPECIFIED.);
#598=B_SPLINE_CURVE_WITH_KNOTS('',3,(#34956,#34957,#34958,#34959,#34960,
#34961,#34962,#34963,#34964,#34965,#34966),.UNSPECIFIED.,.F.,.F.,(4,1,1,
1,1,1,1,1,4),(116.238928182822,116.441517666285,117.439865140746,118.438212615208,
119.43656008967,120.434907564131,121.433255038593,122.431602513054,122.522113490002),
 .UNSPECIFIED.);
#599=B_SPLINE_CURVE_WITH_KNOTS('',3,(#34967,#34968,#34969,#34970,#34971,
#34972,#34973,#34974,#34975,#34976),.UNSPECIFIED.,.F.,.F.,(4,1,1,1,1,1,
1,4),(116.238928182822,117.177300113507,118.176105825076,119.174911536646,
120.173717248216,121.172522959786,122.171328671356,122.522113490002),
 .UNSPECIFIED.);
#600=B_SPLINE_CURVE_WITH_KNOTS('',3,(#34981,#34982,#34983,#34984,#34985,
#34986,#34987,#34988,#34989,#34990),.UNSPECIFIED.,.F.,.F.,(4,1,1,1,1,1,
1,4),(109.955742875643,110.451432819515,111.449780293977,112.448127768438,
113.4464752429,114.444822717362,115.443170191823,116.238928182822),
 .UNSPECIFIED.);
#601=B_SPLINE_CURVE_WITH_KNOTS('',3,(#34991,#34992,#34993,#34994,#34995,
#34996,#34997,#34998,#34999,#35000,#35001),.UNSPECIFIED.,.F.,.F.,(4,1,1,
1,1,1,1,1,4),(109.955742875643,110.185660132518,111.184465844088,112.183271555658,
113.182077267228,114.180882978797,115.179688690367,116.178494401937,116.238928182822),
 .UNSPECIFIED.);
#602=B_SPLINE_CURVE_WITH_KNOTS('',3,(#35006,#35007,#35008,#35009,#35010,
#35011,#35012,#35013,#35014,#35015),.UNSPECIFIED.,.F.,.F.,(4,1,1,1,1,1,
1,4),(103.672557568463,104.461347972746,105.459695447207,106.458042921669,
107.456390396131,108.454737870592,109.453085345054,109.955742875643),
 .UNSPECIFIED.);
#603=B_SPLINE_CURVE_WITH_KNOTS('',3,(#35016,#35017,#35018,#35019,#35020,
#35021,#35022,#35023,#35024,#35025),.UNSPECIFIED.,.F.,.F.,(4,1,1,1,1,1,
1,4),(103.672557568463,104.1928258631,105.191631574669,106.190437286239,
107.189242997809,108.188048709379,109.186854420948,109.955742875643),
 .UNSPECIFIED.);
#604=B_SPLINE_CURVE_WITH_KNOTS('',3,(#35030,#35031,#35032,#35033,#35034,
#35035,#35036,#35037,#35038,#35039,#35040),.UNSPECIFIED.,.F.,.F.,(4,1,1,
1,1,1,1,1,4),(97.3893722612837,97.4729156515147,98.4712631259763,99.4696106004379,
100.467958074899,101.466305549361,102.464653023823,103.463000498284,103.672557568463),
 .UNSPECIFIED.);
#605=B_SPLINE_CURVE_WITH_KNOTS('',3,(#35041,#35042,#35043,#35044,#35045,
#35046,#35047,#35048,#35049,#35050),.UNSPECIFIED.,.F.,.F.,(4,1,1,1,1,1,
1,4),(97.3893722612837,98.199991593681,99.1987973052507,100.197603016821,
101.19640872839,102.19521443996,103.19402015153,103.672557568463),
 .UNSPECIFIED.);
#606=B_SPLINE_CURVE_WITH_KNOTS('',3,(#35055,#35056,#35057,#35058,#35059,
#35060,#35061,#35062,#35063,#35064),.UNSPECIFIED.,.F.,.F.,(4,1,1,1,1,1,
1,4),(91.1061869541041,91.4828308047452,92.4811782792068,93.4795257536684,
94.4778732281299,95.4762207025915,96.4745681770531,97.3893722612837),
 .UNSPECIFIED.);
#607=B_SPLINE_CURVE_WITH_KNOTS('',3,(#35065,#35066,#35067,#35068,#35069,
#35070,#35071,#35072,#35073,#35074,#35075),.UNSPECIFIED.,.F.,.F.,(4,1,1,
1,1,1,1,1,4),(91.1061869541041,91.2083516126925,92.2071573242623,93.2059630358321,
94.2047687474019,95.2035744589716,96.2023801705414,97.2011858821112,97.3893722612837),
 .UNSPECIFIED.);
#608=B_SPLINE_CURVE_WITH_KNOTS('',3,(#35080,#35081,#35082,#35083,#35084,
#35085,#35086,#35087,#35088,#35089),.UNSPECIFIED.,.F.,.F.,(4,1,1,1,1,1,
1,4),(84.8230016469245,85.4927459579757,86.4910934324373,87.4894409068988,
88.4877883813604,89.486135855822,90.4844833302836,91.1061869541041),
 .UNSPECIFIED.);
#609=B_SPLINE_CURVE_WITH_KNOTS('',3,(#35090,#35091,#35092,#35093,#35094,
#35095,#35096,#35097,#35098,#35099),.UNSPECIFIED.,.F.,.F.,(4,1,1,1,1,1,
1,4),(84.8230016469245,85.2155173432739,86.2143230548436,87.2131287664134,
88.2119344779832,89.210740189553,90.2095459011228,91.1061869541041),
 .UNSPECIFIED.);
#610=B_SPLINE_CURVE_WITH_KNOTS('',3,(#35104,#35105,#35106,#35107,#35108,
#35109,#35110,#35111,#35112,#35113),.UNSPECIFIED.,.F.,.F.,(4,1,1,1,1,1,
1,4),(78.5398163397449,79.5026611112062,80.5010085856677,81.4993560601293,
82.4977035345909,83.4960510090525,84.4943984835141,84.8230016469245),
 .UNSPECIFIED.);
#611=B_SPLINE_CURVE_WITH_KNOTS('',3,(#35114,#35115,#35116,#35117,#35118,
#35119,#35120,#35121,#35122,#35123),.UNSPECIFIED.,.F.,.F.,(4,1,1,1,1,1,
1,4),(78.5398163397449,79.2226830738552,80.221488785425,81.2202944969948,
82.2191002085646,83.2179059201343,84.2167116317041,84.8230016469245),
 .UNSPECIFIED.);
#612=B_SPLINE_CURVE_WITH_KNOTS('',3,(#35128,#35129,#35130,#35131,#35132,
#35133,#35134,#35135,#35136,#35137,#35138),.UNSPECIFIED.,.F.,.F.,(4,1,1,
1,1,1,1,1,4),(72.2566310325653,72.5142287899751,73.5125762644366,74.5109237388982,
75.5092712133598,76.5076186878214,77.505966162283,78.5043136367446,78.5398163397449),
 .UNSPECIFIED.);
#613=B_SPLINE_CURVE_WITH_KNOTS('',3,(#35139,#35140,#35141,#35142,#35143,
#35144,#35145,#35146,#35147,#35148),.UNSPECIFIED.,.F.,.F.,(4,1,1,1,1,1,
1,4),(72.2566310325653,73.2298488044366,74.2286545160063,75.2274602275761,
76.2262659391459,77.2250716507157,78.2238773622854,78.5398163397449),
 .UNSPECIFIED.);
#614=B_SPLINE_CURVE_WITH_KNOTS('',3,(#35153,#35154,#35155,#35156,#35157,
#35158,#35159,#35160,#35161,#35162),.UNSPECIFIED.,.F.,.F.,(4,1,1,1,1,1,
1,4),(65.9734457253857,66.5241439432056,67.5224914176671,68.5208388921287,
69.5191863665903,70.5175338410519,71.5158813155135,72.2566310325653),
 .UNSPECIFIED.);
#615=B_SPLINE_CURVE_WITH_KNOTS('',3,(#35163,#35164,#35165,#35166,#35167,
#35168,#35169,#35170,#35171,#35172,#35173),.UNSPECIFIED.,.F.,.F.,(4,1,1,
1,1,1,1,1,4),(65.9734457253857,66.2382088234481,67.2370145350179,68.2358202465877,
69.2346259581575,70.2334316697272,71.232237381297,72.2310430928668,72.2566310325653),
 .UNSPECIFIED.);
#616=B_SPLINE_CURVE_WITH_KNOTS('',3,(#35178,#35179,#35180,#35181,#35182,
#35183,#35184,#35185,#35186,#35187),.UNSPECIFIED.,.F.,.F.,(4,1,1,1,1,1,
1,4),(59.6902604182061,60.534059096436,61.5324065708976,62.5307540453592,
63.5291015198208,64.5274489942824,65.525796468744,65.9734457253857),
 .UNSPECIFIED.);
#617=B_SPLINE_CURVE_WITH_KNOTS('',3,(#35188,#35189,#35190,#35191,#35192,
#35193,#35194,#35195,#35196,#35197),.UNSPECIFIED.,.F.,.F.,(4,1,1,1,1,1,
1,4),(59.6902604182061,60.2453745540295,61.2441802655993,62.242985977169,
63.2417916887388,64.2405974003086,65.2394031118784,65.9734457253857),
 .UNSPECIFIED.);
#618=B_SPLINE_CURVE_WITH_KNOTS('',3,(#35202,#35203,#35204,#35205,#35206,
#35207,#35208,#35209,#35210,#35211,#35212),.UNSPECIFIED.,.F.,.F.,(4,1,1,
1,1,1,1,1,4),(53.4070751110265,53.545626775205,54.5439742496665,55.5423217241281,
56.5406691985897,57.5390166730513,58.5373641475129,59.5357116219745,59.6902604182061),
 .UNSPECIFIED.);
#619=B_SPLINE_CURVE_WITH_KNOTS('',3,(#35213,#35214,#35215,#35216,#35217,
#35218,#35219,#35220,#35221,#35222),.UNSPECIFIED.,.F.,.F.,(4,1,1,1,1,1,
1,4),(53.4070751110265,54.2525402846108,55.2513459961806,56.2501517077504,
57.2489574193202,58.2477631308899,59.2465688424597,59.6902604182061),
 .UNSPECIFIED.);
#620=B_SPLINE_CURVE_WITH_KNOTS('',3,(#35227,#35228,#35229,#35230,#35231,
#35232,#35233,#35234,#35235,#35236),.UNSPECIFIED.,.F.,.F.,(4,1,1,1,1,1,
1,4),(47.1238898038469,47.5555419284354,48.553889402897,49.5522368773586,
50.5505843518202,51.5489318262818,52.5472793007434,53.4070751110265),
 .UNSPECIFIED.);
#621=B_SPLINE_CURVE_WITH_KNOTS('',3,(#35237,#35238,#35239,#35240,#35241,
#35242,#35243,#35244,#35245,#35246,#35247),.UNSPECIFIED.,.F.,.F.,(4,1,1,
1,1,1,1,1,4),(47.1238898038469,47.2609003036224,48.2597060151922,49.258511726762,
50.2573174383317,51.2561231499015,52.2549288614713,53.2537345730411,53.4070751110265),
 .UNSPECIFIED.);
#622=B_SPLINE_CURVE_WITH_KNOTS('',3,(#35252,#35253,#35254,#35255,#35256,
#35257,#35258,#35259,#35260,#35261),.UNSPECIFIED.,.F.,.F.,(4,1,1,1,1,1,
1,4),(40.8407044966673,41.5654570816659,42.5638045561275,43.5621520305891,
44.5604995050507,45.5588469795123,46.5571944539738,47.1238898038469),
 .UNSPECIFIED.);
#623=B_SPLINE_CURVE_WITH_KNOTS('',3,(#35262,#35263,#35264,#35265,#35266,
#35267,#35268,#35269,#35270,#35271),.UNSPECIFIED.,.F.,.F.,(4,1,1,1,1,1,
1,4),(40.8407044966673,41.2680660342037,42.2668717457735,43.2656774573433,
44.2644831689131,45.2632888804829,46.2620945920526,47.1238898038469),
 .UNSPECIFIED.);
#624=B_SPLINE_CURVE_WITH_KNOTS('',3,(#35276,#35277,#35278,#35279,#35280,
#35281,#35282,#35283,#35284,#35285,#35286),.UNSPECIFIED.,.F.,.F.,(4,1,1,
1,1,1,1,1,4),(34.5575191894877,34.5770247604348,35.5753722348964,36.573719709358,
37.5720671838196,38.5704146582812,39.5687621327428,40.5671096072043,40.8407044966673),
 .UNSPECIFIED.);
#625=B_SPLINE_CURVE_WITH_KNOTS('',3,(#35287,#35288,#35289,#35290,#35291,
#35292,#35293,#35294,#35295,#35296),.UNSPECIFIED.,.F.,.F.,(4,1,1,1,1,1,
1,4),(34.5575191894877,35.2752317647851,36.2740374763549,37.2728431879246,
38.2716488994944,39.2704546110642,40.269260322634,40.8407044966673),
 .UNSPECIFIED.);
#626=B_SPLINE_CURVE_WITH_KNOTS('',3,(#35301,#35302,#35303,#35304,#35305,
#35306,#35307,#35308,#35309,#35310),.UNSPECIFIED.,.F.,.F.,(4,1,1,1,1,1,
1,4),(28.2743338823082,28.5869399136653,29.5852873881269,30.5836348625885,
31.5819823370501,32.5803298115117,33.5786772859732,34.5575191894877),
 .UNSPECIFIED.);
#627=B_SPLINE_CURVE_WITH_KNOTS('',3,(#35311,#35312,#35313,#35314,#35315,
#35316,#35317,#35318,#35319,#35320,#35321),.UNSPECIFIED.,.F.,.F.,(4,1,1,
1,1,1,1,1,4),(28.2743338823082,28.2835917837967,29.2823974953664,30.2812032069362,
31.280008918506,32.2788146300758,33.2776203416455,34.2764260532153,34.5575191894877),
 .UNSPECIFIED.);
#628=B_SPLINE_CURVE_WITH_KNOTS('',3,(#35326,#35327,#35328,#35329,#35330,
#35331,#35332,#35333,#35334,#35335),.UNSPECIFIED.,.F.,.F.,(4,1,1,1,1,1,
1,4),(21.9911485751286,22.5968550668958,23.5952025413574,24.593550015819,
25.5918974902806,26.5902449647422,27.5885924392037,28.2743338823082),
 .UNSPECIFIED.);
#629=B_SPLINE_CURVE_WITH_KNOTS('',3,(#35336,#35337,#35338,#35339,#35340,
#35341,#35342,#35343,#35344,#35345),.UNSPECIFIED.,.F.,.F.,(4,1,1,1,1,1,
1,4),(21.9911485751286,22.290757514378,23.2895632259478,24.2883689375176,
25.2871746490873,26.2859803606571,27.2847860722269,28.2743338823082),
 .UNSPECIFIED.);
#630=B_SPLINE_CURVE_WITH_KNOTS('',3,(#35350,#35351,#35352,#35353,#35354,
#35355,#35356,#35357,#35358,#35359),.UNSPECIFIED.,.F.,.F.,(4,1,1,1,1,1,
1,4),(15.707963267949,16.6067702201263,17.6051176945879,18.6034651690495,
19.6018126435111,20.6001601179726,21.5985075924342,21.9911485751286),
 .UNSPECIFIED.);
#631=B_SPLINE_CURVE_WITH_KNOTS('',3,(#35360,#35361,#35362,#35363,#35364,
#35365,#35366,#35367,#35368,#35369),.UNSPECIFIED.,.F.,.F.,(4,1,1,1,1,1,
1,4),(15.707963267949,16.2979232449593,17.2967289565291,18.2955346680989,
19.2943403796687,20.2931460912385,21.2919518028082,21.9911485751286),
 .UNSPECIFIED.);
#632=B_SPLINE_CURVE_WITH_KNOTS('',3,(#35372,#35373,#35374,#35375,#35376,
#35377,#35378,#35379,#35380,#35381,#35382,#35383,#35384,#35385,#35386,#35387,
#35388,#35389,#35390,#35391,#35392,#35393,#35394,#35395,#35396,#35397,#35398,
#35399,#35400,#35401,#35402,#35403,#35404,#35405,#35406,#35407,#35408,#35409,
#35410,#35411,#35412,#35413,#35414,#35415,#35416,#35417,#35418,#35419,#35420,
#35421,#35422,#35423,#35424,#35425,#35426,#35427,#35428,#35429,#35430,#35431,
#35432,#35433,#35434,#35435,#35436,#35437,#35438,#35439,#35440,#35441,#35442,
#35443,#35444,#35445,#35446,#35447,#35448,#35449,#35450,#35451,#35452,#35453,
#35454,#35455,#35456,#35457,#35458,#35459,#35460,#35461,#35462,#35463,#35464,
#35465,#35466,#35467,#35468,#35469,#35470,#35471,#35472,#35473,#35474,#35475,
#35476,#35477,#35478,#35479,#35480,#35481,#35482,#35483,#35484,#35485,#35486,
#35487,#35488,#35489,#35490,#35491,#35492,#35493,#35494,#35495,#35496,#35497,
#35498,#35499,#35500,#35501,#35502,#35503,#35504,#35505,#35506,#35507,#35508,
#35509,#35510,#35511,#35512,#35513,#35514,#35515,#35516,#35517,#35518,#35519,
#35520,#35521,#35522,#35523,#35524,#35525,#35526,#35527,#35528,#35529,#35530,
#35531,#35532,#35533,#35534,#35535,#35536,#35537,#35538,#35539,#35540,#35541,
#35542,#35543,#35544,#35545,#35546,#35547,#35548,#35549,#35550,#35551,#35552,
#35553,#35554,#35555,#35556,#35557,#35558,#35559,#35560,#35561,#35562,#35563,
#35564,#35565,#35566,#35567,#35568,#35569,#35570,#35571,#35572,#35573,#35574,
#35575,#35576,#35577,#35578,#35579,#35580,#35581,#35582,#35583,#35584,#35585,
#35586,#35587,#35588,#35589,#35590,#35591,#35592,#35593,#35594,#35595,#35596,
#35597,#35598,#35599,#35600,#35601,#35602,#35603),.UNSPECIFIED.,.F.,.F.,
(4,3,3,3,3,3,3,3,3,3,3,3,3,3,3,3,3,3,3,3,3,3,3,3,3,3,3,3,3,3,3,3,3,3,3,
3,3,3,3,3,3,3,3,3,3,3,3,3,3,3,3,3,3,3,3,3,3,3,3,3,3,3,3,3,3,3,3,3,3,3,3,
3,3,3,3,3,3,4),(-2.07787844821581,-2.04563640817454,-2.01260600406739,-1.99390262471517,
-1.97880815407869,-1.97343611688677,-1.93978265453417,-1.90587423526444,
-1.88438455677208,-1.87589993511254,-1.87071648916707,-1.83652656870669,
-1.80253536734925,-1.7682460873374,-1.75110144733148,-1.74333138277347,
-1.73705920337893,-1.73395680732556,-1.70122489773177,-1.66760788468754,
-1.63163034935991,-1.61589017765406,-1.60492981834386,-1.60020318232811,
-1.56577415958123,-1.53098947454713,-1.49635100238812,-1.4672101523077,
-1.46216466120046,-1.42716054566692,-1.39267814268788,-1.37978760206645,
-1.34531390132733,-1.33245646351828,-1.32592267957129,-1.32082668753048,
-1.28679878189102,-1.2516716099619,-1.21635641577775,-1.19129075085948,
-1.18499879133774,-1.18014246087519,-1.1446795062145,-1.10922024591651,
-1.07424600071327,-1.04503854857244,-1.03811338002803,-1.0158310964316,
-0.981392848951218,-0.946133107350497,-0.910369520876374,-0.899628872347486,
-0.89368994999567,-0.857962841308724,-0.82181130706931,-0.785718553763474,
-0.767732714465289,-0.754402261382112,-0.748013249342093,-0.711600160631613,
-0.675777877337977,-0.641831839377992,-0.620163722971144,-0.609175591942721,
-0.603763283335243,-0.56872451739821,-0.532416642828612,-0.495724942594248,
-0.470652071878519,-0.458093605572563,-0.451831603827856,-0.415093157349795,
-0.378123471546787,-0.341518871530435,-0.318330424199427,-0.308274893383926,
-0.301672805800084,-0.295141976868419),.UNSPECIFIED.);
#633=B_SPLINE_CURVE_WITH_KNOTS('',3,(#35605,#35606,#35607,#35608,#35609,
#35610,#35611,#35612,#35613,#35614,#35615,#35616,#35617,#35618,#35619,#35620,
#35621,#35622,#35623,#35624,#35625,#35626,#35627,#35628,#35629,#35630,#35631,
#35632,#35633,#35634,#35635,#35636,#35637,#35638,#35639,#35640,#35641,#35642,
#35643,#35644,#35645,#35646,#35647,#35648,#35649,#35650,#35651,#35652,#35653,
#35654,#35655,#35656,#35657,#35658,#35659,#35660,#35661,#35662,#35663,#35664,
#35665,#35666,#35667,#35668,#35669,#35670,#35671),.UNSPECIFIED.,.F.,.F.,
(4,3,3,3,3,3,3,3,3,3,3,3,3,3,3,3,3,3,3,3,3,3,4),(-0.560387248253829,-0.523489675423405,
-0.486909280826814,-0.451409765500931,-0.428581929912694,-0.422644096024468,
-0.417538776764712,-0.382486843658728,-0.360098423147984,-0.324342694600126,
-0.288456460870319,-0.277039646852259,-0.272658549855339,-0.23782854730266,
-0.202954723102529,-0.168490668078001,-0.147429334568251,-0.135539740506508,
-0.130645012249701,-0.0971180289394068,-0.0640503905793665,-0.0319885771286076,
0.),.UNSPECIFIED.);
#634=B_SPLINE_CURVE_WITH_KNOTS('',3,(#35674,#35675,#35676,#35677,#35678,
#35679,#35680,#35681,#35682,#35683,#35684,#35685,#35686,#35687,#35688,#35689,
#35690,#35691,#35692,#35693,#35694,#35695,#35696,#35697,#35698,#35699,#35700,
#35701,#35702,#35703,#35704),.UNSPECIFIED.,.F.,.F.,(4,3,3,3,3,3,3,3,3,3,
4),(-0.295141976868419,-0.258118008913044,-0.221832521729933,-0.184905796964689,
-0.161792572344103,-0.155196944416255,-0.149950158553442,-0.112462618915081,
-0.0749997768837546,-0.0374998884418773,0.),.UNSPECIFIED.);
#635=B_SPLINE_CURVE_WITH_KNOTS('',3,(#36341,#36342,#36343,#36344,#36345,
#36346,#36347,#36348),.UNSPECIFIED.,.F.,.F.,(4,1,1,1,1,4),(11.6150328478184,
12.61338032228,13.6117277967416,14.6100752712031,15.6084227456647,15.707963267949),
 .UNSPECIFIED.);
#636=B_SPLINE_CURVE_WITH_KNOTS('',3,(#36349,#36350,#36351,#36352,#36353,
#36354,#36355,#36356,#36357,#36358,#36359,#36360,#36361,#36362,#36363,#36364,
#36365,#36366,#36367,#36368,#36369,#36370,#36371,#36372,#36373,#36374,#36375,
#36376,#36377,#36378,#36379,#36380,#36381,#36382,#36383,#36384,#36385,#36386,
#36387,#36388,#36389,#36390,#36391,#36392,#36393,#36394,#36395,#36396,#36397,
#36398,#36399,#36400,#36401,#36402,#36403,#36404,#36405,#36406,#36407,#36408,
#36409,#36410,#36411,#36412,#36413,#36414,#36415,#36416,#36417,#36418,#36419,
#36420,#36421,#36422,#36423,#36424,#36425,#36426,#36427,#36428,#36429,#36430,
#36431,#36432,#36433,#36434,#36435,#36436,#36437,#36438,#36439,#36440,#36441,
#36442,#36443,#36444,#36445),.UNSPECIFIED.,.F.,.F.,(4,3,3,3,3,3,3,3,3,3,
3,3,3,3,3,3,3,3,3,3,3,3,3,3,3,3,3,3,3,3,3,3,4),(-0.75940314415766,-0.731099230044352,
-0.694405090916541,-0.673021753795954,-0.659792230351525,-0.653579099280099,
-0.615915673993481,-0.58296017686769,-0.568542146875157,-0.56016187063185,
-0.554528541316208,-0.518574457756444,-0.482794928028838,-0.44802285832865,
-0.424085067993276,-0.41225754927003,-0.407433722504049,-0.373002009397425,
-0.352271696987154,-0.317344582417244,-0.282174956583422,-0.274866834214802,
-0.269904808501567,-0.23562822660491,-0.201185303792214,-0.167047167238569,
-0.146166271333748,-0.135071182701311,-0.130169248221992,-0.0967451917617864,
-0.0637506042838665,-0.03178494031496,0.),.UNSPECIFIED.);
#637=B_SPLINE_CURVE_WITH_KNOTS('',3,(#36446,#36447,#36448,#36449,#36450,
#36451,#36452,#36453,#36454,#36455,#36456,#36457,#36458,#36459,#36460,#36461,
#36462,#36463,#36464),.UNSPECIFIED.,.F.,.F.,(4,3,3,3,3,3,4),(-153.229510295036,
-152.747163592623,-151.748816118161,-150.750468643699,-149.752121169238,
-148.753773694776,-148.606192485261),.UNSPECIFIED.);
#638=B_SPLINE_CURVE_WITH_KNOTS('',3,(#36467,#36468,#36469,#36470,#36471,
#36472,#36473,#36474,#36475),.UNSPECIFIED.,.F.,.F.,(4,1,1,1,1,1,4),(10.3761157273103,
11.3038946871105,12.3027003986802,13.30150611025,14.3003118218198,15.2991175333896,
15.707963267949),.UNSPECIFIED.);
#639=B_SPLINE_CURVE_WITH_KNOTS('',3,(#37117,#37118,#37119,#37120,#37121,
#37122,#37123,#37124,#37125,#37126,#37127,#37128,#37129,#37130,#37131,#37132,
#37133,#37134,#37135,#37136,#37137,#37138),.UNSPECIFIED.,.F.,.F.,(4,3,3,
3,3,3,3,4),(145.630562473499,145.825633889187,146.824439600757,147.823245312327,
148.822051023897,149.820856735466,150.819662447036,151.160872120127),
 .UNSPECIFIED.);
#640=B_SPLINE_CURVE_WITH_KNOTS('',3,(#37139,#37140,#37141,#37142,#37143,
#37144,#37145,#37146,#37147,#37148,#37149,#37150,#37151,#37152,#37153,#37154,
#37155,#37156,#37157,#37158,#37159,#37160,#37161,#37162,#37163,#37164,#37165,
#37166,#37167,#37168,#37169,#37170,#37171,#37172,#37173,#37174,#37175,#37176,
#37177,#37178,#37179,#37180,#37181,#37182,#37183,#37184,#37185,#37186,#37187,
#37188,#37189,#37190,#37191,#37192,#37193,#37194,#37195,#37196,#37197,#37198,
#37199,#37200,#37201,#37202,#37203,#37204,#37205,#37206,#37207,#37208,#37209,
#37210,#37211,#37212,#37213,#37214,#37215,#37216,#37217,#37218,#37219,#37220,
#37221,#37222,#37223,#37224,#37225,#37226,#37227,#37228,#37229,#37230,#37231,
#37232,#37233,#37234,#37235),.UNSPECIFIED.,.F.,.F.,(4,3,3,3,3,3,3,3,3,3,
3,3,3,3,3,3,3,3,3,3,3,3,3,3,3,3,3,3,3,3,3,3,4),(-0.761903739928579,-0.737714840814909,
-0.705408016786385,-0.685226614670373,-0.676627161339419,-0.668738660960247,
-0.635678094311993,-0.604031530389268,-0.590186158673076,-0.583843379993958,
-0.578312161070379,-0.543995147795815,-0.509206617715678,-0.474634013675463,
-0.451601905989146,-0.445054542245308,-0.439067220218037,-0.403526955466083,
-0.382505582930195,-0.348068670802762,-0.312989133154698,-0.301425205487243,
-0.296110141258073,-0.261171717718659,-0.225140081955213,-0.188826370911274,
-0.165223074547365,-0.15245028863213,-0.147771515823046,-0.110734161208511,
-0.0736990584503352,-0.0368495292251676,0.),.UNSPECIFIED.);
#2215=SHAPE_REPRESENTATION_RELATIONSHIP('SRR','None',#97608,#2234);
#2234=ADVANCED_BREP_SHAPE_REPRESENTATION('',(#2272),#97458);
#2253=STYLED_ITEM('',(#97720),#2272);
#2272=MANIFOLD_SOLID_BREP('Body1',#21814);
#2312=FACE_BOUND('',#3888,.T.);
#2313=FACE_BOUND('',#3891,.T.);
#2405=PLANE('',#22234);
#2406=PLANE('',#22235);
#2407=PLANE('',#22236);
#2408=PLANE('',#22237);
#2409=PLANE('',#22238);
#2410=PLANE('',#22239);
#2411=PLANE('',#22240);
#2412=PLANE('',#22241);
#2413=PLANE('',#22245);
#2414=PLANE('',#22246);
#2649=FACE_OUTER_BOUND('',#3827,.T.);
#2650=FACE_OUTER_BOUND('',#3828,.T.);
#2651=FACE_OUTER_BOUND('',#3829,.T.);
#2652=FACE_OUTER_BOUND('',#3830,.T.);
#2653=FACE_OUTER_BOUND('',#3831,.T.);
#2654=FACE_OUTER_BOUND('',#3832,.T.);
#2655=FACE_OUTER_BOUND('',#3833,.T.);
#2656=FACE_OUTER_BOUND('',#3834,.T.);
#2657=FACE_OUTER_BOUND('',#3835,.T.);
#2658=FACE_OUTER_BOUND('',#3836,.T.);
#2659=FACE_OUTER_BOUND('',#3837,.T.);
#2660=FACE_OUTER_BOUND('',#3838,.T.);
#2661=FACE_OUTER_BOUND('',#3839,.T.);
#2662=FACE_OUTER_BOUND('',#3840,.T.);
#2663=FACE_OUTER_BOUND('',#3841,.T.);
#2664=FACE_OUTER_BOUND('',#3842,.T.);
#2665=FACE_OUTER_BOUND('',#3843,.T.);
#2666=FACE_OUTER_BOUND('',#3844,.T.);
#2667=FACE_OUTER_BOUND('',#3845,.T.);
#2668=FACE_OUTER_BOUND('',#3846,.T.);
#2669=FACE_OUTER_BOUND('',#3847,.T.);
#2670=FACE_OUTER_BOUND('',#3848,.T.);
#2671=FACE_OUTER_BOUND('',#3849,.T.);
#2672=FACE_OUTER_BOUND('',#3850,.T.);
#2673=FACE_OUTER_BOUND('',#3851,.T.);
#2674=FACE_OUTER_BOUND('',#3852,.T.);
#2675=FACE_OUTER_BOUND('',#3853,.T.);
#2676=FACE_OUTER_BOUND('',#3854,.T.);
#2677=FACE_OUTER_BOUND('',#3855,.T.);
#2678=FACE_OUTER_BOUND('',#3856,.T.);
#2679=FACE_OUTER_BOUND('',#3857,.T.);
#2680=FACE_OUTER_BOUND('',#3858,.T.);
#2681=FACE_OUTER_BOUND('',#3859,.T.);
#2682=FACE_OUTER_BOUND('',#3860,.T.);
#2683=FACE_OUTER_BOUND('',#3861,.T.);
#2684=FACE_OUTER_BOUND('',#3862,.T.);
#2685=FACE_OUTER_BOUND('',#3863,.T.);
#2686=FACE_OUTER_BOUND('',#3864,.T.);
#2687=FACE_OUTER_BOUND('',#3865,.T.);
#2688=FACE_OUTER_BOUND('',#3866,.T.);
#2689=FACE_OUTER_BOUND('',#3867,.T.);
#2690=FACE_OUTER_BOUND('',#3868,.T.);
#2691=FACE_OUTER_BOUND('',#3869,.T.);
#2692=FACE_OUTER_BOUND('',#3870,.T.);
#2693=FACE_OUTER_BOUND('',#3871,.T.);
#2694=FACE_OUTER_BOUND('',#3872,.T.);
#2695=FACE_OUTER_BOUND('',#3873,.T.);
#2696=FACE_OUTER_BOUND('',#3874,.T.);
#2697=FACE_OUTER_BOUND('',#3875,.T.);
#2698=FACE_OUTER_BOUND('',#3876,.T.);
#2699=FACE_OUTER_BOUND('',#3877,.T.);
#2700=FACE_OUTER_BOUND('',#3878,.T.);
#2701=FACE_OUTER_BOUND('',#3879,.T.);
#2702=FACE_OUTER_BOUND('',#3880,.T.);
#2703=FACE_OUTER_BOUND('',#3881,.T.);
#2704=FACE_OUTER_BOUND('',#3882,.T.);
#2705=FACE_OUTER_BOUND('',#3883,.T.);
#2706=FACE_OUTER_BOUND('',#3884,.T.);
#2707=FACE_OUTER_BOUND('',#3885,.T.);
#2708=FACE_OUTER_BOUND('',#3886,.T.);
#2709=FACE_OUTER_BOUND('',#3887,.T.);
#2710=FACE_OUTER_BOUND('',#3889,.T.);
#2711=FACE_OUTER_BOUND('',#3890,.T.);
#2712=FACE_OUTER_BOUND('',#3892,.T.);
#3827=EDGE_LOOP('',(#13748,#13749,#13750,#13751));
#3828=EDGE_LOOP('',(#13752,#13753,#13754,#13755));
#3829=EDGE_LOOP('',(#13756,#13757,#13758,#13759));
#3830=EDGE_LOOP('',(#13760,#13761,#13762,#13763));
#3831=EDGE_LOOP('',(#13764,#13765,#13766,#13767));
#3832=EDGE_LOOP('',(#13768,#13769,#13770,#13771));
#3833=EDGE_LOOP('',(#13772,#13773,#13774,#13775));
#3834=EDGE_LOOP('',(#13776,#13777,#13778,#13779));
#3835=EDGE_LOOP('',(#13780,#13781,#13782,#13783));
#3836=EDGE_LOOP('',(#13784,#13785,#13786,#13787));
#3837=EDGE_LOOP('',(#13788,#13789,#13790,#13791));
#3838=EDGE_LOOP('',(#13792,#13793,#13794,#13795));
#3839=EDGE_LOOP('',(#13796,#13797,#13798,#13799));
#3840=EDGE_LOOP('',(#13800,#13801,#13802,#13803));
#3841=EDGE_LOOP('',(#13804,#13805,#13806,#13807));
#3842=EDGE_LOOP('',(#13808,#13809,#13810,#13811));
#3843=EDGE_LOOP('',(#13812,#13813,#13814,#13815));
#3844=EDGE_LOOP('',(#13816,#13817,#13818,#13819));
#3845=EDGE_LOOP('',(#13820,#13821,#13822,#13823));
#3846=EDGE_LOOP('',(#13824,#13825,#13826,#13827));
#3847=EDGE_LOOP('',(#13828,#13829,#13830,#13831));
#3848=EDGE_LOOP('',(#13832,#13833,#13834,#13835));
#3849=EDGE_LOOP('',(#13836,#13837,#13838,#13839));
#3850=EDGE_LOOP('',(#13840,#13841,#13842,#13843));
#3851=EDGE_LOOP('',(#13844,#13845,#13846,#13847));
#3852=EDGE_LOOP('',(#13848,#13849,#13850,#13851));
#3853=EDGE_LOOP('',(#13852,#13853,#13854,#13855));
#3854=EDGE_LOOP('',(#13856,#13857,#13858,#13859));
#3855=EDGE_LOOP('',(#13860,#13861,#13862,#13863));
#3856=EDGE_LOOP('',(#13864,#13865,#13866,#13867));
#3857=EDGE_LOOP('',(#13868,#13869,#13870,#13871));
#3858=EDGE_LOOP('',(#13872,#13873,#13874,#13875));
#3859=EDGE_LOOP('',(#13876,#13877,#13878,#13879));
#3860=EDGE_LOOP('',(#13880,#13881,#13882,#13883));
#3861=EDGE_LOOP('',(#13884,#13885,#13886,#13887));
#3862=EDGE_LOOP('',(#13888,#13889,#13890,#13891));
#3863=EDGE_LOOP('',(#13892,#13893,#13894,#13895));
#3864=EDGE_LOOP('',(#13896,#13897,#13898,#13899));
#3865=EDGE_LOOP('',(#13900,#13901,#13902,#13903));
#3866=EDGE_LOOP('',(#13904,#13905,#13906,#13907));
#3867=EDGE_LOOP('',(#13908,#13909,#13910,#13911));
#3868=EDGE_LOOP('',(#13912,#13913,#13914,#13915));
#3869=EDGE_LOOP('',(#13916,#13917,#13918,#13919));
#3870=EDGE_LOOP('',(#13920,#13921,#13922,#13923));
#3871=EDGE_LOOP('',(#13924,#13925,#13926,#13927));
#3872=EDGE_LOOP('',(#13928,#13929,#13930,#13931));
#3873=EDGE_LOOP('',(#13932,#13933,#13934,#13935));
#3874=EDGE_LOOP('',(#13936,#13937,#13938,#13939));
#3875=EDGE_LOOP('',(#13940,#13941,#13942,#13943,#13944,#13945,#13946,#13947));
#3876=EDGE_LOOP('',(#13948,#13949,#13950,#13951,#13952,#13953,#13954,#13955,
#13956,#13957,#13958,#13959,#13960,#13961,#13962,#13963,#13964,#13965,#13966,
#13967,#13968,#13969,#13970,#13971,#13972,#13973,#13974,#13975,#13976,#13977,
#13978,#13979,#13980,#13981,#13982,#13983,#13984,#13985,#13986,#13987,#13988,
#13989,#13990,#13991,#13992,#13993,#13994,#13995,#13996,#13997,#13998,#13999));
#3877=EDGE_LOOP('',(#14000,#14001,#14002,#14003));
#3878=EDGE_LOOP('',(#14004,#14005,#14006,#14007,#14008,#14009,#14010,#14011,
#14012,#14013,#14014,#14015,#14016,#14017,#14018,#14019,#14020,#14021,#14022,
#14023,#14024,#14025,#14026,#14027,#14028,#14029,#14030,#14031,#14032,#14033,
#14034,#14035,#14036,#14037,#14038,#14039,#14040,#14041,#14042,#14043,#14044,
#14045,#14046,#14047,#14048,#14049,#14050,#14051,#14052,#14053,#14054,#14055,
#14056));
#3879=EDGE_LOOP('',(#14057,#14058,#14059,#14060));
#3880=EDGE_LOOP('',(#14061,#14062,#14063,#14064));
#3881=EDGE_LOOP('',(#14065,#14066,#14067,#14068));
#3882=EDGE_LOOP('',(#14069,#14070,#14071,#14072));
#3883=EDGE_LOOP('',(#14073,#14074,#14075,#14076));
#3884=EDGE_LOOP('',(#14077,#14078,#14079,#14080));
#3885=EDGE_LOOP('',(#14081,#14082,#14083,#14084));
#3886=EDGE_LOOP('',(#14085,#14086,#14087,#14088,#14089,#14090));
#3887=EDGE_LOOP('',(#14091));
#3888=EDGE_LOOP('',(#14092,#14093,#14094,#14095));
#3889=EDGE_LOOP('',(#14096,#14097,#14098,#14099));
#3890=EDGE_LOOP('',(#14100));
#3891=EDGE_LOOP('',(#14101,#14102,#14103,#14104,#14105,#14106));
#3892=EDGE_LOOP('',(#14107));
#5066=LINE('',#33619,#6280);
#5067=LINE('',#33643,#6281);
#5068=LINE('',#33691,#6282);
#5069=LINE('',#33739,#6283);
#5070=LINE('',#33787,#6284);
#5071=LINE('',#33841,#6285);
#5072=LINE('',#33889,#6286);
#5073=LINE('',#33937,#6287);
#5074=LINE('',#33991,#6288);
#5075=LINE('',#34039,#6289);
#5076=LINE('',#34087,#6290);
#5077=LINE('',#34141,#6291);
#5078=LINE('',#34189,#6292);
#5079=LINE('',#34237,#6293);
#5080=LINE('',#34285,#6294);
#5081=LINE('',#34339,#6295);
#5082=LINE('',#34387,#6296);
#5083=LINE('',#34435,#6297);
#5084=LINE('',#34489,#6298);
#5085=LINE('',#34537,#6299);
#5086=LINE('',#34585,#6300);
#5087=LINE('',#34633,#6301);
#5088=LINE('',#34687,#6302);
#5089=LINE('',#34735,#6303);
#5090=LINE('',#34783,#6304);
#5091=LINE('',#34808,#6305);
#5092=LINE('',#34833,#6306);
#5093=LINE('',#34857,#6307);
#5094=LINE('',#34882,#6308);
#5095=LINE('',#34907,#6309);
#5096=LINE('',#34931,#6310);
#5097=LINE('',#34955,#6311);
#5098=LINE('',#34980,#6312);
#5099=LINE('',#35005,#6313);
#5100=LINE('',#35029,#6314);
#5101=LINE('',#35054,#6315);
#5102=LINE('',#35079,#6316);
#5103=LINE('',#35103,#6317);
#5104=LINE('',#35127,#6318);
#5105=LINE('',#35152,#6319);
#5106=LINE('',#35177,#6320);
#5107=LINE('',#35201,#6321);
#5108=LINE('',#35226,#6322);
#5109=LINE('',#35251,#6323);
#5110=LINE('',#35275,#6324);
#5111=LINE('',#35300,#6325);
#5112=LINE('',#35325,#6326);
#5113=LINE('',#35349,#6327);
#5114=LINE('',#35706,#6328);
#5115=LINE('',#37240,#6329);
#5116=LINE('',#37242,#6330);
#5117=LINE('',#37244,#6331);
#5118=LINE('',#37245,#6332);
#5119=LINE('',#37248,#6333);
#5120=LINE('',#37250,#6334);
#5121=LINE('',#37251,#6335);
#5122=LINE('',#37254,#6336);
#5123=LINE('',#37256,#6337);
#5124=LINE('',#37257,#6338);
#5125=LINE('',#37260,#6339);
#5126=LINE('',#37262,#6340);
#5127=LINE('',#37263,#6341);
#5128=LINE('',#37266,#6342);
#5129=LINE('',#37268,#6343);
#5130=LINE('',#37269,#6344);
#5131=LINE('',#37271,#6345);
#5132=LINE('',#37272,#6346);
#5133=LINE('',#37279,#6347);
#6280=VECTOR('',#23910,4.);
#6281=VECTOR('',#23915,4.);
#6282=VECTOR('',#23918,4.);
#6283=VECTOR('',#23921,4.);
#6284=VECTOR('',#23924,4.);
#6285=VECTOR('',#23927,4.);
#6286=VECTOR('',#23930,4.);
#6287=VECTOR('',#23933,4.);
#6288=VECTOR('',#23936,4.);
#6289=VECTOR('',#23939,4.);
#6290=VECTOR('',#23942,4.);
#6291=VECTOR('',#23945,4.);
#6292=VECTOR('',#23948,4.);
#6293=VECTOR('',#23951,4.);
#6294=VECTOR('',#23954,4.);
#6295=VECTOR('',#23957,4.);
#6296=VECTOR('',#23960,4.);
#6297=VECTOR('',#23963,4.);
#6298=VECTOR('',#23966,4.);
#6299=VECTOR('',#23969,4.);
#6300=VECTOR('',#23972,4.);
#6301=VECTOR('',#23975,4.);
#6302=VECTOR('',#23978,4.);
#6303=VECTOR('',#23981,4.);
#6304=VECTOR('',#23984,3.37175);
#6305=VECTOR('',#23989,3.37175);
#6306=VECTOR('',#23992,3.37175);
#6307=VECTOR('',#23995,3.37175);
#6308=VECTOR('',#23998,3.37175);
#6309=VECTOR('',#24001,3.37175);
#6310=VECTOR('',#24004,3.37175);
#6311=VECTOR('',#24007,3.37175);
#6312=VECTOR('',#24010,3.37175);
#6313=VECTOR('',#24013,3.37175);
#6314=VECTOR('',#24016,3.37175);
#6315=VECTOR('',#24019,3.37175);
#6316=VECTOR('',#24022,3.37175);
#6317=VECTOR('',#24025,3.37175);
#6318=VECTOR('',#24028,3.37175);
#6319=VECTOR('',#24031,3.37175);
#6320=VECTOR('',#24034,3.37175);
#6321=VECTOR('',#24037,3.37175);
#6322=VECTOR('',#24040,3.37175);
#6323=VECTOR('',#24043,3.37175);
#6324=VECTOR('',#24046,3.37175);
#6325=VECTOR('',#24049,3.37175);
#6326=VECTOR('',#24052,3.37175);
#6327=VECTOR('',#24055,3.37175);
#6328=VECTOR('',#24060,3.5);
#6329=VECTOR('',#24071,10.);
#6330=VECTOR('',#24072,10.);
#6331=VECTOR('',#24073,10.);
#6332=VECTOR('',#24074,10.);
#6333=VECTOR('',#24077,10.);
#6334=VECTOR('',#24078,10.);
#6335=VECTOR('',#24079,10.);
#6336=VECTOR('',#24082,10.);
#6337=VECTOR('',#24083,10.);
#6338=VECTOR('',#24084,10.);
#6339=VECTOR('',#24087,10.);
#6340=VECTOR('',#24088,10.);
#6341=VECTOR('',#24089,10.);
#6342=VECTOR('',#24092,10.);
#6343=VECTOR('',#24093,10.);
#6344=VECTOR('',#24094,10.);
#6345=VECTOR('',#24097,10.);
#6346=VECTOR('',#24098,10.);
#6347=VECTOR('',#24107,6.5);
#7392=CIRCLE('',#22179,3.942);
#7393=CIRCLE('',#22204,3.37175);
#7394=CIRCLE('',#22229,3.942);
#7395=CIRCLE('',#22230,3.);
#7396=CIRCLE('',#22232,3.37175);
#7397=CIRCLE('',#22242,6.5);
#7398=CIRCLE('',#22244,6.5);
#7825=VERTEX_POINT('',#33617);
#7826=VERTEX_POINT('',#33618);
#7827=VERTEX_POINT('',#33620);
#7828=VERTEX_POINT('',#33631);
#7829=VERTEX_POINT('',#33641);
#7830=VERTEX_POINT('',#33642);
#7831=VERTEX_POINT('',#33689);
#7832=VERTEX_POINT('',#33690);
#7833=VERTEX_POINT('',#33737);
#7834=VERTEX_POINT('',#33738);
#7835=VERTEX_POINT('',#33785);
#7836=VERTEX_POINT('',#33786);
#7837=VERTEX_POINT('',#33839);
#7838=VERTEX_POINT('',#33840);
#7839=VERTEX_POINT('',#33887);
#7840=VERTEX_POINT('',#33888);
#7841=VERTEX_POINT('',#33935);
#7842=VERTEX_POINT('',#33936);
#7843=VERTEX_POINT('',#33989);
#7844=VERTEX_POINT('',#33990);
#7845=VERTEX_POINT('',#34037);
#7846=VERTEX_POINT('',#34038);
#7847=VERTEX_POINT('',#34085);
#7848=VERTEX_POINT('',#34086);
#7849=VERTEX_POINT('',#34139);
#7850=VERTEX_POINT('',#34140);
#7851=VERTEX_POINT('',#34187);
#7852=VERTEX_POINT('',#34188);
#7853=VERTEX_POINT('',#34235);
#7854=VERTEX_POINT('',#34236);
#7855=VERTEX_POINT('',#34283);
#7856=VERTEX_POINT('',#34284);
#7857=VERTEX_POINT('',#34337);
#7858=VERTEX_POINT('',#34338);
#7859=VERTEX_POINT('',#34385);
#7860=VERTEX_POINT('',#34386);
#7861=VERTEX_POINT('',#34433);
#7862=VERTEX_POINT('',#34434);
#7863=VERTEX_POINT('',#34487);
#7864=VERTEX_POINT('',#34488);
#7865=VERTEX_POINT('',#34535);
#7866=VERTEX_POINT('',#34536);
#7867=VERTEX_POINT('',#34583);
#7868=VERTEX_POINT('',#34584);
#7869=VERTEX_POINT('',#34631);
#7870=VERTEX_POINT('',#34632);
#7871=VERTEX_POINT('',#34685);
#7872=VERTEX_POINT('',#34686);
#7873=VERTEX_POINT('',#34733);
#7874=VERTEX_POINT('',#34734);
#7875=VERTEX_POINT('',#34781);
#7876=VERTEX_POINT('',#34782);
#7877=VERTEX_POINT('',#34784);
#7878=VERTEX_POINT('',#34795);
#7879=VERTEX_POINT('',#34806);
#7880=VERTEX_POINT('',#34807);
#7881=VERTEX_POINT('',#34831);
#7882=VERTEX_POINT('',#34832);
#7883=VERTEX_POINT('',#34855);
#7884=VERTEX_POINT('',#34856);
#7885=VERTEX_POINT('',#34880);
#7886=VERTEX_POINT('',#34881);
#7887=VERTEX_POINT('',#34905);
#7888=VERTEX_POINT('',#34906);
#7889=VERTEX_POINT('',#34929);
#7890=VERTEX_POINT('',#34930);
#7891=VERTEX_POINT('',#34953);
#7892=VERTEX_POINT('',#34954);
#7893=VERTEX_POINT('',#34978);
#7894=VERTEX_POINT('',#34979);
#7895=VERTEX_POINT('',#35003);
#7896=VERTEX_POINT('',#35004);
#7897=VERTEX_POINT('',#35027);
#7898=VERTEX_POINT('',#35028);
#7899=VERTEX_POINT('',#35052);
#7900=VERTEX_POINT('',#35053);
#7901=VERTEX_POINT('',#35077);
#7902=VERTEX_POINT('',#35078);
#7903=VERTEX_POINT('',#35101);
#7904=VERTEX_POINT('',#35102);
#7905=VERTEX_POINT('',#35125);
#7906=VERTEX_POINT('',#35126);
#7907=VERTEX_POINT('',#35150);
#7908=VERTEX_POINT('',#35151);
#7909=VERTEX_POINT('',#35175);
#7910=VERTEX_POINT('',#35176);
#7911=VERTEX_POINT('',#35199);
#7912=VERTEX_POINT('',#35200);
#7913=VERTEX_POINT('',#35224);
#7914=VERTEX_POINT('',#35225);
#7915=VERTEX_POINT('',#35249);
#7916=VERTEX_POINT('',#35250);
#7917=VERTEX_POINT('',#35273);
#7918=VERTEX_POINT('',#35274);
#7919=VERTEX_POINT('',#35298);
#7920=VERTEX_POINT('',#35299);
#7921=VERTEX_POINT('',#35323);
#7922=VERTEX_POINT('',#35324);
#7923=VERTEX_POINT('',#35347);
#7924=VERTEX_POINT('',#35348);
#7925=VERTEX_POINT('',#35371);
#7926=VERTEX_POINT('',#35604);
#7927=VERTEX_POINT('',#35672);
#7928=VERTEX_POINT('',#35705);
#7929=VERTEX_POINT('',#36340);
#7930=VERTEX_POINT('',#36466);
#7931=VERTEX_POINT('',#37238);
#7932=VERTEX_POINT('',#37239);
#7933=VERTEX_POINT('',#37241);
#7934=VERTEX_POINT('',#37243);
#7935=VERTEX_POINT('',#37247);
#7936=VERTEX_POINT('',#37249);
#7937=VERTEX_POINT('',#37253);
#7938=VERTEX_POINT('',#37255);
#7939=VERTEX_POINT('',#37259);
#7940=VERTEX_POINT('',#37261);
#7941=VERTEX_POINT('',#37265);
#7942=VERTEX_POINT('',#37267);
#7943=VERTEX_POINT('',#37275);
#7944=VERTEX_POINT('',#37278);
#10131=EDGE_CURVE('',#7825,#7826,#5066,.T.);
#10132=EDGE_CURVE('',#7825,#7827,#536,.T.);
#10133=EDGE_CURVE('',#7827,#7828,#7392,.F.);
#10134=EDGE_CURVE('',#7828,#7826,#537,.T.);
#10135=EDGE_CURVE('',#7829,#7830,#5067,.T.);
#10136=EDGE_CURVE('',#7829,#7825,#538,.T.);
#10137=EDGE_CURVE('',#7826,#7830,#539,.T.);
#10138=EDGE_CURVE('',#7831,#7832,#5068,.T.);
#10139=EDGE_CURVE('',#7831,#7829,#540,.T.);
#10140=EDGE_CURVE('',#7830,#7832,#541,.T.);
#10141=EDGE_CURVE('',#7833,#7834,#5069,.T.);
#10142=EDGE_CURVE('',#7833,#7831,#542,.T.);
#10143=EDGE_CURVE('',#7832,#7834,#543,.T.);
#10144=EDGE_CURVE('',#7835,#7836,#5070,.T.);
#10145=EDGE_CURVE('',#7835,#7833,#544,.T.);
#10146=EDGE_CURVE('',#7834,#7836,#545,.T.);
#10147=EDGE_CURVE('',#7837,#7838,#5071,.T.);
#10148=EDGE_CURVE('',#7837,#7835,#546,.T.);
#10149=EDGE_CURVE('',#7836,#7838,#547,.T.);
#10150=EDGE_CURVE('',#7839,#7840,#5072,.T.);
#10151=EDGE_CURVE('',#7839,#7837,#548,.T.);
#10152=EDGE_CURVE('',#7838,#7840,#549,.T.);
#10153=EDGE_CURVE('',#7841,#7842,#5073,.T.);
#10154=EDGE_CURVE('',#7841,#7839,#550,.T.);
#10155=EDGE_CURVE('',#7840,#7842,#551,.T.);
#10156=EDGE_CURVE('',#7843,#7844,#5074,.T.);
#10157=EDGE_CURVE('',#7843,#7841,#552,.T.);
#10158=EDGE_CURVE('',#7842,#7844,#553,.T.);
#10159=EDGE_CURVE('',#7845,#7846,#5075,.T.);
#10160=EDGE_CURVE('',#7845,#7843,#554,.T.);
#10161=EDGE_CURVE('',#7844,#7846,#555,.T.);
#10162=EDGE_CURVE('',#7847,#7848,#5076,.T.);
#10163=EDGE_CURVE('',#7847,#7845,#556,.T.);
#10164=EDGE_CURVE('',#7846,#7848,#557,.T.);
#10165=EDGE_CURVE('',#7849,#7850,#5077,.T.);
#10166=EDGE_CURVE('',#7849,#7847,#558,.T.);
#10167=EDGE_CURVE('',#7848,#7850,#559,.T.);
#10168=EDGE_CURVE('',#7851,#7852,#5078,.T.);
#10169=EDGE_CURVE('',#7851,#7849,#560,.T.);
#10170=EDGE_CURVE('',#7850,#7852,#561,.T.);
#10171=EDGE_CURVE('',#7853,#7854,#5079,.T.);
#10172=EDGE_CURVE('',#7853,#7851,#562,.T.);
#10173=EDGE_CURVE('',#7852,#7854,#563,.T.);
#10174=EDGE_CURVE('',#7855,#7856,#5080,.T.);
#10175=EDGE_CURVE('',#7855,#7853,#564,.T.);
#10176=EDGE_CURVE('',#7854,#7856,#565,.T.);
#10177=EDGE_CURVE('',#7857,#7858,#5081,.T.);
#10178=EDGE_CURVE('',#7857,#7855,#566,.T.);
#10179=EDGE_CURVE('',#7856,#7858,#567,.T.);
#10180=EDGE_CURVE('',#7859,#7860,#5082,.T.);
#10181=EDGE_CURVE('',#7859,#7857,#568,.T.);
#10182=EDGE_CURVE('',#7858,#7860,#569,.T.);
#10183=EDGE_CURVE('',#7861,#7862,#5083,.T.);
#10184=EDGE_CURVE('',#7861,#7859,#570,.T.);
#10185=EDGE_CURVE('',#7860,#7862,#571,.T.);
#10186=EDGE_CURVE('',#7863,#7864,#5084,.T.);
#10187=EDGE_CURVE('',#7863,#7861,#572,.T.);
#10188=EDGE_CURVE('',#7862,#7864,#573,.T.);
#10189=EDGE_CURVE('',#7865,#7866,#5085,.T.);
#10190=EDGE_CURVE('',#7865,#7863,#574,.T.);
#10191=EDGE_CURVE('',#7864,#7866,#575,.T.);
#10192=EDGE_CURVE('',#7867,#7868,#5086,.T.);
#10193=EDGE_CURVE('',#7867,#7865,#576,.T.);
#10194=EDGE_CURVE('',#7866,#7868,#577,.T.);
#10195=EDGE_CURVE('',#7869,#7870,#5087,.T.);
#10196=EDGE_CURVE('',#7869,#7867,#578,.T.);
#10197=EDGE_CURVE('',#7868,#7870,#579,.T.);
#10198=EDGE_CURVE('',#7871,#7872,#5088,.T.);
#10199=EDGE_CURVE('',#7871,#7869,#580,.T.);
#10200=EDGE_CURVE('',#7870,#7872,#581,.T.);
#10201=EDGE_CURVE('',#7873,#7874,#5089,.T.);
#10202=EDGE_CURVE('',#7873,#7871,#582,.T.);
#10203=EDGE_CURVE('',#7872,#7874,#583,.T.);
#10204=EDGE_CURVE('',#7875,#7876,#5090,.T.);
#10205=EDGE_CURVE('',#7875,#7877,#584,.T.);
#10206=EDGE_CURVE('',#7877,#7878,#7393,.T.);
#10207=EDGE_CURVE('',#7876,#7878,#585,.T.);
#10208=EDGE_CURVE('',#7879,#7880,#5091,.T.);
#10209=EDGE_CURVE('',#7879,#7875,#586,.T.);
#10210=EDGE_CURVE('',#7880,#7876,#587,.T.);
#10211=EDGE_CURVE('',#7881,#7882,#5092,.T.);
#10212=EDGE_CURVE('',#7881,#7879,#588,.T.);
#10213=EDGE_CURVE('',#7882,#7880,#589,.T.);
#10214=EDGE_CURVE('',#7883,#7884,#5093,.T.);
#10215=EDGE_CURVE('',#7883,#7881,#590,.T.);
#10216=EDGE_CURVE('',#7884,#7882,#591,.T.);
#10217=EDGE_CURVE('',#7885,#7886,#5094,.T.);
#10218=EDGE_CURVE('',#7885,#7883,#592,.T.);
#10219=EDGE_CURVE('',#7886,#7884,#593,.T.);
#10220=EDGE_CURVE('',#7887,#7888,#5095,.T.);
#10221=EDGE_CURVE('',#7887,#7885,#594,.T.);
#10222=EDGE_CURVE('',#7888,#7886,#595,.T.);
#10223=EDGE_CURVE('',#7889,#7890,#5096,.T.);
#10224=EDGE_CURVE('',#7889,#7887,#596,.T.);
#10225=EDGE_CURVE('',#7890,#7888,#597,.T.);
#10226=EDGE_CURVE('',#7891,#7892,#5097,.T.);
#10227=EDGE_CURVE('',#7891,#7889,#598,.T.);
#10228=EDGE_CURVE('',#7892,#7890,#599,.T.);
#10229=EDGE_CURVE('',#7893,#7894,#5098,.T.);
#10230=EDGE_CURVE('',#7893,#7891,#600,.T.);
#10231=EDGE_CURVE('',#7894,#7892,#601,.T.);
#10232=EDGE_CURVE('',#7895,#7896,#5099,.T.);
#10233=EDGE_CURVE('',#7895,#7893,#602,.T.);
#10234=EDGE_CURVE('',#7896,#7894,#603,.T.);
#10235=EDGE_CURVE('',#7897,#7898,#5100,.T.);
#10236=EDGE_CURVE('',#7897,#7895,#604,.T.);
#10237=EDGE_CURVE('',#7898,#7896,#605,.T.);
#10238=EDGE_CURVE('',#7899,#7900,#5101,.T.);
#10239=EDGE_CURVE('',#7899,#7897,#606,.T.);
#10240=EDGE_CURVE('',#7900,#7898,#607,.T.);
#10241=EDGE_CURVE('',#7901,#7902,#5102,.T.);
#10242=EDGE_CURVE('',#7901,#7899,#608,.T.);
#10243=EDGE_CURVE('',#7902,#7900,#609,.T.);
#10244=EDGE_CURVE('',#7903,#7904,#5103,.T.);
#10245=EDGE_CURVE('',#7903,#7901,#610,.T.);
#10246=EDGE_CURVE('',#7904,#7902,#611,.T.);
#10247=EDGE_CURVE('',#7905,#7906,#5104,.T.);
#10248=EDGE_CURVE('',#7905,#7903,#612,.T.);
#10249=EDGE_CURVE('',#7906,#7904,#613,.T.);
#10250=EDGE_CURVE('',#7907,#7908,#5105,.T.);
#10251=EDGE_CURVE('',#7907,#7905,#614,.T.);
#10252=EDGE_CURVE('',#7908,#7906,#615,.T.);
#10253=EDGE_CURVE('',#7909,#7910,#5106,.T.);
#10254=EDGE_CURVE('',#7909,#7907,#616,.T.);
#10255=EDGE_CURVE('',#7910,#7908,#617,.T.);
#10256=EDGE_CURVE('',#7911,#7912,#5107,.T.);
#10257=EDGE_CURVE('',#7911,#7909,#618,.T.);
#10258=EDGE_CURVE('',#7912,#7910,#619,.T.);
#10259=EDGE_CURVE('',#7913,#7914,#5108,.T.);
#10260=EDGE_CURVE('',#7913,#7911,#620,.T.);
#10261=EDGE_CURVE('',#7914,#7912,#621,.T.);
#10262=EDGE_CURVE('',#7915,#7916,#5109,.T.);
#10263=EDGE_CURVE('',#7915,#7913,#622,.T.);
#10264=EDGE_CURVE('',#7916,#7914,#623,.T.);
#10265=EDGE_CURVE('',#7917,#7918,#5110,.T.);
#10266=EDGE_CURVE('',#7917,#7915,#624,.T.);
#10267=EDGE_CURVE('',#7918,#7916,#625,.T.);
#10268=EDGE_CURVE('',#7919,#7920,#5111,.T.);
#10269=EDGE_CURVE('',#7919,#7917,#626,.T.);
#10270=EDGE_CURVE('',#7920,#7918,#627,.T.);
#10271=EDGE_CURVE('',#7921,#7922,#5112,.T.);
#10272=EDGE_CURVE('',#7921,#7919,#628,.T.);
#10273=EDGE_CURVE('',#7922,#7920,#629,.T.);
#10274=EDGE_CURVE('',#7923,#7924,#5113,.T.);
#10275=EDGE_CURVE('',#7923,#7921,#630,.T.);
#10276=EDGE_CURVE('',#7924,#7922,#631,.T.);
#10277=EDGE_CURVE('',#7878,#7925,#632,.T.);
#10278=EDGE_CURVE('',#7926,#7877,#633,.T.);
#10279=EDGE_CURVE('',#7927,#7926,#7394,.T.);
#10280=EDGE_CURVE('',#7925,#7927,#634,.T.);
#10281=EDGE_CURVE('',#7925,#7928,#5114,.T.);
#10282=EDGE_CURVE('',#7928,#7928,#7395,.T.);
#10283=EDGE_CURVE('',#7929,#7923,#635,.T.);
#10284=EDGE_CURVE('',#7827,#7929,#636,.T.);
#10285=EDGE_CURVE('',#7926,#7873,#637,.T.);
#10286=EDGE_CURVE('',#7930,#7924,#638,.T.);
#10287=EDGE_CURVE('',#7929,#7930,#7396,.T.);
#10288=EDGE_CURVE('',#7874,#7927,#639,.T.);
#10289=EDGE_CURVE('',#7930,#7828,#640,.T.);
#10290=EDGE_CURVE('',#7931,#7932,#5115,.T.);
#10291=EDGE_CURVE('',#7931,#7933,#5116,.T.);
#10292=EDGE_CURVE('',#7933,#7934,#5117,.T.);
#10293=EDGE_CURVE('',#7932,#7934,#5118,.T.);
#10294=EDGE_CURVE('',#7935,#7931,#5119,.T.);
#10295=EDGE_CURVE('',#7935,#7936,#5120,.T.);
#10296=EDGE_CURVE('',#7936,#7933,#5121,.T.);
#10297=EDGE_CURVE('',#7937,#7935,#5122,.T.);
#10298=EDGE_CURVE('',#7937,#7938,#5123,.T.);
#10299=EDGE_CURVE('',#7938,#7936,#5124,.T.);
#10300=EDGE_CURVE('',#7939,#7937,#5125,.T.);
#10301=EDGE_CURVE('',#7939,#7940,#5126,.T.);
#10302=EDGE_CURVE('',#7940,#7938,#5127,.T.);
#10303=EDGE_CURVE('',#7941,#7939,#5128,.T.);
#10304=EDGE_CURVE('',#7941,#7942,#5129,.T.);
#10305=EDGE_CURVE('',#7942,#7940,#5130,.T.);
#10306=EDGE_CURVE('',#7932,#7941,#5131,.T.);
#10307=EDGE_CURVE('',#7934,#7942,#5132,.T.);
#10308=EDGE_CURVE('',#7943,#7943,#7397,.T.);
#10309=EDGE_CURVE('',#7943,#7944,#5133,.T.);
#10310=EDGE_CURVE('',#7944,#7944,#7398,.T.);
#13748=ORIENTED_EDGE('',*,*,#10131,.F.);
#13749=ORIENTED_EDGE('',*,*,#10132,.T.);
#13750=ORIENTED_EDGE('',*,*,#10133,.T.);
#13751=ORIENTED_EDGE('',*,*,#10134,.T.);
#13752=ORIENTED_EDGE('',*,*,#10135,.F.);
#13753=ORIENTED_EDGE('',*,*,#10136,.T.);
#13754=ORIENTED_EDGE('',*,*,#10131,.T.);
#13755=ORIENTED_EDGE('',*,*,#10137,.T.);
#13756=ORIENTED_EDGE('',*,*,#10138,.F.);
#13757=ORIENTED_EDGE('',*,*,#10139,.T.);
#13758=ORIENTED_EDGE('',*,*,#10135,.T.);
#13759=ORIENTED_EDGE('',*,*,#10140,.T.);
#13760=ORIENTED_EDGE('',*,*,#10141,.F.);
#13761=ORIENTED_EDGE('',*,*,#10142,.T.);
#13762=ORIENTED_EDGE('',*,*,#10138,.T.);
#13763=ORIENTED_EDGE('',*,*,#10143,.T.);
#13764=ORIENTED_EDGE('',*,*,#10144,.F.);
#13765=ORIENTED_EDGE('',*,*,#10145,.T.);
#13766=ORIENTED_EDGE('',*,*,#10141,.T.);
#13767=ORIENTED_EDGE('',*,*,#10146,.T.);
#13768=ORIENTED_EDGE('',*,*,#10147,.F.);
#13769=ORIENTED_EDGE('',*,*,#10148,.T.);
#13770=ORIENTED_EDGE('',*,*,#10144,.T.);
#13771=ORIENTED_EDGE('',*,*,#10149,.T.);
#13772=ORIENTED_EDGE('',*,*,#10150,.F.);
#13773=ORIENTED_EDGE('',*,*,#10151,.T.);
#13774=ORIENTED_EDGE('',*,*,#10147,.T.);
#13775=ORIENTED_EDGE('',*,*,#10152,.T.);
#13776=ORIENTED_EDGE('',*,*,#10153,.F.);
#13777=ORIENTED_EDGE('',*,*,#10154,.T.);
#13778=ORIENTED_EDGE('',*,*,#10150,.T.);
#13779=ORIENTED_EDGE('',*,*,#10155,.T.);
#13780=ORIENTED_EDGE('',*,*,#10156,.F.);
#13781=ORIENTED_EDGE('',*,*,#10157,.T.);
#13782=ORIENTED_EDGE('',*,*,#10153,.T.);
#13783=ORIENTED_EDGE('',*,*,#10158,.T.);
#13784=ORIENTED_EDGE('',*,*,#10159,.F.);
#13785=ORIENTED_EDGE('',*,*,#10160,.T.);
#13786=ORIENTED_EDGE('',*,*,#10156,.T.);
#13787=ORIENTED_EDGE('',*,*,#10161,.T.);
#13788=ORIENTED_EDGE('',*,*,#10162,.F.);
#13789=ORIENTED_EDGE('',*,*,#10163,.T.);
#13790=ORIENTED_EDGE('',*,*,#10159,.T.);
#13791=ORIENTED_EDGE('',*,*,#10164,.T.);
#13792=ORIENTED_EDGE('',*,*,#10165,.F.);
#13793=ORIENTED_EDGE('',*,*,#10166,.T.);
#13794=ORIENTED_EDGE('',*,*,#10162,.T.);
#13795=ORIENTED_EDGE('',*,*,#10167,.T.);
#13796=ORIENTED_EDGE('',*,*,#10168,.F.);
#13797=ORIENTED_EDGE('',*,*,#10169,.T.);
#13798=ORIENTED_EDGE('',*,*,#10165,.T.);
#13799=ORIENTED_EDGE('',*,*,#10170,.T.);
#13800=ORIENTED_EDGE('',*,*,#10171,.F.);
#13801=ORIENTED_EDGE('',*,*,#10172,.T.);
#13802=ORIENTED_EDGE('',*,*,#10168,.T.);
#13803=ORIENTED_EDGE('',*,*,#10173,.T.);
#13804=ORIENTED_EDGE('',*,*,#10174,.F.);
#13805=ORIENTED_EDGE('',*,*,#10175,.T.);
#13806=ORIENTED_EDGE('',*,*,#10171,.T.);
#13807=ORIENTED_EDGE('',*,*,#10176,.T.);
#13808=ORIENTED_EDGE('',*,*,#10177,.F.);
#13809=ORIENTED_EDGE('',*,*,#10178,.T.);
#13810=ORIENTED_EDGE('',*,*,#10174,.T.);
#13811=ORIENTED_EDGE('',*,*,#10179,.T.);
#13812=ORIENTED_EDGE('',*,*,#10180,.F.);
#13813=ORIENTED_EDGE('',*,*,#10181,.T.);
#13814=ORIENTED_EDGE('',*,*,#10177,.T.);
#13815=ORIENTED_EDGE('',*,*,#10182,.T.);
#13816=ORIENTED_EDGE('',*,*,#10183,.F.);
#13817=ORIENTED_EDGE('',*,*,#10184,.T.);
#13818=ORIENTED_EDGE('',*,*,#10180,.T.);
#13819=ORIENTED_EDGE('',*,*,#10185,.T.);
#13820=ORIENTED_EDGE('',*,*,#10186,.F.);
#13821=ORIENTED_EDGE('',*,*,#10187,.T.);
#13822=ORIENTED_EDGE('',*,*,#10183,.T.);
#13823=ORIENTED_EDGE('',*,*,#10188,.T.);
#13824=ORIENTED_EDGE('',*,*,#10189,.F.);
#13825=ORIENTED_EDGE('',*,*,#10190,.T.);
#13826=ORIENTED_EDGE('',*,*,#10186,.T.);
#13827=ORIENTED_EDGE('',*,*,#10191,.T.);
#13828=ORIENTED_EDGE('',*,*,#10192,.F.);
#13829=ORIENTED_EDGE('',*,*,#10193,.T.);
#13830=ORIENTED_EDGE('',*,*,#10189,.T.);
#13831=ORIENTED_EDGE('',*,*,#10194,.T.);
#13832=ORIENTED_EDGE('',*,*,#10195,.F.);
#13833=ORIENTED_EDGE('',*,*,#10196,.T.);
#13834=ORIENTED_EDGE('',*,*,#10192,.T.);
#13835=ORIENTED_EDGE('',*,*,#10197,.T.);
#13836=ORIENTED_EDGE('',*,*,#10198,.F.);
#13837=ORIENTED_EDGE('',*,*,#10199,.T.);
#13838=ORIENTED_EDGE('',*,*,#10195,.T.);
#13839=ORIENTED_EDGE('',*,*,#10200,.T.);
#13840=ORIENTED_EDGE('',*,*,#10201,.F.);
#13841=ORIENTED_EDGE('',*,*,#10202,.T.);
#13842=ORIENTED_EDGE('',*,*,#10198,.T.);
#13843=ORIENTED_EDGE('',*,*,#10203,.T.);
#13844=ORIENTED_EDGE('',*,*,#10204,.F.);
#13845=ORIENTED_EDGE('',*,*,#10205,.T.);
#13846=ORIENTED_EDGE('',*,*,#10206,.T.);
#13847=ORIENTED_EDGE('',*,*,#10207,.F.);
#13848=ORIENTED_EDGE('',*,*,#10208,.F.);
#13849=ORIENTED_EDGE('',*,*,#10209,.T.);
#13850=ORIENTED_EDGE('',*,*,#10204,.T.);
#13851=ORIENTED_EDGE('',*,*,#10210,.F.);
#13852=ORIENTED_EDGE('',*,*,#10211,.F.);
#13853=ORIENTED_EDGE('',*,*,#10212,.T.);
#13854=ORIENTED_EDGE('',*,*,#10208,.T.);
#13855=ORIENTED_EDGE('',*,*,#10213,.F.);
#13856=ORIENTED_EDGE('',*,*,#10214,.F.);
#13857=ORIENTED_EDGE('',*,*,#10215,.T.);
#13858=ORIENTED_EDGE('',*,*,#10211,.T.);
#13859=ORIENTED_EDGE('',*,*,#10216,.F.);
#13860=ORIENTED_EDGE('',*,*,#10217,.F.);
#13861=ORIENTED_EDGE('',*,*,#10218,.T.);
#13862=ORIENTED_EDGE('',*,*,#10214,.T.);
#13863=ORIENTED_EDGE('',*,*,#10219,.F.);
#13864=ORIENTED_EDGE('',*,*,#10220,.F.);
#13865=ORIENTED_EDGE('',*,*,#10221,.T.);
#13866=ORIENTED_EDGE('',*,*,#10217,.T.);
#13867=ORIENTED_EDGE('',*,*,#10222,.F.);
#13868=ORIENTED_EDGE('',*,*,#10223,.F.);
#13869=ORIENTED_EDGE('',*,*,#10224,.T.);
#13870=ORIENTED_EDGE('',*,*,#10220,.T.);
#13871=ORIENTED_EDGE('',*,*,#10225,.F.);
#13872=ORIENTED_EDGE('',*,*,#10226,.F.);
#13873=ORIENTED_EDGE('',*,*,#10227,.T.);
#13874=ORIENTED_EDGE('',*,*,#10223,.T.);
#13875=ORIENTED_EDGE('',*,*,#10228,.F.);
#13876=ORIENTED_EDGE('',*,*,#10229,.F.);
#13877=ORIENTED_EDGE('',*,*,#10230,.T.);
#13878=ORIENTED_EDGE('',*,*,#10226,.T.);
#13879=ORIENTED_EDGE('',*,*,#10231,.F.);
#13880=ORIENTED_EDGE('',*,*,#10232,.F.);
#13881=ORIENTED_EDGE('',*,*,#10233,.T.);
#13882=ORIENTED_EDGE('',*,*,#10229,.T.);
#13883=ORIENTED_EDGE('',*,*,#10234,.F.);
#13884=ORIENTED_EDGE('',*,*,#10235,.F.);
#13885=ORIENTED_EDGE('',*,*,#10236,.T.);
#13886=ORIENTED_EDGE('',*,*,#10232,.T.);
#13887=ORIENTED_EDGE('',*,*,#10237,.F.);
#13888=ORIENTED_EDGE('',*,*,#10238,.F.);
#13889=ORIENTED_EDGE('',*,*,#10239,.T.);
#13890=ORIENTED_EDGE('',*,*,#10235,.T.);
#13891=ORIENTED_EDGE('',*,*,#10240,.F.);
#13892=ORIENTED_EDGE('',*,*,#10241,.F.);
#13893=ORIENTED_EDGE('',*,*,#10242,.T.);
#13894=ORIENTED_EDGE('',*,*,#10238,.T.);
#13895=ORIENTED_EDGE('',*,*,#10243,.F.);
#13896=ORIENTED_EDGE('',*,*,#10244,.F.);
#13897=ORIENTED_EDGE('',*,*,#10245,.T.);
#13898=ORIENTED_EDGE('',*,*,#10241,.T.);
#13899=ORIENTED_EDGE('',*,*,#10246,.F.);
#13900=ORIENTED_EDGE('',*,*,#10247,.F.);
#13901=ORIENTED_EDGE('',*,*,#10248,.T.);
#13902=ORIENTED_EDGE('',*,*,#10244,.T.);
#13903=ORIENTED_EDGE('',*,*,#10249,.F.);
#13904=ORIENTED_EDGE('',*,*,#10250,.F.);
#13905=ORIENTED_EDGE('',*,*,#10251,.T.);
#13906=ORIENTED_EDGE('',*,*,#10247,.T.);
#13907=ORIENTED_EDGE('',*,*,#10252,.F.);
#13908=ORIENTED_EDGE('',*,*,#10253,.F.);
#13909=ORIENTED_EDGE('',*,*,#10254,.T.);
#13910=ORIENTED_EDGE('',*,*,#10250,.T.);
#13911=ORIENTED_EDGE('',*,*,#10255,.F.);
#13912=ORIENTED_EDGE('',*,*,#10256,.F.);
#13913=ORIENTED_EDGE('',*,*,#10257,.T.);
#13914=ORIENTED_EDGE('',*,*,#10253,.T.);
#13915=ORIENTED_EDGE('',*,*,#10258,.F.);
#13916=ORIENTED_EDGE('',*,*,#10259,.F.);
#13917=ORIENTED_EDGE('',*,*,#10260,.T.);
#13918=ORIENTED_EDGE('',*,*,#10256,.T.);
#13919=ORIENTED_EDGE('',*,*,#10261,.F.);
#13920=ORIENTED_EDGE('',*,*,#10262,.F.);
#13921=ORIENTED_EDGE('',*,*,#10263,.T.);
#13922=ORIENTED_EDGE('',*,*,#10259,.T.);
#13923=ORIENTED_EDGE('',*,*,#10264,.F.);
#13924=ORIENTED_EDGE('',*,*,#10265,.F.);
#13925=ORIENTED_EDGE('',*,*,#10266,.T.);
#13926=ORIENTED_EDGE('',*,*,#10262,.T.);
#13927=ORIENTED_EDGE('',*,*,#10267,.F.);
#13928=ORIENTED_EDGE('',*,*,#10268,.F.);
#13929=ORIENTED_EDGE('',*,*,#10269,.T.);
#13930=ORIENTED_EDGE('',*,*,#10265,.T.);
#13931=ORIENTED_EDGE('',*,*,#10270,.F.);
#13932=ORIENTED_EDGE('',*,*,#10271,.F.);
#13933=ORIENTED_EDGE('',*,*,#10272,.T.);
#13934=ORIENTED_EDGE('',*,*,#10268,.T.);
#13935=ORIENTED_EDGE('',*,*,#10273,.F.);
#13936=ORIENTED_EDGE('',*,*,#10274,.F.);
#13937=ORIENTED_EDGE('',*,*,#10275,.T.);
#13938=ORIENTED_EDGE('',*,*,#10271,.T.);
#13939=ORIENTED_EDGE('',*,*,#10276,.F.);
#13940=ORIENTED_EDGE('',*,*,#10277,.F.);
#13941=ORIENTED_EDGE('',*,*,#10206,.F.);
#13942=ORIENTED_EDGE('',*,*,#10278,.F.);
#13943=ORIENTED_EDGE('',*,*,#10279,.F.);
#13944=ORIENTED_EDGE('',*,*,#10280,.F.);
#13945=ORIENTED_EDGE('',*,*,#10281,.T.);
#13946=ORIENTED_EDGE('',*,*,#10282,.F.);
#13947=ORIENTED_EDGE('',*,*,#10281,.F.);
#13948=ORIENTED_EDGE('',*,*,#10278,.T.);
#13949=ORIENTED_EDGE('',*,*,#10205,.F.);
#13950=ORIENTED_EDGE('',*,*,#10209,.F.);
#13951=ORIENTED_EDGE('',*,*,#10212,.F.);
#13952=ORIENTED_EDGE('',*,*,#10215,.F.);
#13953=ORIENTED_EDGE('',*,*,#10218,.F.);
#13954=ORIENTED_EDGE('',*,*,#10221,.F.);
#13955=ORIENTED_EDGE('',*,*,#10224,.F.);
#13956=ORIENTED_EDGE('',*,*,#10227,.F.);
#13957=ORIENTED_EDGE('',*,*,#10230,.F.);
#13958=ORIENTED_EDGE('',*,*,#10233,.F.);
#13959=ORIENTED_EDGE('',*,*,#10236,.F.);
#13960=ORIENTED_EDGE('',*,*,#10239,.F.);
#13961=ORIENTED_EDGE('',*,*,#10242,.F.);
#13962=ORIENTED_EDGE('',*,*,#10245,.F.);
#13963=ORIENTED_EDGE('',*,*,#10248,.F.);
#13964=ORIENTED_EDGE('',*,*,#10251,.F.);
#13965=ORIENTED_EDGE('',*,*,#10254,.F.);
#13966=ORIENTED_EDGE('',*,*,#10257,.F.);
#13967=ORIENTED_EDGE('',*,*,#10260,.F.);
#13968=ORIENTED_EDGE('',*,*,#10263,.F.);
#13969=ORIENTED_EDGE('',*,*,#10266,.F.);
#13970=ORIENTED_EDGE('',*,*,#10269,.F.);
#13971=ORIENTED_EDGE('',*,*,#10272,.F.);
#13972=ORIENTED_EDGE('',*,*,#10275,.F.);
#13973=ORIENTED_EDGE('',*,*,#10283,.F.);
#13974=ORIENTED_EDGE('',*,*,#10284,.F.);
#13975=ORIENTED_EDGE('',*,*,#10132,.F.);
#13976=ORIENTED_EDGE('',*,*,#10136,.F.);
#13977=ORIENTED_EDGE('',*,*,#10139,.F.);
#13978=ORIENTED_EDGE('',*,*,#10142,.F.);
#13979=ORIENTED_EDGE('',*,*,#10145,.F.);
#13980=ORIENTED_EDGE('',*,*,#10148,.F.);
#13981=ORIENTED_EDGE('',*,*,#10151,.F.);
#13982=ORIENTED_EDGE('',*,*,#10154,.F.);
#13983=ORIENTED_EDGE('',*,*,#10157,.F.);
#13984=ORIENTED_EDGE('',*,*,#10160,.F.);
#13985=ORIENTED_EDGE('',*,*,#10163,.F.);
#13986=ORIENTED_EDGE('',*,*,#10166,.F.);
#13987=ORIENTED_EDGE('',*,*,#10169,.F.);
#13988=ORIENTED_EDGE('',*,*,#10172,.F.);
#13989=ORIENTED_EDGE('',*,*,#10175,.F.);
#13990=ORIENTED_EDGE('',*,*,#10178,.F.);
#13991=ORIENTED_EDGE('',*,*,#10181,.F.);
#13992=ORIENTED_EDGE('',*,*,#10184,.F.);
#13993=ORIENTED_EDGE('',*,*,#10187,.F.);
#13994=ORIENTED_EDGE('',*,*,#10190,.F.);
#13995=ORIENTED_EDGE('',*,*,#10193,.F.);
#13996=ORIENTED_EDGE('',*,*,#10196,.F.);
#13997=ORIENTED_EDGE('',*,*,#10199,.F.);
#13998=ORIENTED_EDGE('',*,*,#10202,.F.);
#13999=ORIENTED_EDGE('',*,*,#10285,.F.);
#14000=ORIENTED_EDGE('',*,*,#10274,.T.);
#14001=ORIENTED_EDGE('',*,*,#10286,.F.);
#14002=ORIENTED_EDGE('',*,*,#10287,.F.);
#14003=ORIENTED_EDGE('',*,*,#10283,.T.);
#14004=ORIENTED_EDGE('',*,*,#10277,.T.);
#14005=ORIENTED_EDGE('',*,*,#10280,.T.);
#14006=ORIENTED_EDGE('',*,*,#10288,.F.);
#14007=ORIENTED_EDGE('',*,*,#10203,.F.);
#14008=ORIENTED_EDGE('',*,*,#10200,.F.);
#14009=ORIENTED_EDGE('',*,*,#10197,.F.);
#14010=ORIENTED_EDGE('',*,*,#10194,.F.);
#14011=ORIENTED_EDGE('',*,*,#10191,.F.);
#14012=ORIENTED_EDGE('',*,*,#10188,.F.);
#14013=ORIENTED_EDGE('',*,*,#10185,.F.);
#14014=ORIENTED_EDGE('',*,*,#10182,.F.);
#14015=ORIENTED_EDGE('',*,*,#10179,.F.);
#14016=ORIENTED_EDGE('',*,*,#10176,.F.);
#14017=ORIENTED_EDGE('',*,*,#10173,.F.);
#14018=ORIENTED_EDGE('',*,*,#10170,.F.);
#14019=ORIENTED_EDGE('',*,*,#10167,.F.);
#14020=ORIENTED_EDGE('',*,*,#10164,.F.);
#14021=ORIENTED_EDGE('',*,*,#10161,.F.);
#14022=ORIENTED_EDGE('',*,*,#10158,.F.);
#14023=ORIENTED_EDGE('',*,*,#10155,.F.);
#14024=ORIENTED_EDGE('',*,*,#10152,.F.);
#14025=ORIENTED_EDGE('',*,*,#10149,.F.);
#14026=ORIENTED_EDGE('',*,*,#10146,.F.);
#14027=ORIENTED_EDGE('',*,*,#10143,.F.);
#14028=ORIENTED_EDGE('',*,*,#10140,.F.);
#14029=ORIENTED_EDGE('',*,*,#10137,.F.);
#14030=ORIENTED_EDGE('',*,*,#10134,.F.);
#14031=ORIENTED_EDGE('',*,*,#10289,.F.);
#14032=ORIENTED_EDGE('',*,*,#10286,.T.);
#14033=ORIENTED_EDGE('',*,*,#10276,.T.);
#14034=ORIENTED_EDGE('',*,*,#10273,.T.);
#14035=ORIENTED_EDGE('',*,*,#10270,.T.);
#14036=ORIENTED_EDGE('',*,*,#10267,.T.);
#14037=ORIENTED_EDGE('',*,*,#10264,.T.);
#14038=ORIENTED_EDGE('',*,*,#10261,.T.);
#14039=ORIENTED_EDGE('',*,*,#10258,.T.);
#14040=ORIENTED_EDGE('',*,*,#10255,.T.);
#14041=ORIENTED_EDGE('',*,*,#10252,.T.);
#14042=ORIENTED_EDGE('',*,*,#10249,.T.);
#14043=ORIENTED_EDGE('',*,*,#10246,.T.);
#14044=ORIENTED_EDGE('',*,*,#10243,.T.);
#14045=ORIENTED_EDGE('',*,*,#10240,.T.);
#14046=ORIENTED_EDGE('',*,*,#10237,.T.);
#14047=ORIENTED_EDGE('',*,*,#10234,.T.);
#14048=ORIENTED_EDGE('',*,*,#10231,.T.);
#14049=ORIENTED_EDGE('',*,*,#10228,.T.);
#14050=ORIENTED_EDGE('',*,*,#10225,.T.);
#14051=ORIENTED_EDGE('',*,*,#10222,.T.);
#14052=ORIENTED_EDGE('',*,*,#10219,.T.);
#14053=ORIENTED_EDGE('',*,*,#10216,.T.);
#14054=ORIENTED_EDGE('',*,*,#10213,.T.);
#14055=ORIENTED_EDGE('',*,*,#10210,.T.);
#14056=ORIENTED_EDGE('',*,*,#10207,.T.);
#14057=ORIENTED_EDGE('',*,*,#10201,.T.);
#14058=ORIENTED_EDGE('',*,*,#10288,.T.);
#14059=ORIENTED_EDGE('',*,*,#10279,.T.);
#14060=ORIENTED_EDGE('',*,*,#10285,.T.);
#14061=ORIENTED_EDGE('',*,*,#10290,.F.);
#14062=ORIENTED_EDGE('',*,*,#10291,.T.);
#14063=ORIENTED_EDGE('',*,*,#10292,.T.);
#14064=ORIENTED_EDGE('',*,*,#10293,.F.);
#14065=ORIENTED_EDGE('',*,*,#10294,.F.);
#14066=ORIENTED_EDGE('',*,*,#10295,.T.);
#14067=ORIENTED_EDGE('',*,*,#10296,.T.);
#14068=ORIENTED_EDGE('',*,*,#10291,.F.);
#14069=ORIENTED_EDGE('',*,*,#10297,.F.);
#14070=ORIENTED_EDGE('',*,*,#10298,.T.);
#14071=ORIENTED_EDGE('',*,*,#10299,.T.);
#14072=ORIENTED_EDGE('',*,*,#10295,.F.);
#14073=ORIENTED_EDGE('',*,*,#10300,.F.);
#14074=ORIENTED_EDGE('',*,*,#10301,.T.);
#14075=ORIENTED_EDGE('',*,*,#10302,.T.);
#14076=ORIENTED_EDGE('',*,*,#10298,.F.);
#14077=ORIENTED_EDGE('',*,*,#10303,.F.);
#14078=ORIENTED_EDGE('',*,*,#10304,.T.);
#14079=ORIENTED_EDGE('',*,*,#10305,.T.);
#14080=ORIENTED_EDGE('',*,*,#10301,.F.);
#14081=ORIENTED_EDGE('',*,*,#10306,.F.);
#14082=ORIENTED_EDGE('',*,*,#10293,.T.);
#14083=ORIENTED_EDGE('',*,*,#10307,.T.);
#14084=ORIENTED_EDGE('',*,*,#10304,.F.);
#14085=ORIENTED_EDGE('',*,*,#10307,.F.);
#14086=ORIENTED_EDGE('',*,*,#10292,.F.);
#14087=ORIENTED_EDGE('',*,*,#10296,.F.);
#14088=ORIENTED_EDGE('',*,*,#10299,.F.);
#14089=ORIENTED_EDGE('',*,*,#10302,.F.);
#14090=ORIENTED_EDGE('',*,*,#10305,.F.);
#14091=ORIENTED_EDGE('',*,*,#10308,.T.);
#14092=ORIENTED_EDGE('',*,*,#10284,.T.);
#14093=ORIENTED_EDGE('',*,*,#10287,.T.);
#14094=ORIENTED_EDGE('',*,*,#10289,.T.);
#14095=ORIENTED_EDGE('',*,*,#10133,.F.);
#14096=ORIENTED_EDGE('',*,*,#10308,.F.);
#14097=ORIENTED_EDGE('',*,*,#10309,.T.);
#14098=ORIENTED_EDGE('',*,*,#10310,.T.);
#14099=ORIENTED_EDGE('',*,*,#10309,.F.);
#14100=ORIENTED_EDGE('',*,*,#10310,.F.);
#14101=ORIENTED_EDGE('',*,*,#10290,.T.);
#14102=ORIENTED_EDGE('',*,*,#10306,.T.);
#14103=ORIENTED_EDGE('',*,*,#10303,.T.);
#14104=ORIENTED_EDGE('',*,*,#10300,.T.);
#14105=ORIENTED_EDGE('',*,*,#10297,.T.);
#14106=ORIENTED_EDGE('',*,*,#10294,.T.);
#14107=ORIENTED_EDGE('',*,*,#10282,.T.);
#19788=CYLINDRICAL_SURFACE('',#22178,3.942);
#19789=CYLINDRICAL_SURFACE('',#22180,3.942);
#19790=CYLINDRICAL_SURFACE('',#22181,3.942);
#19791=CYLINDRICAL_SURFACE('',#22182,3.942);
#19792=CYLINDRICAL_SURFACE('',#22183,3.942);
#19793=CYLINDRICAL_SURFACE('',#22184,3.942);
#19794=CYLINDRICAL_SURFACE('',#22185,3.942);
#19795=CYLINDRICAL_SURFACE('',#22186,3.942);
#19796=CYLINDRICAL_SURFACE('',#22187,3.942);
#19797=CYLINDRICAL_SURFACE('',#22188,3.942);
#19798=CYLINDRICAL_SURFACE('',#22189,3.942);
#19799=CYLINDRICAL_SURFACE('',#22190,3.942);
#19800=CYLINDRICAL_SURFACE('',#22191,3.942);
#19801=CYLINDRICAL_SURFACE('',#22192,3.942);
#19802=CYLINDRICAL_SURFACE('',#22193,3.942);
#19803=CYLINDRICAL_SURFACE('',#22194,3.942);
#19804=CYLINDRICAL_SURFACE('',#22195,3.942);
#19805=CYLINDRICAL_SURFACE('',#22196,3.942);
#19806=CYLINDRICAL_SURFACE('',#22197,3.942);
#19807=CYLINDRICAL_SURFACE('',#22198,3.942);
#19808=CYLINDRICAL_SURFACE('',#22199,3.942);
#19809=CYLINDRICAL_SURFACE('',#22200,3.942);
#19810=CYLINDRICAL_SURFACE('',#22201,3.942);
#19811=CYLINDRICAL_SURFACE('',#22202,3.942);
#19812=CYLINDRICAL_SURFACE('',#22203,3.37175);
#19813=CYLINDRICAL_SURFACE('',#22205,3.37175);
#19814=CYLINDRICAL_SURFACE('',#22206,3.37175);
#19815=CYLINDRICAL_SURFACE('',#22207,3.37175);
#19816=CYLINDRICAL_SURFACE('',#22208,3.37175);
#19817=CYLINDRICAL_SURFACE('',#22209,3.37175);
#19818=CYLINDRICAL_SURFACE('',#22210,3.37175);
#19819=CYLINDRICAL_SURFACE('',#22211,3.37175);
#19820=CYLINDRICAL_SURFACE('',#22212,3.37175);
#19821=CYLINDRICAL_SURFACE('',#22213,3.37175);
#19822=CYLINDRICAL_SURFACE('',#22214,3.37175);
#19823=CYLINDRICAL_SURFACE('',#22215,3.37175);
#19824=CYLINDRICAL_SURFACE('',#22216,3.37175);
#19825=CYLINDRICAL_SURFACE('',#22217,3.37175);
#19826=CYLINDRICAL_SURFACE('',#22218,3.37175);
#19827=CYLINDRICAL_SURFACE('',#22219,3.37175);
#19828=CYLINDRICAL_SURFACE('',#22220,3.37175);
#19829=CYLINDRICAL_SURFACE('',#22221,3.37175);
#19830=CYLINDRICAL_SURFACE('',#22222,3.37175);
#19831=CYLINDRICAL_SURFACE('',#22223,3.37175);
#19832=CYLINDRICAL_SURFACE('',#22224,3.37175);
#19833=CYLINDRICAL_SURFACE('',#22225,3.37175);
#19834=CYLINDRICAL_SURFACE('',#22226,3.37175);
#19835=CYLINDRICAL_SURFACE('',#22227,3.37175);
#19836=CYLINDRICAL_SURFACE('',#22231,3.37175);
#19837=CYLINDRICAL_SURFACE('',#22233,3.942);
#19838=CYLINDRICAL_SURFACE('',#22243,6.5);
#20769=ADVANCED_FACE('',(#2649),#19788,.T.);
#20770=ADVANCED_FACE('',(#2650),#19789,.T.);
#20771=ADVANCED_FACE('',(#2651),#19790,.T.);
#20772=ADVANCED_FACE('',(#2652),#19791,.T.);
#20773=ADVANCED_FACE('',(#2653),#19792,.T.);
#20774=ADVANCED_FACE('',(#2654),#19793,.T.);
#20775=ADVANCED_FACE('',(#2655),#19794,.T.);
#20776=ADVANCED_FACE('',(#2656),#19795,.T.);
#20777=ADVANCED_FACE('',(#2657),#19796,.T.);
#20778=ADVANCED_FACE('',(#2658),#19797,.T.);
#20779=ADVANCED_FACE('',(#2659),#19798,.T.);
#20780=ADVANCED_FACE('',(#2660),#19799,.T.);
#20781=ADVANCED_FACE('',(#2661),#19800,.T.);
#20782=ADVANCED_FACE('',(#2662),#19801,.T.);
#20783=ADVANCED_FACE('',(#2663),#19802,.T.);
#20784=ADVANCED_FACE('',(#2664),#19803,.T.);
#20785=ADVANCED_FACE('',(#2665),#19804,.T.);
#20786=ADVANCED_FACE('',(#2666),#19805,.T.);
#20787=ADVANCED_FACE('',(#2667),#19806,.T.);
#20788=ADVANCED_FACE('',(#2668),#19807,.T.);
#20789=ADVANCED_FACE('',(#2669),#19808,.T.);
#20790=ADVANCED_FACE('',(#2670),#19809,.T.);
#20791=ADVANCED_FACE('',(#2671),#19810,.T.);
#20792=ADVANCED_FACE('',(#2672),#19811,.T.);
#20793=ADVANCED_FACE('',(#2673),#19812,.T.);
#20794=ADVANCED_FACE('',(#2674),#19813,.T.);
#20795=ADVANCED_FACE('',(#2675),#19814,.T.);
#20796=ADVANCED_FACE('',(#2676),#19815,.T.);
#20797=ADVANCED_FACE('',(#2677),#19816,.T.);
#20798=ADVANCED_FACE('',(#2678),#19817,.T.);
#20799=ADVANCED_FACE('',(#2679),#19818,.T.);
#20800=ADVANCED_FACE('',(#2680),#19819,.T.);
#20801=ADVANCED_FACE('',(#2681),#19820,.T.);
#20802=ADVANCED_FACE('',(#2682),#19821,.T.);
#20803=ADVANCED_FACE('',(#2683),#19822,.T.);
#20804=ADVANCED_FACE('',(#2684),#19823,.T.);
#20805=ADVANCED_FACE('',(#2685),#19824,.T.);
#20806=ADVANCED_FACE('',(#2686),#19825,.T.);
#20807=ADVANCED_FACE('',(#2687),#19826,.T.);
#20808=ADVANCED_FACE('',(#2688),#19827,.T.);
#20809=ADVANCED_FACE('',(#2689),#19828,.T.);
#20810=ADVANCED_FACE('',(#2690),#19829,.T.);
#20811=ADVANCED_FACE('',(#2691),#19830,.T.);
#20812=ADVANCED_FACE('',(#2692),#19831,.T.);
#20813=ADVANCED_FACE('',(#2693),#19832,.T.);
#20814=ADVANCED_FACE('',(#2694),#19833,.T.);
#20815=ADVANCED_FACE('',(#2695),#19834,.T.);
#20816=ADVANCED_FACE('',(#2696),#19835,.T.);
#20817=ADVANCED_FACE('',(#2697),#330,.T.);
#20818=ADVANCED_FACE('',(#2698),#342,.F.);
#20819=ADVANCED_FACE('',(#2699),#19836,.T.);
#20820=ADVANCED_FACE('',(#2700),#343,.F.);
#20821=ADVANCED_FACE('',(#2701),#19837,.T.);
#20822=ADVANCED_FACE('',(#2702),#2405,.F.);
#20823=ADVANCED_FACE('',(#2703),#2406,.F.);
#20824=ADVANCED_FACE('',(#2704),#2407,.F.);
#20825=ADVANCED_FACE('',(#2705),#2408,.F.);
#20826=ADVANCED_FACE('',(#2706),#2409,.F.);
#20827=ADVANCED_FACE('',(#2707),#2410,.F.);
#20828=ADVANCED_FACE('',(#2708),#2411,.F.);
#20829=ADVANCED_FACE('',(#2709,#2312),#2412,.T.);
#20830=ADVANCED_FACE('',(#2710),#19838,.T.);
#20831=ADVANCED_FACE('',(#2711,#2313),#2413,.F.);
#20832=ADVANCED_FACE('',(#2712),#2414,.T.);
#21814=CLOSED_SHELL('',(#20769,#20770,#20771,#20772,#20773,#20774,#20775,
#20776,#20777,#20778,#20779,#20780,#20781,#20782,#20783,#20784,#20785,#20786,
#20787,#20788,#20789,#20790,#20791,#20792,#20793,#20794,#20795,#20796,#20797,
#20798,#20799,#20800,#20801,#20802,#20803,#20804,#20805,#20806,#20807,#20808,
#20809,#20810,#20811,#20812,#20813,#20814,#20815,#20816,#20817,#20818,#20819,
#20820,#20821,#20822,#20823,#20824,#20825,#20826,#20827,#20828,#20829,#20830,
#20831,#20832));
#22177=AXIS2_PLACEMENT_3D('',#33615,#23906,#23907);
#22178=AXIS2_PLACEMENT_3D('',#33616,#23908,#23909);
#22179=AXIS2_PLACEMENT_3D('',#33632,#23911,#23912);
#22180=AXIS2_PLACEMENT_3D('',#33640,#23913,#23914);
#22181=AXIS2_PLACEMENT_3D('',#33688,#23916,#23917);
#22182=AXIS2_PLACEMENT_3D('',#33736,#23919,#23920);
#22183=AXIS2_PLACEMENT_3D('',#33784,#23922,#23923);
#22184=AXIS2_PLACEMENT_3D('',#33838,#23925,#23926);
#22185=AXIS2_PLACEMENT_3D('',#33886,#23928,#23929);
#22186=AXIS2_PLACEMENT_3D('',#33934,#23931,#23932);
#22187=AXIS2_PLACEMENT_3D('',#33988,#23934,#23935);
#22188=AXIS2_PLACEMENT_3D('',#34036,#23937,#23938);
#22189=AXIS2_PLACEMENT_3D('',#34084,#23940,#23941);
#22190=AXIS2_PLACEMENT_3D('',#34138,#23943,#23944);
#22191=AXIS2_PLACEMENT_3D('',#34186,#23946,#23947);
#22192=AXIS2_PLACEMENT_3D('',#34234,#23949,#23950);
#22193=AXIS2_PLACEMENT_3D('',#34282,#23952,#23953);
#22194=AXIS2_PLACEMENT_3D('',#34336,#23955,#23956);
#22195=AXIS2_PLACEMENT_3D('',#34384,#23958,#23959);
#22196=AXIS2_PLACEMENT_3D('',#34432,#23961,#23962);
#22197=AXIS2_PLACEMENT_3D('',#34486,#23964,#23965);
#22198=AXIS2_PLACEMENT_3D('',#34534,#23967,#23968);
#22199=AXIS2_PLACEMENT_3D('',#34582,#23970,#23971);
#22200=AXIS2_PLACEMENT_3D('',#34630,#23973,#23974);
#22201=AXIS2_PLACEMENT_3D('',#34684,#23976,#23977);
#22202=AXIS2_PLACEMENT_3D('',#34732,#23979,#23980);
#22203=AXIS2_PLACEMENT_3D('',#34780,#23982,#23983);
#22204=AXIS2_PLACEMENT_3D('',#34796,#23985,#23986);
#22205=AXIS2_PLACEMENT_3D('',#34805,#23987,#23988);
#22206=AXIS2_PLACEMENT_3D('',#34830,#23990,#23991);
#22207=AXIS2_PLACEMENT_3D('',#34854,#23993,#23994);
#22208=AXIS2_PLACEMENT_3D('',#34879,#23996,#23997);
#22209=AXIS2_PLACEMENT_3D('',#34904,#23999,#24000);
#22210=AXIS2_PLACEMENT_3D('',#34928,#24002,#24003);
#22211=AXIS2_PLACEMENT_3D('',#34952,#24005,#24006);
#22212=AXIS2_PLACEMENT_3D('',#34977,#24008,#24009);
#22213=AXIS2_PLACEMENT_3D('',#35002,#24011,#24012);
#22214=AXIS2_PLACEMENT_3D('',#35026,#24014,#24015);
#22215=AXIS2_PLACEMENT_3D('',#35051,#24017,#24018);
#22216=AXIS2_PLACEMENT_3D('',#35076,#24020,#24021);
#22217=AXIS2_PLACEMENT_3D('',#35100,#24023,#24024);
#22218=AXIS2_PLACEMENT_3D('',#35124,#24026,#24027);
#22219=AXIS2_PLACEMENT_3D('',#35149,#24029,#24030);
#22220=AXIS2_PLACEMENT_3D('',#35174,#24032,#24033);
#22221=AXIS2_PLACEMENT_3D('',#35198,#24035,#24036);
#22222=AXIS2_PLACEMENT_3D('',#35223,#24038,#24039);
#22223=AXIS2_PLACEMENT_3D('',#35248,#24041,#24042);
#22224=AXIS2_PLACEMENT_3D('',#35272,#24044,#24045);
#22225=AXIS2_PLACEMENT_3D('',#35297,#24047,#24048);
#22226=AXIS2_PLACEMENT_3D('',#35322,#24050,#24051);
#22227=AXIS2_PLACEMENT_3D('',#35346,#24053,#24054);
#22228=AXIS2_PLACEMENT_3D('',#35370,#24056,#24057);
#22229=AXIS2_PLACEMENT_3D('',#35673,#24058,#24059);
#22230=AXIS2_PLACEMENT_3D('',#35707,#24061,#24062);
#22231=AXIS2_PLACEMENT_3D('',#36465,#24063,#24064);
#22232=AXIS2_PLACEMENT_3D('',#36476,#24065,#24066);
#22233=AXIS2_PLACEMENT_3D('',#37236,#24067,#24068);
#22234=AXIS2_PLACEMENT_3D('',#37237,#24069,#24070);
#22235=AXIS2_PLACEMENT_3D('',#37246,#24075,#24076);
#22236=AXIS2_PLACEMENT_3D('',#37252,#24080,#24081);
#22237=AXIS2_PLACEMENT_3D('',#37258,#24085,#24086);
#22238=AXIS2_PLACEMENT_3D('',#37264,#24090,#24091);
#22239=AXIS2_PLACEMENT_3D('',#37270,#24095,#24096);
#22240=AXIS2_PLACEMENT_3D('',#37273,#24099,#24100);
#22241=AXIS2_PLACEMENT_3D('',#37274,#24101,#24102);
#22242=AXIS2_PLACEMENT_3D('',#37276,#24103,#24104);
#22243=AXIS2_PLACEMENT_3D('',#37277,#24105,#24106);
#22244=AXIS2_PLACEMENT_3D('',#37280,#24108,#24109);
#22245=AXIS2_PLACEMENT_3D('',#37281,#24110,#24111);
#22246=AXIS2_PLACEMENT_3D('',#37282,#24112,#24113);
#23906=DIRECTION('axis',(0.,0.,1.));
#23907=DIRECTION('refdir',(1.,0.,0.));
#23908=DIRECTION('center_axis',(0.,0.,1.));
#23909=DIRECTION('ref_axis',(1.,0.,0.));
#23910=DIRECTION('',(0.,0.,-1.));
#23911=DIRECTION('center_axis',(0.,0.,-1.));
#23912=DIRECTION('ref_axis',(1.,0.,0.));
#23913=DIRECTION('center_axis',(0.,0.,1.));
#23914=DIRECTION('ref_axis',(1.,0.,0.));
#23915=DIRECTION('',(0.,0.,-1.));
#23916=DIRECTION('center_axis',(0.,0.,1.));
#23917=DIRECTION('ref_axis',(1.,0.,0.));
#23918=DIRECTION('',(0.,0.,-1.));
#23919=DIRECTION('center_axis',(0.,0.,1.));
#23920=DIRECTION('ref_axis',(1.,0.,0.));
#23921=DIRECTION('',(0.,0.,-1.));
#23922=DIRECTION('center_axis',(0.,0.,1.));
#23923=DIRECTION('ref_axis',(1.,0.,0.));
#23924=DIRECTION('',(0.,0.,-1.));
#23925=DIRECTION('center_axis',(0.,0.,1.));
#23926=DIRECTION('ref_axis',(1.,0.,0.));
#23927=DIRECTION('',(0.,0.,-1.));
#23928=DIRECTION('center_axis',(0.,0.,1.));
#23929=DIRECTION('ref_axis',(1.,0.,0.));
#23930=DIRECTION('',(0.,0.,-1.));
#23931=DIRECTION('center_axis',(0.,0.,1.));
#23932=DIRECTION('ref_axis',(1.,0.,0.));
#23933=DIRECTION('',(0.,0.,-1.));
#23934=DIRECTION('center_axis',(0.,0.,1.));
#23935=DIRECTION('ref_axis',(1.,0.,0.));
#23936=DIRECTION('',(0.,0.,-1.));
#23937=DIRECTION('center_axis',(0.,0.,1.));
#23938=DIRECTION('ref_axis',(1.,0.,0.));
#23939=DIRECTION('',(0.,0.,-1.));
#23940=DIRECTION('center_axis',(0.,0.,1.));
#23941=DIRECTION('ref_axis',(1.,0.,0.));
#23942=DIRECTION('',(0.,0.,-1.));
#23943=DIRECTION('center_axis',(0.,0.,1.));
#23944=DIRECTION('ref_axis',(1.,0.,0.));
#23945=DIRECTION('',(0.,0.,-1.));
#23946=DIRECTION('center_axis',(0.,0.,1.));
#23947=DIRECTION('ref_axis',(1.,0.,0.));
#23948=DIRECTION('',(0.,0.,-1.));
#23949=DIRECTION('center_axis',(0.,0.,1.));
#23950=DIRECTION('ref_axis',(1.,0.,0.));
#23951=DIRECTION('',(0.,0.,-1.));
#23952=DIRECTION('center_axis',(0.,0.,1.));
#23953=DIRECTION('ref_axis',(1.,0.,0.));
#23954=DIRECTION('',(0.,0.,-1.));
#23955=DIRECTION('center_axis',(0.,0.,1.));
#23956=DIRECTION('ref_axis',(1.,0.,0.));
#23957=DIRECTION('',(0.,0.,-1.));
#23958=DIRECTION('center_axis',(0.,0.,1.));
#23959=DIRECTION('ref_axis',(1.,0.,0.));
#23960=DIRECTION('',(0.,0.,-1.));
#23961=DIRECTION('center_axis',(0.,0.,1.));
#23962=DIRECTION('ref_axis',(1.,0.,0.));
#23963=DIRECTION('',(0.,0.,-1.));
#23964=DIRECTION('center_axis',(0.,0.,1.));
#23965=DIRECTION('ref_axis',(1.,0.,0.));
#23966=DIRECTION('',(0.,0.,-1.));
#23967=DIRECTION('center_axis',(0.,0.,1.));
#23968=DIRECTION('ref_axis',(1.,0.,0.));
#23969=DIRECTION('',(0.,0.,-1.));
#23970=DIRECTION('center_axis',(0.,0.,1.));
#23971=DIRECTION('ref_axis',(1.,0.,0.));
#23972=DIRECTION('',(0.,0.,-1.));
#23973=DIRECTION('center_axis',(0.,0.,1.));
#23974=DIRECTION('ref_axis',(1.,0.,0.));
#23975=DIRECTION('',(0.,0.,-1.));
#23976=DIRECTION('center_axis',(0.,0.,1.));
#23977=DIRECTION('ref_axis',(1.,0.,0.));
#23978=DIRECTION('',(0.,0.,-1.));
#23979=DIRECTION('center_axis',(0.,0.,1.));
#23980=DIRECTION('ref_axis',(1.,0.,0.));
#23981=DIRECTION('',(0.,0.,-1.));
#23982=DIRECTION('center_axis',(0.,0.,1.));
#23983=DIRECTION('ref_axis',(0.997333825498281,-0.0729742455731076,0.));
#23984=DIRECTION('',(0.,0.,1.));
#23985=DIRECTION('center_axis',(0.,0.,-1.));
#23986=DIRECTION('ref_axis',(1.,-6.20171864138877E-14,0.));
#23987=DIRECTION('center_axis',(0.,0.,1.));
#23988=DIRECTION('ref_axis',(1.,-6.20171864138877E-14,0.));
#23989=DIRECTION('',(0.,0.,1.));
#23990=DIRECTION('center_axis',(0.,0.,1.));
#23991=DIRECTION('ref_axis',(1.,-6.20171864138877E-14,0.));
#23992=DIRECTION('',(0.,0.,1.));
#23993=DIRECTION('center_axis',(0.,0.,1.));
#23994=DIRECTION('ref_axis',(1.,-6.20171864138877E-14,0.));
#23995=DIRECTION('',(0.,0.,1.));
#23996=DIRECTION('center_axis',(0.,0.,1.));
#23997=DIRECTION('ref_axis',(1.,-6.20171864138877E-14,0.));
#23998=DIRECTION('',(0.,0.,1.));
#23999=DIRECTION('center_axis',(0.,0.,1.));
#24000=DIRECTION('ref_axis',(1.,-6.20171864138877E-14,0.));
#24001=DIRECTION('',(0.,0.,1.));
#24002=DIRECTION('center_axis',(0.,0.,1.));
#24003=DIRECTION('ref_axis',(1.,-6.20171864138877E-14,0.));
#24004=DIRECTION('',(0.,0.,1.));
#24005=DIRECTION('center_axis',(0.,0.,1.));
#24006=DIRECTION('ref_axis',(1.,-6.20171864138877E-14,0.));
#24007=DIRECTION('',(0.,0.,1.));
#24008=DIRECTION('center_axis',(0.,0.,1.));
#24009=DIRECTION('ref_axis',(1.,-6.20171864138877E-14,0.));
#24010=DIRECTION('',(0.,0.,1.));
#24011=DIRECTION('center_axis',(0.,0.,1.));
#24012=DIRECTION('ref_axis',(1.,-6.20171864138877E-14,0.));
#24013=DIRECTION('',(0.,0.,1.));
#24014=DIRECTION('center_axis',(0.,0.,1.));
#24015=DIRECTION('ref_axis',(1.,-6.20171864138877E-14,0.));
#24016=DIRECTION('',(0.,0.,1.));
#24017=DIRECTION('center_axis',(0.,0.,1.));
#24018=DIRECTION('ref_axis',(1.,-6.20171864138877E-14,0.));
#24019=DIRECTION('',(0.,0.,1.));
#24020=DIRECTION('center_axis',(0.,0.,1.));
#24021=DIRECTION('ref_axis',(1.,-6.20171864138877E-14,0.));
#24022=DIRECTION('',(0.,0.,1.));
#24023=DIRECTION('center_axis',(0.,0.,1.));
#24024=DIRECTION('ref_axis',(1.,-6.20171864138877E-14,0.));
#24025=DIRECTION('',(0.,0.,1.));
#24026=DIRECTION('center_axis',(0.,0.,1.));
#24027=DIRECTION('ref_axis',(1.,-6.20171864138877E-14,0.));
#24028=DIRECTION('',(0.,0.,1.));
#24029=DIRECTION('center_axis',(0.,0.,1.));
#24030=DIRECTION('ref_axis',(1.,-6.20171864138877E-14,0.));
#24031=DIRECTION('',(0.,0.,1.));
#24032=DIRECTION('center_axis',(0.,0.,1.));
#24033=DIRECTION('ref_axis',(1.,-6.20171864138877E-14,0.));
#24034=DIRECTION('',(0.,0.,1.));
#24035=DIRECTION('center_axis',(0.,0.,1.));
#24036=DIRECTION('ref_axis',(1.,-6.20171864138877E-14,0.));
#24037=DIRECTION('',(0.,0.,1.));
#24038=DIRECTION('center_axis',(0.,0.,1.));
#24039=DIRECTION('ref_axis',(1.,-6.20171864138877E-14,0.));
#24040=DIRECTION('',(0.,0.,1.));
#24041=DIRECTION('center_axis',(0.,0.,1.));
#24042=DIRECTION('ref_axis',(1.,-6.20171864138877E-14,0.));
#24043=DIRECTION('',(0.,0.,1.));
#24044=DIRECTION('center_axis',(0.,0.,1.));
#24045=DIRECTION('ref_axis',(1.,-6.20171864138877E-14,0.));
#24046=DIRECTION('',(0.,0.,1.));
#24047=DIRECTION('center_axis',(0.,0.,1.));
#24048=DIRECTION('ref_axis',(1.,-6.20171864138877E-14,0.));
#24049=DIRECTION('',(0.,0.,1.));
#24050=DIRECTION('center_axis',(0.,0.,1.));
#24051=DIRECTION('ref_axis',(1.,-6.20171864138877E-14,0.));
#24052=DIRECTION('',(0.,0.,1.));
#24053=DIRECTION('center_axis',(0.,0.,1.));
#24054=DIRECTION('ref_axis',(1.,-6.20171864138877E-14,0.));
#24055=DIRECTION('',(0.,0.,1.));
#24056=DIRECTION('center_axis',(0.,0.,-1.));
#24057=DIRECTION('ref_axis',(1.,0.,0.));
#24058=DIRECTION('center_axis',(0.,0.,-1.));
#24059=DIRECTION('ref_axis',(1.,0.,0.));
#24060=DIRECTION('',(0.707106781186547,8.65956056235493E-17,0.707106781186548));
#24061=DIRECTION('center_axis',(0.,0.,1.));
#24062=DIRECTION('ref_axis',(1.,0.,0.));
#24063=DIRECTION('center_axis',(0.,0.,1.));
#24064=DIRECTION('ref_axis',(1.,-6.20171864138877E-14,0.));
#24065=DIRECTION('center_axis',(0.,0.,-1.));
#24066=DIRECTION('ref_axis',(1.,-6.20171864138877E-14,0.));
#24067=DIRECTION('center_axis',(0.,0.,1.));
#24068=DIRECTION('ref_axis',(1.,0.,0.));
#24069=DIRECTION('center_axis',(-1.60246890531964E-16,-1.,0.));
#24070=DIRECTION('ref_axis',(1.,-1.60246890531964E-16,0.));
#24071=DIRECTION('',(1.,-1.60246890531964E-16,0.));
#24072=DIRECTION('',(0.,0.,1.));
#24073=DIRECTION('',(1.,-1.60246890531964E-16,0.));
#24074=DIRECTION('',(0.,0.,1.));
#24075=DIRECTION('center_axis',(-0.866025403784439,-0.5,0.));
#24076=DIRECTION('ref_axis',(0.5,-0.866025403784439,0.));
#24077=DIRECTION('',(0.5,-0.866025403784439,0.));
#24078=DIRECTION('',(0.,0.,1.));
#24079=DIRECTION('',(0.5,-0.866025403784439,0.));
#24080=DIRECTION('center_axis',(-0.866025403784439,0.5,0.));
#24081=DIRECTION('ref_axis',(-0.5,-0.866025403784439,0.));
#24082=DIRECTION('',(-0.5,-0.866025403784439,0.));
#24083=DIRECTION('',(0.,0.,1.));
#24084=DIRECTION('',(-0.5,-0.866025403784439,0.));
#24085=DIRECTION('center_axis',(1.60246890531964E-16,1.,0.));
#24086=DIRECTION('ref_axis',(-1.,1.60246890531964E-16,0.));
#24087=DIRECTION('',(-1.,1.60246890531964E-16,0.));
#24088=DIRECTION('',(0.,0.,1.));
#24089=DIRECTION('',(-1.,1.60246890531964E-16,0.));
#24090=DIRECTION('center_axis',(0.866025403784439,0.5,0.));
#24091=DIRECTION('ref_axis',(-0.5,0.866025403784439,0.));
#24092=DIRECTION('',(-0.5,0.866025403784439,0.));
#24093=DIRECTION('',(0.,0.,1.));
#24094=DIRECTION('',(-0.5,0.866025403784439,0.));
#24095=DIRECTION('center_axis',(0.866025403784439,-0.5,0.));
#24096=DIRECTION('ref_axis',(0.5,0.866025403784439,0.));
#24097=DIRECTION('',(0.5,0.866025403784439,0.));
#24098=DIRECTION('',(0.5,0.866025403784439,0.));
#24099=DIRECTION('center_axis',(0.,0.,1.));
#24100=DIRECTION('ref_axis',(1.,0.,0.));
#24101=DIRECTION('center_axis',(0.,0.,1.));
#24102=DIRECTION('ref_axis',(1.,0.,0.));
#24103=DIRECTION('center_axis',(0.,0.,1.));
#24104=DIRECTION('ref_axis',(1.,0.,0.));
#24105=DIRECTION('center_axis',(0.,0.,1.));
#24106=DIRECTION('ref_axis',(1.,0.,0.));
#24107=DIRECTION('',(0.,0.,-1.));
#24108=DIRECTION('center_axis',(0.,0.,1.));
#24109=DIRECTION('ref_axis',(1.,0.,0.));
#24110=DIRECTION('center_axis',(0.,0.,1.));
#24111=DIRECTION('ref_axis',(1.,0.,0.));
#24112=DIRECTION('center_axis',(0.,0.,1.));
#24113=DIRECTION('ref_axis',(1.,0.,0.));
#33615=CARTESIAN_POINT('',(0.,0.,0.));
#33616=CARTESIAN_POINT('Origin',(0.,0.,0.));
#33617=CARTESIAN_POINT('',(-3.94684541635378,0.00250618816942501,0.322176117089595));
#33618=CARTESIAN_POINT('',(-3.94571229786942,0.00420644411048898,0.1778238829104));
#33619=CARTESIAN_POINT('',(-3.942,-4.82755768223887E-16,0.));
#33620=CARTESIAN_POINT('',(1.7270326134187,3.54354657824448,0.));
#33621=CARTESIAN_POINT('Ctrl Pts',(-3.94684541635378,0.00250618816942501,
0.322176117089595));
#33622=CARTESIAN_POINT('Ctrl Pts',(-3.94773112778461,0.132835587750837,
0.316895328369763));
#33623=CARTESIAN_POINT('Ctrl Pts',(-3.94183789351545,0.26307859818693,0.311614539649932));
#33624=CARTESIAN_POINT('Ctrl Pts',(-3.92890301514817,0.39261184999977,0.3063337509301));
#33625=CARTESIAN_POINT('Ctrl Pts',(-3.79917189807037,1.69177315474756,0.253369772435476));
#33626=CARTESIAN_POINT('Ctrl Pts',(-2.96110743411295,2.91953839146377,0.200405793940852));
#33627=CARTESIAN_POINT('Ctrl Pts',(-1.79852789548214,3.51470668248002,0.147441815446229));
#33628=CARTESIAN_POINT('Ctrl Pts',(-0.719726524887938,4.06698577113378,
0.098294543630819));
#33629=CARTESIAN_POINT('Ctrl Pts',(0.638504507243322,4.07455564834572,0.0491472718154096));
#33630=CARTESIAN_POINT('Ctrl Pts',(1.73118107496479,3.54876586530513,-4.77048955893622E-17));
#33631=CARTESIAN_POINT('',(-1.72703261341866,3.5435465782445,0.));
#33632=CARTESIAN_POINT('Origin',(0.,0.,0.));
#33633=CARTESIAN_POINT('Ctrl Pts',(-1.72703261341866,3.5435465782445,-1.38777878078145E-15));
#33634=CARTESIAN_POINT('Ctrl Pts',(-2.90680413394004,2.96855656546122,0.0529882887282479));
#33635=CARTESIAN_POINT('Ctrl Pts',(-3.76655616656995,1.76297958901422,0.105976577456497));
#33636=CARTESIAN_POINT('Ctrl Pts',(-3.92036033233788,0.467860933696955,
0.158964866184747));
#33637=CARTESIAN_POINT('Ctrl Pts',(-3.93860710223307,0.314212741058287,
0.165251205093298));
#33638=CARTESIAN_POINT('Ctrl Pts',(-3.94691794439651,0.159304285881835,
0.171537544001849));
#33639=CARTESIAN_POINT('Ctrl Pts',(-3.94571229786942,0.00420644411048898,
0.1778238829104));
#33640=CARTESIAN_POINT('Origin',(0.,0.,0.));
#33641=CARTESIAN_POINT('',(-3.93670753965503,0.00216852164164449,1.32217611708959));
#33642=CARTESIAN_POINT('',(-3.93636006504333,0.00190811380198534,1.1778238829104));
#33643=CARTESIAN_POINT('',(-3.942,-4.82755768223887E-16,0.));
#33644=CARTESIAN_POINT('Ctrl Pts',(-3.93670753965503,0.00216852164164449,
1.32217611708959));
#33645=CARTESIAN_POINT('Ctrl Pts',(-3.93928378279248,0.519701728735777,
1.30134586600417));
#33646=CARTESIAN_POINT('Ctrl Pts',(-3.8445230015698,1.03632804611489,1.28051561491875));
#33647=CARTESIAN_POINT('Ctrl Pts',(-3.6480161981814,1.51081450660005,1.25968536383333));
#33648=CARTESIAN_POINT('Ctrl Pts',(-3.14836873517057,2.71726615166507,1.2067213853387));
#33649=CARTESIAN_POINT('Ctrl Pts',(-1.9909276922364,3.6512813246822,1.15375740684408));
#33650=CARTESIAN_POINT('Ctrl Pts',(-0.706151782787128,3.88482400643261,
1.10079342834945));
#33651=CARTESIAN_POINT('Ctrl Pts',(0.57862412666215,4.11836668818302,1.04782944985483));
#33652=CARTESIAN_POINT('Ctrl Pts',(1.99073490262654,3.65143687866671,0.994865471360208));
#33653=CARTESIAN_POINT('Ctrl Pts',(2.88298828242626,2.69797395029701,0.941901492865584));
#33654=CARTESIAN_POINT('Ctrl Pts',(3.77524166222597,1.74451102192732,0.88893751437096));
#33655=CARTESIAN_POINT('Ctrl Pts',(4.14763764586101,0.304514974704242,0.835973535876336));
#33656=CARTESIAN_POINT('Ctrl Pts',(3.82952478082154,-0.96194142997557,0.783009557381713));
#33657=CARTESIAN_POINT('Ctrl Pts',(3.51141191578207,-2.22839783465538,0.730045578887089));
#33658=CARTESIAN_POINT('Ctrl Pts',(2.50279020206811,-3.32131459679193,0.677081600392466));
#33659=CARTESIAN_POINT('Ctrl Pts',(1.26587965171505,-3.74001178475658,0.624117621897842));
#33660=CARTESIAN_POINT('Ctrl Pts',(0.0289691013620001,-4.15870897272123,
0.571153643403219));
#33661=CARTESIAN_POINT('Ctrl Pts',(-1.43623028563014,-3.90318658651399,
0.518189664908595));
#33662=CARTESIAN_POINT('Ctrl Pts',(-2.45813109402713,-3.09014670702069,
0.465225686413971));
#33663=CARTESIAN_POINT('Ctrl Pts',(-3.37814298820071,-2.35817120272038,
0.417542496639179));
#33664=CARTESIAN_POINT('Ctrl Pts',(-3.9388478333255,-1.17431072748125,0.369859306864387));
#33665=CARTESIAN_POINT('Ctrl Pts',(-3.94684541635378,0.00250618816942501,
0.322176117089595));
#33666=CARTESIAN_POINT('Ctrl Pts',(-3.94571229786942,0.00420644411048898,
0.1778238829104));
#33667=CARTESIAN_POINT('Ctrl Pts',(-3.93675540826681,-1.14803363217555,
0.224525832730098));
#33668=CARTESIAN_POINT('Ctrl Pts',(-3.40256651647006,-2.31072629277711,
0.271227782549796));
#33669=CARTESIAN_POINT('Ctrl Pts',(-2.51512664140724,-3.04478428612434,
0.317929732369494));
#33670=CARTESIAN_POINT('Ctrl Pts',(-1.50823248580272,-3.87765051644084,
0.370918021097743));
#33671=CARTESIAN_POINT('Ctrl Pts',(-0.0465878756876988,-4.1587226428863,
0.423906309825993));
#33672=CARTESIAN_POINT('Ctrl Pts',(1.1983574972874,-3.76190237425103,0.476894598554242));
#33673=CARTESIAN_POINT('Ctrl Pts',(2.44330287026249,-3.36508210561577,0.529882887282491));
#33674=CARTESIAN_POINT('Ctrl Pts',(3.47154900609766,-2.29036944189979,0.58287117601074));
#33675=CARTESIAN_POINT('Ctrl Pts',(3.81196419489399,-1.02929753659268,0.635859464738989));
#33676=CARTESIAN_POINT('Ctrl Pts',(4.15237938369031,0.231774368714438,0.688847753467239));
#33677=CARTESIAN_POINT('Ctrl Pts',(3.80496362544778,1.67920551561269,0.741836042195488));
#33678=CARTESIAN_POINT('Ctrl Pts',(2.92880392464218,2.64832610367255,0.794824330923737));
#33679=CARTESIAN_POINT('Ctrl Pts',(2.05264422383658,3.61744669173242,0.847812619651987));
#33680=CARTESIAN_POINT('Ctrl Pts',(0.647740580467906,4.1082567209539,0.900800908380236));
#33681=CARTESIAN_POINT('Ctrl Pts',(-0.641345987445116,3.89601342814375,
0.953789197108486));
#33682=CARTESIAN_POINT('Ctrl Pts',(-1.93043255535814,3.68377013533359,1.00677748583673));
#33683=CARTESIAN_POINT('Ctrl Pts',(-3.10370204781551,2.7684735204918,1.05976577456498));
#33684=CARTESIAN_POINT('Ctrl Pts',(-3.6230578333699,1.56976054866973,1.11275406329323));
#33685=CARTESIAN_POINT('Ctrl Pts',(-3.83564812513838,1.0790858560709,1.13444400316562));
#33686=CARTESIAN_POINT('Ctrl Pts',(-3.9386720278785,0.540923388712033,1.15613394303801));
#33687=CARTESIAN_POINT('Ctrl Pts',(-3.93636006504333,0.00190811380198534,
1.1778238829104));
#33688=CARTESIAN_POINT('Origin',(0.,0.,0.));
#33689=CARTESIAN_POINT('',(-3.93898402517327,-0.0032694952000395,2.32217611708959));
#33690=CARTESIAN_POINT('',(-3.93943713807335,-0.00339197931643889,2.1778238829104));
#33691=CARTESIAN_POINT('',(-3.942,-4.82755768223887E-16,0.));
#33692=CARTESIAN_POINT('Ctrl Pts',(-3.93898402517327,-0.0032694952000395,
2.32217611708959));
#33693=CARTESIAN_POINT('Ctrl Pts',(-3.93192709039827,0.89928000152811,2.28579640363858));
#33694=CARTESIAN_POINT('Ctrl Pts',(-3.6239186993101,1.80618191912708,2.24941669018756));
#33695=CARTESIAN_POINT('Ctrl Pts',(-3.05593295732034,2.50036976841156,2.21303697673655));
#33696=CARTESIAN_POINT('Ctrl Pts',(-2.22902197396405,3.51101407626844,2.16007299824193));
#33697=CARTESIAN_POINT('Ctrl Pts',(-0.851077281590667,4.07080133208995,
2.1071090197473));
#33698=CARTESIAN_POINT('Ctrl Pts',(0.446378324979883,3.92317725380663,2.05414504125268));
#33699=CARTESIAN_POINT('Ctrl Pts',(1.74383393155043,3.77555317552331,2.00118106275806));
#33700=CARTESIAN_POINT('Ctrl Pts',(2.96080045231815,2.92051776313515,1.94821708426343));
#33701=CARTESIAN_POINT('Ctrl Pts',(3.53953231896037,1.74993928366879,1.89525310576881));
#33702=CARTESIAN_POINT('Ctrl Pts',(4.11826418560259,0.57936080420243,1.84228912727419));
#33703=CARTESIAN_POINT('Ctrl Pts',(4.05876139811932,-0.906760742342139,
1.78932514877956));
#33704=CARTESIAN_POINT('Ctrl Pts',(3.38829497669137,-2.0273218478537,1.73636117028494));
#33705=CARTESIAN_POINT('Ctrl Pts',(2.71782855526341,-3.14788295336526,1.68339719179031));
#33706=CARTESIAN_POINT('Ctrl Pts',(1.43639849989078,-3.90288361784382,1.63043321329569));
#33707=CARTESIAN_POINT('Ctrl Pts',(0.131293493556904,-3.9463054651445,1.57746923480107));
#33708=CARTESIAN_POINT('Ctrl Pts',(-1.17381151277698,-3.98972731244518,
1.52450525630644));
#33709=CARTESIAN_POINT('Ctrl Pts',(-2.50259147007212,-3.32157034256797,
1.47154127781182));
#33710=CARTESIAN_POINT('Ctrl Pts',(-3.24605450717593,-2.24804779907291,
1.4185772993172));
#33711=CARTESIAN_POINT('Ctrl Pts',(-3.69712029286904,-1.59673190927805,
1.386443571908));
#33712=CARTESIAN_POINT('Ctrl Pts',(-3.93273330552895,-0.796202603784206,
1.3543098444988));
#33713=CARTESIAN_POINT('Ctrl Pts',(-3.93670753965503,0.00216852164164449,
1.32217611708959));
#33714=CARTESIAN_POINT('Ctrl Pts',(-3.93636006504333,0.00190811380198534,
1.1778238829104));
#33715=CARTESIAN_POINT('Ctrl Pts',(-3.93302392765509,-0.775885103331329,
1.20912223176626));
#33716=CARTESIAN_POINT('Ctrl Pts',(-3.71035557449182,-1.55545405153981,
1.24042058062212));
#33717=CARTESIAN_POINT('Ctrl Pts',(-3.28106611164764,-2.19667847798475,
1.27171892947798));
#33718=CARTESIAN_POINT('Ctrl Pts',(-2.5542765257196,-3.28227520401484,1.32470721820623));
#33719=CARTESIAN_POINT('Ctrl Pts',(-1.23525527521213,-3.97133932727269,
1.37769550693448));
#33720=CARTESIAN_POINT('Ctrl Pts',(0.0709513775297463,-3.94785759961686,
1.43068379566273));
#33721=CARTESIAN_POINT('Ctrl Pts',(1.37715803027162,-3.92437587196102,1.48367208439098));
#33722=CARTESIAN_POINT('Ctrl Pts',(2.67055008524789,-3.1883482933915,1.53666037311923));
#33723=CARTESIAN_POINT('Ctrl Pts',(3.3578681272901,-2.07735647460328,1.58964866184748));
#33724=CARTESIAN_POINT('Ctrl Pts',(4.0451861693323,-0.966364655815065,1.64263695057573));
#33725=CARTESIAN_POINT('Ctrl Pts',(4.12643019844044,0.519591403191845,1.69562523930397));
#33726=CARTESIAN_POINT('Ctrl Pts',(3.56432857554823,1.69889860460012,1.74861352803222));
#33727=CARTESIAN_POINT('Ctrl Pts',(3.00222695265603,2.87820580600839,1.80160181676047));
#33728=CARTESIAN_POINT('Ctrl Pts',(1.7967796777635,3.75086414981802,1.85459010548872));
#33729=CARTESIAN_POINT('Ctrl Pts',(0.500920035194316,3.91659925522552,1.90757839421697));
#33730=CARTESIAN_POINT('Ctrl Pts',(-0.794939607374858,4.08233436063301,
1.96056668294522));
#33731=CARTESIAN_POINT('Ctrl Pts',(-2.18121161762068,3.54114622763838,2.01355497167347));
#33732=CARTESIAN_POINT('Ctrl Pts',(-3.02202408579975,2.54126994215436,2.06654326040172));
#33733=CARTESIAN_POINT('Ctrl Pts',(-3.61062040344951,1.84132373296486,2.10363680123794));
#33734=CARTESIAN_POINT('Ctrl Pts',(-3.93191648715648,0.916599256990189,
2.14073034207417));
#33735=CARTESIAN_POINT('Ctrl Pts',(-3.93943713807335,-0.00339197931643889,
2.1778238829104));
#33736=CARTESIAN_POINT('Origin',(0.,0.,0.));
#33737=CARTESIAN_POINT('',(-3.94841909008794,-0.000476659622032916,3.3221761170896));
#33738=CARTESIAN_POINT('',(-3.94848727448062,-0.000227313299713517,3.1778238829104));
#33739=CARTESIAN_POINT('',(-3.942,-4.82755768223887E-16,0.));
#33740=CARTESIAN_POINT('Ctrl Pts',(-3.94841909008794,-0.000476659622032916,
3.3221761170896));
#33741=CARTESIAN_POINT('Ctrl Pts',(-3.94623626626659,1.27989932784314,3.27024694127299));
#33742=CARTESIAN_POINT('Ctrl Pts',(-3.2656648832367,2.56226681984272,3.21831776545638));
#33743=CARTESIAN_POINT('Ctrl Pts',(-2.20319423243154,3.27666141545475,3.16638858963978));
#33744=CARTESIAN_POINT('Ctrl Pts',(-1.11955152454134,4.00529188962783,3.11342461114515));
#33745=CARTESIAN_POINT('Ctrl Pts',(0.361362461026873,4.14308771897741,3.06046063265053));
#33746=CARTESIAN_POINT('Ctrl Pts',(1.56083317716561,3.62689600200629,3.00749665415591));
#33747=CARTESIAN_POINT('Ctrl Pts',(2.76030389330435,3.11070428503517,2.95453267566128));
#33748=CARTESIAN_POINT('Ctrl Pts',(3.67833134001362,1.94052502174336,2.90156869716666));
#33749=CARTESIAN_POINT('Ctrl Pts',(3.89417629964206,0.652660565018754,2.84860471867204));
#33750=CARTESIAN_POINT('Ctrl Pts',(4.11002125927051,-0.635203891705856,
2.79564074017741));
#33751=CARTESIAN_POINT('Ctrl Pts',(3.62368373181814,-2.04075354186327,2.74267676168279));
#33752=CARTESIAN_POINT('Ctrl Pts',(2.65805604729365,-2.91981385750971,2.68971278318817));
#33753=CARTESIAN_POINT('Ctrl Pts',(1.69242836276915,-3.79887417315615,2.63674880469354));
#33754=CARTESIAN_POINT('Ctrl Pts',(0.247510521172539,-4.15144515429161,
2.58378482619892));
#33755=CARTESIAN_POINT('Ctrl Pts',(-1.01448026111426,-3.8159408321598,2.53082084770429));
#33756=CARTESIAN_POINT('Ctrl Pts',(-2.27647104340105,-3.48043651002799,
2.47785686920967));
#33757=CARTESIAN_POINT('Ctrl Pts',(-3.35553476637803,-2.45685688462891,
2.42489289071505));
#33758=CARTESIAN_POINT('Ctrl Pts',(-3.75712799069693,-1.21431639198325,
2.37192891222042));
#33759=CARTESIAN_POINT('Ctrl Pts',(-3.88287625699264,-0.825247793982355,
2.35534464717681));
#33760=CARTESIAN_POINT('Ctrl Pts',(-3.94220103997636,-0.414710890659917,
2.3387603821332));
#33761=CARTESIAN_POINT('Ctrl Pts',(-3.93898402517327,-0.0032694952000395,
2.32217611708959));
#33762=CARTESIAN_POINT('Ctrl Pts',(-3.93943713807335,-0.00339197931643889,
2.1778238829104));
#33763=CARTESIAN_POINT('Ctrl Pts',(-3.9426597705752,-0.397612332356497,
2.19371863080242));
#33764=CARTESIAN_POINT('Ctrl Pts',(-3.8882681890457,-0.790963586497156,
2.20961337869445));
#33765=CARTESIAN_POINT('Ctrl Pts',(-3.77260571048107,-1.16538770550329,
2.22550812658647));
#33766=CARTESIAN_POINT('Ctrl Pts',(-3.387021940871,-2.41360462970351,2.27849641531472));
#33767=CARTESIAN_POINT('Ctrl Pts',(-2.32050147553854,-3.45147404013054,
2.33148470404296));
#33768=CARTESIAN_POINT('Ctrl Pts',(-1.06225033291184,-3.80293352608456,
2.38447299277121));
#33769=CARTESIAN_POINT('Ctrl Pts',(0.19600080971487,-4.15439301203859,2.43746128149946));
#33770=CARTESIAN_POINT('Ctrl Pts',(1.64598262963581,-3.81944257351961,2.49044957022771));
#33771=CARTESIAN_POINT('Ctrl Pts',(2.62259865984893,-2.95172107137353,2.54343785895596));
#33772=CARTESIAN_POINT('Ctrl Pts',(3.59921469006204,-2.08399956922746,2.59642614768421));
#33773=CARTESIAN_POINT('Ctrl Pts',(4.10246493056733,-0.683507003454308,
2.64941443641246));
#33774=CARTESIAN_POINT('Ctrl Pts',(3.90151184350976,0.607360005829592,2.70240272514071));
#33775=CARTESIAN_POINT('Ctrl Pts',(3.70055875645219,1.89822701511349,2.75539101386896));
#33776=CARTESIAN_POINT('Ctrl Pts',(2.79540234183177,3.07946846790813,2.80837930259721));
#33777=CARTESIAN_POINT('Ctrl Pts',(1.60123168012205,3.60925720078016,2.86136759132546));
#33778=CARTESIAN_POINT('Ctrl Pts',(0.407061018412325,4.1390459336522,2.91435588005371));
#33779=CARTESIAN_POINT('Ctrl Pts',(-1.0761238903867,4.01738194660163,2.96734416878196));
#33780=CARTESIAN_POINT('Ctrl Pts',(-2.16799636339283,3.30007158724765,3.0203324575102));
#33781=CARTESIAN_POINT('Ctrl Pts',(-3.24974830176843,2.58940995703755,3.07282959931027));
#33782=CARTESIAN_POINT('Ctrl Pts',(-3.94740831268547,1.29409283853931,3.12532674111033));
#33783=CARTESIAN_POINT('Ctrl Pts',(-3.94848727448062,-0.000227313299713517,
3.1778238829104));
#33784=CARTESIAN_POINT('Origin',(0.,0.,0.));
#33785=CARTESIAN_POINT('',(-3.94039517343639,0.00354505425716481,4.32217611708959));
#33786=CARTESIAN_POINT('',(-3.94011414712863,0.00351656949004968,4.1778238829104));
#33787=CARTESIAN_POINT('',(-3.942,-4.82755768223887E-16,0.));
#33788=CARTESIAN_POINT('Ctrl Pts',(-3.94039517343639,0.00354505425716481,
4.32217611708959));
#33789=CARTESIAN_POINT('Ctrl Pts',(-3.94353004938676,0.363314892612021,
4.30766145740202));
#33790=CARTESIAN_POINT('Ctrl Pts',(-3.89832073254977,0.722311104007169,
4.29314679771445));
#33791=CARTESIAN_POINT('Ctrl Pts',(-3.80162926767229,1.06685976451013,4.27863213802688));
#33792=CARTESIAN_POINT('Ctrl Pts',(-3.44880221029601,2.32411747761066,4.22566815953225));
#33793=CARTESIAN_POINT('Ctrl Pts',(-2.41048038450093,3.38900325344725,4.17270418103763));
#33794=CARTESIAN_POINT('Ctrl Pts',(-1.16253486527102,3.7734715492884,4.119740202543));
#33795=CARTESIAN_POINT('Ctrl Pts',(0.0854106539588831,4.15793984512954,
4.06677622404838));
#33796=CARTESIAN_POINT('Ctrl Pts',(1.54297986662362,3.86199066097525,4.01381224555376));
#33797=CARTESIAN_POINT('Ctrl Pts',(2.54215731665373,3.02125984033277,3.96084826705914));
#33798=CARTESIAN_POINT('Ctrl Pts',(3.54133476668386,2.18052901969028,3.90788428856451));
#33799=CARTESIAN_POINT('Ctrl Pts',(4.08212045407936,0.795016562559593,3.85492031006988));
#33800=CARTESIAN_POINT('Ctrl Pts',(3.91666803670668,-0.500286254334146,
3.80195633157526));
#33801=CARTESIAN_POINT('Ctrl Pts',(3.75121561933401,-1.79558907122787,3.74899235308063));
#33802=CARTESIAN_POINT('Ctrl Pts',(2.87952509719318,-3.00068224788464,3.69602837458601));
#33803=CARTESIAN_POINT('Ctrl Pts',(1.70109910586756,-3.56326208407903,3.64306439609139));
#33804=CARTESIAN_POINT('Ctrl Pts',(0.522673114541947,-4.12584192027342,
3.59010041759677));
#33805=CARTESIAN_POINT('Ctrl Pts',(-0.962488345968457,-4.04590841600543,
3.53713643910214));
#33806=CARTESIAN_POINT('Ctrl Pts',(-2.07372407526821,-3.36009572803379,
3.48417246060752));
#33807=CARTESIAN_POINT('Ctrl Pts',(-3.18495980456796,-2.67428304006214,
3.4312084821129));
#33808=CARTESIAN_POINT('Ctrl Pts',(-3.92226980265706,-1.38259116838684,
3.37824450361827));
#33809=CARTESIAN_POINT('Ctrl Pts',(-3.94773908659551,-0.0770126730508915,
3.32528052512365));
#33810=CARTESIAN_POINT('Ctrl Pts',(-3.94823670184224,-0.0515044661197667,
3.32424572244563));
#33811=CARTESIAN_POINT('Ctrl Pts',(-3.94846258763822,-0.025990958277152,
3.32321091976761));
#33812=CARTESIAN_POINT('Ctrl Pts',(-3.94841909008794,-0.000476659622032916,
3.3221761170896));
#33813=CARTESIAN_POINT('Ctrl Pts',(-3.94848727448062,-0.000227313299713517,
3.1778238829104));
#33814=CARTESIAN_POINT('Ctrl Pts',(-3.94849736891154,-0.0123365700109349,
3.17831502983858));
#33815=CARTESIAN_POINT('Ctrl Pts',(-3.94844649235883,-0.0244457394587464,
3.17880617676677));
#33816=CARTESIAN_POINT('Ctrl Pts',(-3.94833438892723,-0.0365543420562738,
3.17929732369495));
#33817=CARTESIAN_POINT('Ctrl Pts',(-3.9362399042423,-1.34291318034886,3.2322856124232));
#33818=CARTESIAN_POINT('Ctrl Pts',(-3.21149089765924,-2.64267412527665,
3.28527390115145));
#33819=CARTESIAN_POINT('Ctrl Pts',(-2.1065247612934,-3.33964579658387,3.3382621898797));
#33820=CARTESIAN_POINT('Ctrl Pts',(-1.00155862492758,-4.03661746789108,
3.39125047860795));
#33821=CARTESIAN_POINT('Ctrl Pts',(0.483624641221001,-4.13079986557773,
3.4442387673362));
#33822=CARTESIAN_POINT('Ctrl Pts',(1.66778169459976,-3.57899215935798,3.49722705606445));
#33823=CARTESIAN_POINT('Ctrl Pts',(2.85193874797851,-3.02718445313824,3.5502153447927));
#33824=CARTESIAN_POINT('Ctrl Pts',(3.73506958858744,-1.82938664301209,3.60320363352094));
#33825=CARTESIAN_POINT('Ctrl Pts',(3.91208817286041,-0.535020350876169,
3.65619192224919));
#33826=CARTESIAN_POINT('Ctrl Pts',(4.08910675713339,0.759345941259773,3.70918021097745));
#33827=CARTESIAN_POINT('Ctrl Pts',(3.56001308507038,2.1502807154055,3.7621684997057));
#33828=CARTESIAN_POINT('Ctrl Pts',(2.56749878545275,2.99977176280624,3.81515678843395));
#33829=CARTESIAN_POINT('Ctrl Pts',(1.57498448583515,3.84926281020697,3.86814507716219));
#33830=CARTESIAN_POINT('Ctrl Pts',(0.11904955866294,4.15731013086274,3.92113336589044));
#33831=CARTESIAN_POINT('Ctrl Pts',(-1.13247866152849,3.78261453618225,3.97412165461869));
#33832=CARTESIAN_POINT('Ctrl Pts',(-2.38400688171994,3.40791894150175,4.02710994334694));
#33833=CARTESIAN_POINT('Ctrl Pts',(-3.43112839493061,2.35048043148498,4.08009823207519));
#33834=CARTESIAN_POINT('Ctrl Pts',(-3.79353576624568,1.09533877709901,4.13308652080344));
#33835=CARTESIAN_POINT('Ctrl Pts',(-3.89552779876129,0.742105210239426,
4.14799897483909));
#33836=CARTESIAN_POINT('Ctrl Pts',(-3.94328881467064,0.373213076031263,
4.16291142887475));
#33837=CARTESIAN_POINT('Ctrl Pts',(-3.94011414712863,0.00351656949004968,
4.1778238829104));
#33838=CARTESIAN_POINT('Origin',(0.,0.,0.));
#33839=CARTESIAN_POINT('',(-3.93600110646763,-0.0014281919745418,5.32217611708959));
#33840=CARTESIAN_POINT('',(-3.93605515638862,-0.00152114337219748,5.1778238829104));
#33841=CARTESIAN_POINT('',(-3.942,-4.82755768223887E-16,0.));
#33842=CARTESIAN_POINT('Ctrl Pts',(-3.93600110646763,-0.0014281919745418,
5.32217611708959));
#33843=CARTESIAN_POINT('Ctrl Pts',(-3.93357236454694,0.74585693902175,5.29211199503643));
#33844=CARTESIAN_POINT('Ctrl Pts',(-3.72918845072319,1.49437332783476,5.26204787298327));
#33845=CARTESIAN_POINT('Ctrl Pts',(-3.33126090733014,2.11973479786067,5.2319837509301));
#33846=CARTESIAN_POINT('Ctrl Pts',(-2.63023175991589,3.22143440482896,5.17901977243548));
#33847=CARTESIAN_POINT('Ctrl Pts',(-1.32852280829314,3.94091180862283,5.12605579394085));
#33848=CARTESIAN_POINT('Ctrl Pts',(-0.0227175227337642,3.94842484544612,
5.07309181544622));
#33849=CARTESIAN_POINT('Ctrl Pts',(1.28308776282561,3.95593788226941,5.0201278369516));
#33850=CARTESIAN_POINT('Ctrl Pts',(2.59298938232161,3.25148655212212,4.96716385845699));
#33851=CARTESIAN_POINT('Ctrl Pts',(3.30664910123763,2.15792645084216,4.91419987996236));
#33852=CARTESIAN_POINT('Ctrl Pts',(4.02030882015365,1.06436634956219,4.86123590146774));
#33853=CARTESIAN_POINT('Ctrl Pts',(4.13772663848969,-0.418302522850447,
4.80827192297311));
#33854=CARTESIAN_POINT('Ctrl Pts',(3.60508904482309,-1.61056133843436,4.75530794447848));
#33855=CARTESIAN_POINT('Ctrl Pts',(3.07245145115649,-2.80282015401828,4.70234396598386));
#33856=CARTESIAN_POINT('Ctrl Pts',(1.88975844548724,-3.70466891277347,4.64937998748924));
#33857=CARTESIAN_POINT('Ctrl Pts',(0.599047552189011,-3.90278322178284,
4.59641600899462));
#33858=CARTESIAN_POINT('Ctrl Pts',(-0.691663341109217,-4.10089753079221,
4.54345203049999));
#33859=CARTESIAN_POINT('Ctrl Pts',(-2.09039212203642,-3.59527739005576,
4.49048805200536));
#33860=CARTESIAN_POINT('Ctrl Pts',(-2.95609036802126,-2.61765249450529,
4.43752407351074));
#33861=CARTESIAN_POINT('Ctrl Pts',(-3.58454594852404,-1.90794351207784,
4.39907475470369));
#33862=CARTESIAN_POINT('Ctrl Pts',(-3.93209089021995,-0.949484883048943,
4.36062543589664));
#33863=CARTESIAN_POINT('Ctrl Pts',(-3.94039517343639,0.00354505425716481,
4.32217611708959));
#33864=CARTESIAN_POINT('Ctrl Pts',(-3.94011414712863,0.00351656949004968,
4.1778238829104));
#33865=CARTESIAN_POINT('Ctrl Pts',(-3.93200829706235,-0.94042619377602,
4.215899717603));
#33866=CARTESIAN_POINT('Ctrl Pts',(-3.59183770381144,-1.88961289751958,
4.25397555229559));
#33867=CARTESIAN_POINT('Ctrl Pts',(-2.97445535308007,-2.59678570511794,
4.29205138698818));
#33868=CARTESIAN_POINT('Ctrl Pts',(-2.1152743391799,-3.5809237341938,4.34503967571643));
#33869=CARTESIAN_POINT('Ctrl Pts',(-0.719219081960083,-4.09635499359035,
4.39802796444469));
#33870=CARTESIAN_POINT('Ctrl Pts',(0.573349476162703,-3.90665471020838,
4.45101625317294));
#33871=CARTESIAN_POINT('Ctrl Pts',(1.86591803428548,-3.7169544268264,4.50400454190118));
#33872=CARTESIAN_POINT('Ctrl Pts',(3.05499989331122,-2.82212260066591,4.55699283062943));
#33873=CARTESIAN_POINT('Ctrl Pts',(3.59517138458731,-1.63261243464328,4.60998111935768));
#33874=CARTESIAN_POINT('Ctrl Pts',(4.13534287586339,-0.443102268620652,
4.66296940808593));
#33875=CARTESIAN_POINT('Ctrl Pts',(4.02660399938981,1.04108623726411,4.71595769681418));
#33876=CARTESIAN_POINT('Ctrl Pts',(3.31883252977577,2.13916602570979,4.76894598554243));
#33877=CARTESIAN_POINT('Ctrl Pts',(2.61106106016173,3.23724581415546,4.82193427427068));
#33878=CARTESIAN_POINT('Ctrl Pts',(1.3042569974072,3.94921688516205,4.87492256299893));
#33879=CARTESIAN_POINT('Ctrl Pts',(-0.00215762490102876,3.94850300633285,
4.92791085172718));
#33880=CARTESIAN_POINT('Ctrl Pts',(-1.30857224720925,3.94778912750366,4.98089914045543));
#33881=CARTESIAN_POINT('Ctrl Pts',(-2.61459742907118,3.23439029883869,5.03388742918367));
#33882=CARTESIAN_POINT('Ctrl Pts',(-3.32116840418697,2.13553765533301,5.08687571791192));
#33883=CARTESIAN_POINT('Ctrl Pts',(-3.72541706095167,1.50685388432656,5.11719177291141));
#33884=CARTESIAN_POINT('Ctrl Pts',(-3.93344647436031,0.751999581783958,
5.14750782791091));
#33885=CARTESIAN_POINT('Ctrl Pts',(-3.93605515638862,-0.00152114337219748,
5.1778238829104));
#33886=CARTESIAN_POINT('Origin',(0.,0.,0.));
#33887=CARTESIAN_POINT('',(-3.94563673384516,-0.00288256983268176,6.3221761170896));
#33888=CARTESIAN_POINT('',(-3.94570073178844,-0.00286656758253237,6.1778238829104));
#33889=CARTESIAN_POINT('',(-3.942,-4.82755768223887E-16,0.));
#33890=CARTESIAN_POINT('Ctrl Pts',(-3.94563673384516,-0.00288256983268176,
6.3221761170896));
#33891=CARTESIAN_POINT('Ctrl Pts',(-3.93638288024859,1.12386902299333,6.27656253267084));
#33892=CARTESIAN_POINT('Ctrl Pts',(-3.42887602753453,2.25790074792199,6.23094894825208));
#33893=CARTESIAN_POINT('Ctrl Pts',(-2.57675389815072,2.99180784716095,6.18533536383333));
#33894=CARTESIAN_POINT('Ctrl Pts',(-1.58731667872186,3.84398029351578,6.1323713853387));
#33895=CARTESIAN_POINT('Ctrl Pts',(-0.133249377743896,4.15668177021255,
6.07940740684408));
#33896=CARTESIAN_POINT('Ctrl Pts',(1.1190375023862,3.78659872632712,6.02644342834946));
#33897=CARTESIAN_POINT('Ctrl Pts',(2.37132438251632,3.41651568244167,5.97347944985483));
#33898=CARTESIAN_POINT('Ctrl Pts',(3.42183084179856,2.363648117974,5.92051547136021));
#33899=CARTESIAN_POINT('Ctrl Pts',(3.78910149173018,1.11053353453949,5.86755149286558));
#33900=CARTESIAN_POINT('Ctrl Pts',(4.15637214166179,-0.142581048895014,
5.81458751437096));
#33901=CARTESIAN_POINT('Ctrl Pts',(3.84040698224279,-1.59594265129635,5.76162353587634));
#33902=CARTESIAN_POINT('Ctrl Pts',(2.98601533590735,-2.58346419748652,5.70865955738171));
#33903=CARTESIAN_POINT('Ctrl Pts',(2.1316236895719,-3.57098574367668,5.65569557888709));
#33904=CARTESIAN_POINT('Ctrl Pts',(0.738805556320001,-4.09266723365567,
5.60273160039247));
#33905=CARTESIAN_POINT('Ctrl Pts',(-0.554099537676607,-3.9094179296049,
5.54976762189784));
#33906=CARTESIAN_POINT('Ctrl Pts',(-1.84700463167322,-3.72616862555414,
5.49680364340322));
#33907=CARTESIAN_POINT('Ctrl Pts',(-3.03999668641454,-2.83798852747363,
5.44383966490859));
#33908=CARTESIAN_POINT('Ctrl Pts',(-3.58631804218233,-1.65193757336201,
5.39087568641397));
#33909=CARTESIAN_POINT('Ctrl Pts',(-3.8225291610139,-1.1391287294386,5.36797582997251));
#33910=CARTESIAN_POINT('Ctrl Pts',(-3.93785108037402,-0.570635640986049,
5.34507597353105));
#33911=CARTESIAN_POINT('Ctrl Pts',(-3.93600110646763,-0.0014281919745418,
5.32217611708959));
#33912=CARTESIAN_POINT('Ctrl Pts',(-3.93605515638862,-0.00152114337219748,
5.1778238829104));
#33913=CARTESIAN_POINT('Ctrl Pts',(-3.93800609125369,-0.565050863861574,
5.20049611663916));
#33914=CARTESIAN_POINT('Ctrl Pts',(-3.82506562686086,-1.12783471721807,
5.22316835036792));
#33915=CARTESIAN_POINT('Ctrl Pts',(-3.59338498454405,-1.63654055836231,
5.24584058409668));
#33916=CARTESIAN_POINT('Ctrl Pts',(-3.05191382141567,-2.82545967020557,
5.29882887282492));
#33917=CARTESIAN_POINT('Ctrl Pts',(-1.86185472678928,-3.71899143554569,
5.35181716155317));
#33918=CARTESIAN_POINT('Ctrl Pts',(-0.569079620514193,-3.90727898054932,
5.40480545028142));
#33919=CARTESIAN_POINT('Ctrl Pts',(0.723695485760891,-4.09556652555295,
5.45779373900967));
#33920=CARTESIAN_POINT('Ctrl Pts',(2.11918660368467,-3.57860985022007,5.51078202773792));
#33921=CARTESIAN_POINT('Ctrl Pts',(2.97729155756073,-2.59353342519368,5.56377031646617));
#33922=CARTESIAN_POINT('Ctrl Pts',(3.83539651143679,-1.60845700016728,5.61675860519442));
#33923=CARTESIAN_POINT('Ctrl Pts',(4.15611530126515,-0.155260825447382,
5.66974689392266));
#33924=CARTESIAN_POINT('Ctrl Pts',(3.79233642449449,1.09948401069401,5.72273518265091));
#33925=CARTESIAN_POINT('Ctrl Pts',(3.42855754772383,2.35422884683541,5.77572347137916));
#33926=CARTESIAN_POINT('Ctrl Pts',(2.38028100435414,3.41052234439828,5.82871176010741));
#33927=CARTESIAN_POINT('Ctrl Pts',(1.12834403334923,3.78384994268096,5.88170004883566));
#33928=CARTESIAN_POINT('Ctrl Pts',(-0.12359293765566,4.15717754096363,5.93468833756392));
#33929=CARTESIAN_POINT('Ctrl Pts',(-1.57919033629578,3.8475392399661,5.98767662629216));
#33930=CARTESIAN_POINT('Ctrl Pts',(-2.57077564940419,2.99696399824068,6.04066491502041));
#33931=CARTESIAN_POINT('Ctrl Pts',(-3.4263409160258,2.26306584157345,6.08638457098374));
#33932=CARTESIAN_POINT('Ctrl Pts',(-3.93646396625886,1.126457364296,6.13210422694707));
#33933=CARTESIAN_POINT('Ctrl Pts',(-3.94570073178844,-0.00286656758253237,
6.1778238829104));
#33934=CARTESIAN_POINT('Origin',(0.,0.,0.));
#33935=CARTESIAN_POINT('',(-3.94505905468816,0.00309284708018512,7.32217611708959));
#33936=CARTESIAN_POINT('',(-3.94511280640764,0.00308469250234145,7.1778238829104));
#33937=CARTESIAN_POINT('',(-3.942,-4.82755768223887E-16,0.));
#33938=CARTESIAN_POINT('Ctrl Pts',(-3.94505905468816,0.00309284708018512,
7.32217611708959));
#33939=CARTESIAN_POINT('Ctrl Pts',(-3.9468047458557,0.205704294057958,7.31397704879987));
#33940=CARTESIAN_POINT('Ctrl Pts',(-3.93254600075262,0.408069386251045,
7.30577798051015));
#33941=CARTESIAN_POINT('Ctrl Pts',(-3.90142848745745,0.607808031556218,
7.29757891222042));
#33942=CARTESIAN_POINT('Ctrl Pts',(-3.7004169521544,1.89807089322147,7.2446149337258));
#33943=CARTESIAN_POINT('Ctrl Pts',(-2.79591524746178,3.0787362122301,7.19165095523118));
#33944=CARTESIAN_POINT('Ctrl Pts',(-1.60246363230549,3.60869576898733,7.13868697673655));
#33945=CARTESIAN_POINT('Ctrl Pts',(-0.409012017149199,4.13865532574456,
7.08572299824193));
#33946=CARTESIAN_POINT('Ctrl Pts',(1.07338950847076,4.01790912025038,7.03275901974731));
#33947=CARTESIAN_POINT('Ctrl Pts',(2.16534464372431,3.30179608998848,6.97979504125268));
#33948=CARTESIAN_POINT('Ctrl Pts',(3.25729977897786,2.58568305972658,6.92683106275806));
#33949=CARTESIAN_POINT('Ctrl Pts',(3.95880852386501,1.27420320469696,6.87386708426343));
#33950=CARTESIAN_POINT('Ctrl Pts',(3.94836389256626,-0.0315819228008631,
6.82090310576881));
#33951=CARTESIAN_POINT('Ctrl Pts',(3.93791926126751,-1.33736705029871,6.76793912727419));
#33952=CARTESIAN_POINT('Ctrl Pts',(3.21552125378285,-2.63745745026476,6.71497514877956));
#33953=CARTESIAN_POINT('Ctrl Pts',(2.11225056959203,-3.33601144740646,6.66201117028494));
#33954=CARTESIAN_POINT('Ctrl Pts',(1.00897988540122,-4.03456544454814,6.60904719179032));
#33955=CARTESIAN_POINT('Ctrl Pts',(-0.475163475495736,-4.1315830388655,
6.55608321329569));
#33956=CARTESIAN_POINT('Ctrl Pts',(-1.65998491543528,-3.58260030236365,
6.50311923480107));
#33957=CARTESIAN_POINT('Ctrl Pts',(-2.84480635537483,-3.0336175658618,6.45015525630644));
#33958=CARTESIAN_POINT('Ctrl Pts',(-3.73030587435696,-1.83863449854073,
6.39719127781182));
#33959=CARTESIAN_POINT('Ctrl Pts',(-3.91065206490815,-0.545321256873756,
6.3442272993172));
#33960=CARTESIAN_POINT('Ctrl Pts',(-3.93568069017971,-0.365833947574368,
6.33687690524133));
#33961=CARTESIAN_POINT('Ctrl Pts',(-3.94712794466584,-0.1844527827072,6.32952651116546));
#33962=CARTESIAN_POINT('Ctrl Pts',(-3.94563673384516,-0.00288256983268176,
6.3221761170896));
#33963=CARTESIAN_POINT('Ctrl Pts',(-3.94570073178844,-0.00286656758253237,
6.1778238829104));
#33964=CARTESIAN_POINT('Ctrl Pts',(-3.94716921739174,-0.182409496340425,
6.18509251567532));
#33965=CARTESIAN_POINT('Ctrl Pts',(-3.93597755777244,-0.361768304659314,
6.19236114844024));
#33966=CARTESIAN_POINT('Ctrl Pts',(-3.91150112201508,-0.539295483751872,
6.19962978120516));
#33967=CARTESIAN_POINT('Ctrl Pts',(-3.73306805394085,-1.83346754156567,
6.25261806993341));
#33968=CARTESIAN_POINT('Ctrl Pts',(-2.84862869021566,-3.03029947473994,
6.30560635866166));
#33969=CARTESIAN_POINT('Ctrl Pts',(-1.66386928259682,-3.58081270897423,
6.35859464738991));
#33970=CARTESIAN_POINT('Ctrl Pts',(-0.479109874977974,-4.13132594320853,
6.41158293611816));
#33971=CARTESIAN_POINT('Ctrl Pts',(1.00596957653452,-4.03552047850286,6.4645712248464));
#33972=CARTESIAN_POINT('Ctrl Pts',(2.11017334393921,-3.33734162243677,6.51755951357465));
#33973=CARTESIAN_POINT('Ctrl Pts',(3.21437711134392,-2.63916276637067,6.5705478023029));
#33974=CARTESIAN_POINT('Ctrl Pts',(3.9377051946408,-1.33861051894414,6.62353609103116));
#33975=CARTESIAN_POINT('Ctrl Pts',(3.94837197806129,-0.0322392490748367,
6.6765243797594));
#33976=CARTESIAN_POINT('Ctrl Pts',(3.95903876148178,1.27413202079445,6.72951266848765));
#33977=CARTESIAN_POINT('Ctrl Pts',(3.25704424502592,2.58632231310649,6.7825009572159));
#33978=CARTESIAN_POINT('Ctrl Pts',(2.16438848411372,3.30243896781703,6.83548924594415));
#33979=CARTESIAN_POINT('Ctrl Pts',(1.07173272320153,4.01855562252758,6.8884775346724));
#33980=CARTESIAN_POINT('Ctrl Pts',(-0.411584282167038,4.13859863963661,
6.94146582340065));
#33981=CARTESIAN_POINT('Ctrl Pts',(-1.60517522591216,3.60750511301625,6.9944541121289));
#33982=CARTESIAN_POINT('Ctrl Pts',(-2.7987661696573,3.07641158639588,7.04744240085715));
#33983=CARTESIAN_POINT('Ctrl Pts',(-3.70263105177901,1.89418151604613,7.1004306895854));
#33984=CARTESIAN_POINT('Ctrl Pts',(-3.9021732688668,0.603095702241273,7.15341897831364));
#33985=CARTESIAN_POINT('Ctrl Pts',(-3.9328077662116,0.404883186052253,7.16155394651256));
#33986=CARTESIAN_POINT('Ctrl Pts',(-3.94684167082104,0.204104985193814,
7.16968891471148));
#33987=CARTESIAN_POINT('Ctrl Pts',(-3.94511280640764,0.00308469250234145,
7.1778238829104));
#33988=CARTESIAN_POINT('Origin',(0.,0.,0.));
#33989=CARTESIAN_POINT('',(-3.93579878224384,0.00110209819909501,8.3221761170896));
#33990=CARTESIAN_POINT('',(-3.93583379497513,0.00119086740244391,8.17782388291041));
#33991=CARTESIAN_POINT('',(-3.942,-4.82755768223887E-16,0.));
#33992=CARTESIAN_POINT('Ctrl Pts',(-3.93579878224384,0.00110209819909501,
8.3221761170896));
#33993=CARTESIAN_POINT('Ctrl Pts',(-3.93727495532409,0.591480280077664,
8.29842758643428));
#33994=CARTESIAN_POINT('Ctrl Pts',(-3.81287497830763,1.18126751761344,8.27467905577897));
#33995=CARTESIAN_POINT('Ctrl Pts',(-3.55943403140727,1.70909456204991,8.25093052512365));
#33996=CARTESIAN_POINT('Ctrl Pts',(-2.9942099737124,2.88625455717395,8.19796654662903));
#33997=CARTESIAN_POINT('Ctrl Pts',(-1.78716283564177,3.75523737390689,8.1450025681344));
#33998=CARTESIAN_POINT('Ctrl Pts',(-0.491491832360601,3.91778133957111,
8.09203858963978));
#33999=CARTESIAN_POINT('Ctrl Pts',(0.804179170920576,4.08032530523533,8.03907461114515));
#34000=CARTESIAN_POINT('Ctrl Pts',(2.18847403941229,3.53643041983081,7.98611063265053));
#34001=CARTESIAN_POINT('Ctrl Pts',(3.02695952634759,2.53536799534552,7.93314665415591));
#34002=CARTESIAN_POINT('Ctrl Pts',(3.86544501328289,1.53430557086022,7.88018267566129));
#34003=CARTESIAN_POINT('Ctrl Pts',(4.15812111866178,0.0760756072941503,
7.82721869716666));
#34004=CARTESIAN_POINT('Ctrl Pts',(3.77085207703933,-1.17100361188895,7.77425471867203));
#34005=CARTESIAN_POINT('Ctrl Pts',(3.38358303541687,-2.41808283107204,7.72129074017741));
#34006=CARTESIAN_POINT('Ctrl Pts',(2.31636884679309,-3.45401130587216,7.66832676168279));
#34007=CARTESIAN_POINT('Ctrl Pts',(1.05832218368842,-3.8040148529523,7.61536278318817));
#34008=CARTESIAN_POINT('Ctrl Pts',(-0.199724479416271,-4.15401840003245,
7.56239880469355));
#34009=CARTESIAN_POINT('Ctrl Pts',(-1.64860361700185,-3.81809701939261,
7.50943482619892));
#34010=CARTESIAN_POINT('Ctrl Pts',(-2.62428250283791,-2.95020612691174,
7.45647084770429));
#34011=CARTESIAN_POINT('Ctrl Pts',(-3.44892179457277,-2.21666874973946,
7.41170593749939));
#34012=CARTESIAN_POINT('Ctrl Pts',(-3.93552800730583,-1.10311616471836,
7.36694102729449));
#34013=CARTESIAN_POINT('Ctrl Pts',(-3.94505905468816,0.00309284708018512,
7.32217611708959));
#34014=CARTESIAN_POINT('Ctrl Pts',(-3.94511280640764,0.00308469250234145,
7.1778238829104));
#34015=CARTESIAN_POINT('Ctrl Pts',(-3.93558046309789,-1.10526968584544,
7.22267720343973));
#34016=CARTESIAN_POINT('Ctrl Pts',(-3.44685564182305,-2.22098372195378,
7.26753052396906));
#34017=CARTESIAN_POINT('Ctrl Pts',(-2.61937124393104,-2.95458540793588,
7.31238384449839));
#34018=CARTESIAN_POINT('Ctrl Pts',(-1.64180744985364,-3.82123914704826,
7.36537213322664));
#34019=CARTESIAN_POINT('Ctrl Pts',(-0.191460309644946,-4.15460506801304,
7.41836042195489));
#34020=CARTESIAN_POINT('Ctrl Pts',(1.06640592095225,-3.80177051623037,7.47134871068314));
#34021=CARTESIAN_POINT('Ctrl Pts',(2.32427215154943,-3.44893596444769,7.52433699941139));
#34022=CARTESIAN_POINT('Ctrl Pts',(3.38965747253514,-2.40990093991759,7.57732528813964));
#34023=CARTESIAN_POINT('Ctrl Pts',(3.77387696635039,-1.16126366048821,7.63031357686789));
#34024=CARTESIAN_POINT('Ctrl Pts',(4.15809646016565,0.0873736189411645,
7.68330186559614));
#34025=CARTESIAN_POINT('Ctrl Pts',(3.86115012681045,1.5456131532698,7.73629015432439));
#34026=CARTESIAN_POINT('Ctrl Pts',(3.01924520659187,2.54457049986684,7.78927844305264));
#34027=CARTESIAN_POINT('Ctrl Pts',(2.17734028637328,3.54352784646387,7.84226673178089));
#34028=CARTESIAN_POINT('Ctrl Pts',(0.79047677929132,4.08320300532929,7.89525502050913));
#34029=CARTESIAN_POINT('Ctrl Pts',(-0.505200564699283,3.91605069371529,
7.94824330923738));
#34030=CARTESIAN_POINT('Ctrl Pts',(-1.80087790868988,3.74889838210129,8.00123159796563));
#34031=CARTESIAN_POINT('Ctrl Pts',(-3.00536908958914,2.87491860000785,8.05421988669388));
#34032=CARTESIAN_POINT('Ctrl Pts',(-3.56618228885602,1.69499986105314,8.10720817542213));
#34033=CARTESIAN_POINT('Ctrl Pts',(-3.81530790878367,1.17085387502675,8.13074674458489));
#34034=CARTESIAN_POINT('Ctrl Pts',(-3.93741444221381,0.586335951582262,
8.15428531374765));
#34035=CARTESIAN_POINT('Ctrl Pts',(-3.93583379497513,0.00119086740244391,
8.17782388291041));
#34036=CARTESIAN_POINT('Origin',(0.,0.,0.));
#34037=CARTESIAN_POINT('',(-3.94101045068862,-0.00360005201630542,9.3221761170896));
#34038=CARTESIAN_POINT('',(-3.94073510056759,-0.00358878591061127,9.1778238829104));
#34039=CARTESIAN_POINT('',(-3.942,-4.82755768223887E-16,0.));
#34040=CARTESIAN_POINT('Ctrl Pts',(-3.94101045068862,-0.00360005201630542,
9.3221761170896));
#34041=CARTESIAN_POINT('Ctrl Pts',(-3.93228175108165,0.970079126201241,
9.28287812406869));
#34042=CARTESIAN_POINT('Ctrl Pts',(-3.56768740150403,1.94959821666609,9.24358013104778));
#34043=CARTESIAN_POINT('Ctrl Pts',(-2.91383898553304,2.66460451331084,9.20428213802687));
#34044=CARTESIAN_POINT('Ctrl Pts',(-2.03261297931419,3.6282562219074,9.15131815953225));
#34045=CARTESIAN_POINT('Ctrl Pts',(-0.625975040492547,4.11143697314778,
9.09835418103763));
#34046=CARTESIAN_POINT('Ctrl Pts',(0.661401578964616,3.89270122117173,9.04539020254301));
#34047=CARTESIAN_POINT('Ctrl Pts',(1.9487781984218,3.67396546919568,8.99242622404838));
#34048=CARTESIAN_POINT('Ctrl Pts',(3.11689349851449,2.75331321400316,8.93946224555376));
#34049=CARTESIAN_POINT('Ctrl Pts',(3.63039103221387,1.55268663908397,8.88649826705913));
#34050=CARTESIAN_POINT('Ctrl Pts',(4.14388856591324,0.352060064164805,8.83353428856451));
#34051=CARTESIAN_POINT('Ctrl Pts',(4.00276833321932,-1.12854083048104,8.78057031006989));
#34052=CARTESIAN_POINT('Ctrl Pts',(3.2717068488331,-2.21054498738825,8.72760633157527));
#34053=CARTESIAN_POINT('Ctrl Pts',(2.54064536444688,-3.29254914429547,8.67464235308064));
#34054=CARTESIAN_POINT('Ctrl Pts',(1.21964262836836,-3.97595656346406,8.62167837458601));
#34055=CARTESIAN_POINT('Ctrl Pts',(-0.0858753956759256,-3.94755623929365,
8.56871439609139));
#34056=CARTESIAN_POINT('Ctrl Pts',(-1.39139341972021,-3.91915591512325,
8.51575041759677));
#34057=CARTESIAN_POINT('Ctrl Pts',(-2.68142673173026,-3.17894784761384,
8.46278643910214));
#34058=CARTESIAN_POINT('Ctrl Pts',(-3.36474289907574,-2.06617522710156,
8.40982246060752));
#34059=CARTESIAN_POINT('Ctrl Pts',(-3.74166677096472,-1.45235898112435,
8.38060701276821));
#34060=CARTESIAN_POINT('Ctrl Pts',(-3.93398279378317,-0.725181276064265,
8.35139156492891));
#34061=CARTESIAN_POINT('Ctrl Pts',(-3.93579878224384,0.00110209819909501,
8.3221761170896));
#34062=CARTESIAN_POINT('Ctrl Pts',(-3.93583379497513,0.00119086740244391,
8.17782388291041));
#34063=CARTESIAN_POINT('Ctrl Pts',(-3.93385620587065,-0.730899452746949,
8.2072736024759));
#34064=CARTESIAN_POINT('Ctrl Pts',(-3.73826901230947,-1.46397147804348,
8.23672332204139));
#34065=CARTESIAN_POINT('Ctrl Pts',(-3.35559744737338,-2.0810205230852,8.26617304160688));
#34066=CARTESIAN_POINT('Ctrl Pts',(-2.66706418898931,-3.19126447245286,
8.31916133033513));
#34067=CARTESIAN_POINT('Ctrl Pts',(-1.37286245458661,-3.92589467537216,
8.37214961906338));
#34068=CARTESIAN_POINT('Ctrl Pts',(-0.0666336764464662,-3.94794131155515,
8.42513790779163));
#34069=CARTESIAN_POINT('Ctrl Pts',(1.23959510169366,-3.96998794773813,8.47812619651988));
#34070=CARTESIAN_POINT('Ctrl Pts',(2.55785092357125,-3.27945101718484,8.53111448524812));
#34071=CARTESIAN_POINT('Ctrl Pts',(3.28345891245731,-2.19307505948273,8.58410277397638));
#34072=CARTESIAN_POINT('Ctrl Pts',(4.00906690134337,-1.10669910178063,8.63709106270462));
#34073=CARTESIAN_POINT('Ctrl Pts',(4.14202705723791,0.375515883070263,8.69007935143287));
#34074=CARTESIAN_POINT('Ctrl Pts',(3.62135147131388,1.57368807822049,8.74306764016112));
#34075=CARTESIAN_POINT('Ctrl Pts',(3.10067588538986,2.77186027337072,8.79605592888937));
#34076=CARTESIAN_POINT('Ctrl Pts',(1.92636455764724,3.68598967882027,8.84904421761762));
#34077=CARTESIAN_POINT('Ctrl Pts',(0.637066015602396,3.89677142492153,8.90203250634587));
#34078=CARTESIAN_POINT('Ctrl Pts',(-0.652232526442438,4.1075531710228,8.95502079507412));
#34079=CARTESIAN_POINT('Ctrl Pts',(-2.05651828278951,3.61498725777581,9.00800908380237));
#34080=CARTESIAN_POINT('Ctrl Pts',(-2.93165503760022,2.64501028104501,9.06099737253062));
#34081=CARTESIAN_POINT('Ctrl Pts',(-3.57481082178969,1.93215449058061,9.09993954265721));
#34082=CARTESIAN_POINT('Ctrl Pts',(-3.93216906200874,0.9614452240408,9.13888171278381));
#34083=CARTESIAN_POINT('Ctrl Pts',(-3.94073510056759,-0.00358878591061127,
9.1778238829104));
#34084=CARTESIAN_POINT('Origin',(0.,0.,0.));
#34085=CARTESIAN_POINT('',(-3.94826120782986,0.000860587304522282,10.3221761170896));
#34086=CARTESIAN_POINT('',(-3.94838239458768,0.000624922565347272,10.1778238829104));
#34087=CARTESIAN_POINT('',(-3.942,-4.82755768223887E-16,0.));
#34088=CARTESIAN_POINT('Ctrl Pts',(-3.94826120782986,0.000860587304522282,
10.3221761170896));
#34089=CARTESIAN_POINT('Ctrl Pts',(-3.94839882197096,0.0473049479418113,
10.3202926401977));
#34090=CARTESIAN_POINT('Ctrl Pts',(-3.94765033544244,0.0937447675908473,
10.3184091633059));
#34091=CARTESIAN_POINT('Ctrl Pts',(-3.94600203836796,0.140152628104641,
10.316525686414));
#34092=CARTESIAN_POINT('Ctrl Pts',(-3.89965139229318,1.4451566538172,10.2635617079194));
#34093=CARTESIAN_POINT('Ctrl Pts',(-3.14177325024928,2.72488891140618,10.2105977294247));
#34094=CARTESIAN_POINT('Ctrl Pts',(-2.0197091369755,3.39283802265691,10.1576337509301));
#34095=CARTESIAN_POINT('Ctrl Pts',(-0.897645023701731,4.06078713390763,
10.1046697724355));
#34096=CARTESIAN_POINT('Ctrl Pts',(0.588605060801912,4.11695309882012,10.0517057939409));
#34097=CARTESIAN_POINT('Ctrl Pts',(1.75788099084149,3.53559461307527,9.99874181544624));
#34098=CARTESIAN_POINT('Ctrl Pts',(2.92715692088108,2.95423612733042,9.94577783695161));
#34099=CARTESIAN_POINT('Ctrl Pts',(3.7794586964566,1.73535319092823,9.89281385845698));
#34100=CARTESIAN_POINT('Ctrl Pts',(3.92416969750304,0.437569458677891,9.83984987996236));
#34101=CARTESIAN_POINT('Ctrl Pts',(4.06888069854947,-0.860214273572448,
9.78688590146773));
#34102=CARTESIAN_POINT('Ctrl Pts',(3.50600092506682,-2.23689880167093,9.73392192297312));
#34103=CARTESIAN_POINT('Ctrl Pts',(2.49350261285418,-3.06153875782394,9.68095794447849));
#34104=CARTESIAN_POINT('Ctrl Pts',(1.48100430064151,-3.88617871397697,9.62799396598387));
#34105=CARTESIAN_POINT('Ctrl Pts',(0.0188874496988303,-4.15877409818449,
9.57502998748924));
#34106=CARTESIAN_POINT('Ctrl Pts',(-1.22274826539589,-3.75439229775474,
9.52206600899461));
#34107=CARTESIAN_POINT('Ctrl Pts',(-2.46438398049055,-3.350010497325,9.46910203049999));
#34108=CARTESIAN_POINT('Ctrl Pts',(-3.48553855973727,-2.26865151225807,
9.41613805200537));
#34109=CARTESIAN_POINT('Ctrl Pts',(-3.81820881255261,-1.00591068674825,
9.36317407351075));
#34110=CARTESIAN_POINT('Ctrl Pts',(-3.90404577140141,-0.680093059958056,
9.34950808803704));
#34111=CARTESIAN_POINT('Ctrl Pts',(-3.94404588005443,-0.342199672065631,
9.33584210256332));
#34112=CARTESIAN_POINT('Ctrl Pts',(-3.94101045068862,-0.00360005201630542,
9.3221761170896));
#34113=CARTESIAN_POINT('Ctrl Pts',(-3.94073510056759,-0.00358878591061127,
9.1778238829104));
#34114=CARTESIAN_POINT('Ctrl Pts',(-3.94382479981015,-0.351668569711599,
9.19187000151206));
#34115=CARTESIAN_POINT('Ctrl Pts',(-3.90153714912137,-0.6990100110183,9.20591612011371));
#34116=CARTESIAN_POINT('Ctrl Pts',(-3.81091609517323,-1.03324690266663,
9.21996223871536));
#34117=CARTESIAN_POINT('Ctrl Pts',(-3.46905264466117,-2.29413906943288,
9.27295052744361));
#34118=CARTESIAN_POINT('Ctrl Pts',(-2.4393379903627,-3.36853536275074,9.32593881617186));
#34119=CARTESIAN_POINT('Ctrl Pts',(-1.194095160419,-3.76361759404226,9.37892710490011));
#34120=CARTESIAN_POINT('Ctrl Pts',(0.0511476695246889,-4.15869982533377,
9.43191539362836));
#34121=CARTESIAN_POINT('Ctrl Pts',(1.5119186751136,-3.87446799459896,9.48490368235661));
#34122=CARTESIAN_POINT('Ctrl Pts',(2.5181722452647,-3.04129728726066,9.53789197108486));
#34123=CARTESIAN_POINT('Ctrl Pts',(3.5244258154158,-2.20812657992236,9.59088025981311));
#34124=CARTESIAN_POINT('Ctrl Pts',(4.07616195012909,-0.826016995980571,
9.64386854854136));
#34125=CARTESIAN_POINT('Ctrl Pts',(3.92030308000722,0.471067306450377,9.69685683726961));
#34126=CARTESIAN_POINT('Ctrl Pts',(3.76444420988535,1.76815160888132,9.74984512599786));
#34127=CARTESIAN_POINT('Ctrl Pts',(2.90099033492832,2.98021062980143,9.8028334147261));
#34128=CARTESIAN_POINT('Ctrl Pts',(1.72600180756239,3.55128123451409,9.85582170345435));
#34129=CARTESIAN_POINT('Ctrl Pts',(0.551013280196442,4.12235183922675,9.90880999218261));
#34130=CARTESIAN_POINT('Ctrl Pts',(-0.935509899578419,4.05243402773195,
9.96179828091086));
#34131=CARTESIAN_POINT('Ctrl Pts',(-2.05170977553871,3.37359861917203,10.0147865696391));
#34132=CARTESIAN_POINT('Ctrl Pts',(-3.16790965149901,2.69476321061211,10.0677748583674));
#34133=CARTESIAN_POINT('Ctrl Pts',(-3.91378622364473,1.40701020498706,10.1207631470956));
#34134=CARTESIAN_POINT('Ctrl Pts',(-3.94721103949169,0.101023047050935,
10.1737514358238));
#34135=CARTESIAN_POINT('Ctrl Pts',(-3.94806733432703,0.0675655685271688,
10.175108918186));
#34136=CARTESIAN_POINT('Ctrl Pts',(-3.94845604040098,0.0340961227584357,
10.1764664005482));
#34137=CARTESIAN_POINT('Ctrl Pts',(-3.94838239458768,0.000624922565347272,
10.1778238829104));
#34138=CARTESIAN_POINT('Origin',(0.,0.,0.));
#34139=CARTESIAN_POINT('',(-3.93845364011251,0.00310220437029302,11.3221761170896));
#34140=CARTESIAN_POINT('',(-3.93886953396072,0.00324640498314072,11.1778238829104));
#34141=CARTESIAN_POINT('',(-3.942,-4.82755768223887E-16,0.));
#34142=CARTESIAN_POINT('Ctrl Pts',(-3.93845364011251,0.00310220437029302,
11.3221761170896));
#34143=CARTESIAN_POINT('Ctrl Pts',(-3.94163276156383,0.435745363096063,
11.3047431778321));
#34144=CARTESIAN_POINT('Ctrl Pts',(-3.87593103620607,0.867449899692147,
11.2873102385747));
#34145=CARTESIAN_POINT('Ctrl Pts',(-3.73722250128773,1.27426167714383,11.2698772993172));
#34146=CARTESIAN_POINT('Ctrl Pts',(-3.31580441728399,2.51021907446466,11.2169133208226));
#34147=CARTESIAN_POINT('Ctrl Pts',(-2.2205051385,3.51640664107286,11.163949342328));
#34148=CARTESIAN_POINT('Ctrl Pts',(-0.953308955593125,3.83168068622044,
11.1109853638333));
#34149=CARTESIAN_POINT('Ctrl Pts',(0.313887227313751,4.14695473136801,11.0580213853387));
#34150=CARTESIAN_POINT('Ctrl Pts',(1.75298031434354,3.77131525505496,11.0050574068441));
#34151=CARTESIAN_POINT('Ctrl Pts',(2.70442260335169,2.87692078939432,10.9520934283495));
#34152=CARTESIAN_POINT('Ctrl Pts',(3.65586489235987,1.98252632373365,10.8991294498548));
#34153=CARTESIAN_POINT('Ctrl Pts',(4.11965638334642,0.569376868725343,10.8461654713602));
#34154=CARTESIAN_POINT('Ctrl Pts',(3.88323778121684,-0.714870044482812,
10.7932014928656));
#34155=CARTESIAN_POINT('Ctrl Pts',(3.64681917908728,-1.99911695769091,10.740237514371));
#34156=CARTESIAN_POINT('Ctrl Pts',(2.71019048384171,-3.15446132909884,10.6872735358763));
#34157=CARTESIAN_POINT('Ctrl Pts',(1.5026160073439,-3.65139972893172,10.6343095573817));
#34158=CARTESIAN_POINT('Ctrl Pts',(0.295041530846062,-4.14833812876461,
10.5813455788871));
#34159=CARTESIAN_POINT('Ctrl Pts',(-1.18347872690403,-3.98687055702237,
10.5283816003925));
#34160=CARTESIAN_POINT('Ctrl Pts',(-2.25532728072623,-3.24099887423319,
10.4754176218978));
#34161=CARTESIAN_POINT('Ctrl Pts',(-3.28905932517556,-2.52165148434584,
10.4243371202951));
#34162=CARTESIAN_POINT('Ctrl Pts',(-3.94452906787893,-1.25872547303165,
10.3732566186924));
#34163=CARTESIAN_POINT('Ctrl Pts',(-3.94826120782986,0.000860587304522282,
10.3221761170896));
#34164=CARTESIAN_POINT('Ctrl Pts',(-3.94838239458768,0.000624922565347272,
10.1778238829104));
#34165=CARTESIAN_POINT('Ctrl Pts',(-3.94558133224467,-1.27242665007483,
10.2294546892765));
#34166=CARTESIAN_POINT('Ctrl Pts',(-3.27394054517676,-2.548016178621,10.2810854956425));
#34167=CARTESIAN_POINT('Ctrl Pts',(-2.22159520444575,-3.26422967848529,
10.3327163020086));
#34168=CARTESIAN_POINT('Ctrl Pts',(-1.14158149400459,-3.99927393583826,
10.3857045907369));
#34169=CARTESIAN_POINT('Ctrl Pts',(0.339418986425944,-4.14514114029698,
10.4386928794651));
#34170=CARTESIAN_POINT('Ctrl Pts',(1.54208150481898,-3.63492300865035,10.4916811681933));
#34171=CARTESIAN_POINT('Ctrl Pts',(2.744744023212,-3.12470487700374,10.5446694569216));
#34172=CARTESIAN_POINT('Ctrl Pts',(3.66906857956751,-1.95840140925179,10.5976577456498));
#34173=CARTESIAN_POINT('Ctrl Pts',(3.89107385865357,-0.670987982622134,
10.6506460343781));
#34174=CARTESIAN_POINT('Ctrl Pts',(4.11307913773965,0.616425444007545,10.7036343231063));
#34175=CARTESIAN_POINT('Ctrl Pts',(3.63276513955622,2.02494882951498,10.7566226118346));
#34176=CARTESIAN_POINT('Ctrl Pts',(2.67044859081355,2.90850218671784,10.8096109005628));
#34177=CARTESIAN_POINT('Ctrl Pts',(1.70813204207087,3.79205554392072,10.8625991892911));
#34178=CARTESIAN_POINT('Ctrl Pts',(0.263812942768934,4.15063887281905,10.9155874780193));
#34179=CARTESIAN_POINT('Ctrl Pts',(-1.00000947224434,3.81977246727369,10.9685757667476));
#34180=CARTESIAN_POINT('Ctrl Pts',(-2.2638318872576,3.48890606172833,11.0215640554758));
#34181=CARTESIAN_POINT('Ctrl Pts',(-3.34715761798219,2.46858992173929,11.0745523442041));
#34182=CARTESIAN_POINT('Ctrl Pts',(-3.75307260433058,1.22683604158983,11.1275406329323));
#34183=CARTESIAN_POINT('Ctrl Pts',(-3.88147031395203,0.834048488809281,
11.1443017162584));
#34184=CARTESIAN_POINT('Ctrl Pts',(-3.94208881978707,0.419104697969423,
11.1610627995844));
#34185=CARTESIAN_POINT('Ctrl Pts',(-3.93886953396072,0.00324640498314072,
11.1778238829104));
#34186=CARTESIAN_POINT('Origin',(0.,0.,0.));
#34187=CARTESIAN_POINT('',(-3.93708098219134,-0.00243404615490106,12.3221761170896));
#34188=CARTESIAN_POINT('',(-3.93670434321626,-0.00217448122624482,12.1778238829104));
#34189=CARTESIAN_POINT('',(-3.942,-4.82755768223887E-16,0.));
#34190=CARTESIAN_POINT('Ctrl Pts',(-3.93708098219134,-0.00243404615490106,
12.3221761170896));
#34191=CARTESIAN_POINT('Ctrl Pts',(-3.93246581499902,0.816826384091263,
12.2891937154665));
#34192=CARTESIAN_POINT('Ctrl Pts',(-3.68329161894405,1.63865836153011,12.2562113138435));
#34193=CARTESIAN_POINT('Ctrl Pts',(-3.20967797357049,2.29968305467193,12.2232289122204));
#34194=CARTESIAN_POINT('Ctrl Pts',(-2.4491371489512,3.36117330126154,12.1702649337258));
#34195=CARTESIAN_POINT('Ctrl Pts',(-1.10983987433617,4.00799378602558,12.1173009552312));
#34196=CARTESIAN_POINT('Ctrl Pts',(0.194403355371928,3.94370158371407,12.0643369767366));
#34197=CARTESIAN_POINT('Ctrl Pts',(1.49864658508003,3.87940938140256,12.0113729982419));
#34198=CARTESIAN_POINT('Ctrl Pts',(2.7678357698812,3.1040044920155,11.9584090197473));
#34199=CARTESIAN_POINT('Ctrl Pts',(3.42029150490108,1.97286108671397,11.9054450412527));
#34200=CARTESIAN_POINT('Ctrl Pts',(4.07274723992097,0.841717681412442,11.8524810627581));
#34201=CARTESIAN_POINT('Ctrl Pts',(4.10846952515958,-0.645164239803552,
11.7995170842634));
#34202=CARTESIAN_POINT('Ctrl Pts',(3.51108655579286,-1.8063349754958,11.7465531057688));
#34203=CARTESIAN_POINT('Ctrl Pts',(2.91370358642613,-2.96750571118807,11.6935891272742));
#34204=CARTESIAN_POINT('Ctrl Pts',(1.68321536245406,-3.80296526135658,11.6406251487796));
#34205=CARTESIAN_POINT('Ctrl Pts',(0.383564333431266,-3.92981593056064,
11.5876611702849));
#34206=CARTESIAN_POINT('Ctrl Pts',(-0.91608669559151,-4.0566665997647,11.5346971917903));
#34207=CARTESIAN_POINT('Ctrl Pts',(-2.28490052966501,-3.47490838800432,
11.4817332132957));
#34208=CARTESIAN_POINT('Ctrl Pts',(-3.09553900209,-2.4511656681074,11.4287692348011));
#34209=CARTESIAN_POINT('Ctrl Pts',(-3.6393581823996,-1.76438488268918,11.3932381955639));
#34210=CARTESIAN_POINT('Ctrl Pts',(-3.93197409656805,-0.878691784660489,
11.3577071563268));
#34211=CARTESIAN_POINT('Ctrl Pts',(-3.93845364011251,0.00310220437029302,
11.3221761170896));
#34212=CARTESIAN_POINT('Ctrl Pts',(-3.93886953396072,0.00324640498314072,
11.1778238829104));
#34213=CARTESIAN_POINT('Ctrl Pts',(-3.9319114080084,-0.895584744841287,
11.2140510883126));
#34214=CARTESIAN_POINT('Ctrl Pts',(-3.62672875965172,-1.79868808138705,
11.2502782937149));
#34215=CARTESIAN_POINT('Ctrl Pts',(-3.06311856673542,-2.49158288893653,
11.2865054991171));
#34216=CARTESIAN_POINT('Ctrl Pts',(-2.23874530081967,-3.50505631900356,
11.3394937878453));
#34217=CARTESIAN_POINT('Ctrl Pts',(-0.861494527015975,-4.06881155882777,
11.3924820765736));
#34218=CARTESIAN_POINT('Ctrl Pts',(0.436898299346125,-3.92425795818127,
11.4454703653018));
#34219=CARTESIAN_POINT('Ctrl Pts',(1.73529112570822,-3.77970435753476,11.4984586540301));
#34220=CARTESIAN_POINT('Ctrl Pts',(2.95482600462875,-2.92684191641753,11.5514469427583));
#34221=CARTESIAN_POINT('Ctrl Pts',(3.53611067677546,-1.75687276941591,11.6044352314866));
#34222=CARTESIAN_POINT('Ctrl Pts',(4.11739534892219,-0.586903622414244,
11.6574235202148));
#34223=CARTESIAN_POINT('Ctrl Pts',(4.06042981429509,0.900172230471804,11.7104118089431));
#34224=CARTESIAN_POINT('Ctrl Pts',(3.39134377174076,2.02224332566476,11.7634000976713));
#34225=CARTESIAN_POINT('Ctrl Pts',(2.72225772918646,3.14431442085768,11.8163883863996));
#34226=CARTESIAN_POINT('Ctrl Pts',(1.44105117870494,3.90138075835749,11.8693766751278));
#34227=CARTESIAN_POINT('Ctrl Pts',(0.135404751111381,3.94618121729058,11.9223649638561));
#34228=CARTESIAN_POINT('Ctrl Pts',(-1.17024167648218,3.99098167622367,11.9753532525843));
#34229=CARTESIAN_POINT('Ctrl Pts',(-2.50032798118779,3.32351625659005,12.0283415413126));
#34230=CARTESIAN_POINT('Ctrl Pts',(-3.24475272518949,2.24994675463574,12.0813298300408));
#34231=CARTESIAN_POINT('Ctrl Pts',(-3.69662968598688,1.59827399972424,12.1134945143307));
#34232=CARTESIAN_POINT('Ctrl Pts',(-3.93270958942814,0.796965223217272,
12.1456591986205));
#34233=CARTESIAN_POINT('Ctrl Pts',(-3.93670434321626,-0.00217448122624482,
12.1778238829104));
#34234=CARTESIAN_POINT('Origin',(0.,0.,0.));
#34235=CARTESIAN_POINT('',(-3.94733077553239,-0.00192598462593618,13.3221761170896));
#34236=CARTESIAN_POINT('',(-3.94682996399265,-0.00229165249276323,13.1778238829104));
#34237=CARTESIAN_POINT('',(-3.942,-4.82755768223887E-16,0.));
#34238=CARTESIAN_POINT('Ctrl Pts',(-3.94733077553239,-0.00192598462593618,
13.3221761170896));
#34239=CARTESIAN_POINT('Ctrl Pts',(-3.94013816129704,1.1955636687552,13.273644253101));
#34240=CARTESIAN_POINT('Ctrl Pts',(-3.356565432248,2.39912123530496,13.2251123891123));
#34241=CARTESIAN_POINT('Ctrl Pts',(-2.40836516771617,3.12895382914166,13.1765805251237));
#34242=CARTESIAN_POINT('Ctrl Pts',(-1.37357164668001,3.92543751280327,13.123616546629));
#34243=CARTESIAN_POINT('Ctrl Pts',(0.0954887653771007,4.15772060523228,
13.0706525681344));
#34244=CARTESIAN_POINT('Ctrl Pts',(1.32553410510171,3.71934593472844,13.0176885896398));
#34245=CARTESIAN_POINT('Ctrl Pts',(2.55557944482628,3.28097126422461,12.9647246111452));
#34246=CARTESIAN_POINT('Ctrl Pts',(3.54660971221836,2.17193883078797,12.9117606326505));
#34247=CARTESIAN_POINT('Ctrl Pts',(3.84442792620346,0.900526938073336,12.8587966541559));
#34248=CARTESIAN_POINT('Ctrl Pts',(4.14224614018855,-0.370884954641299,
12.8058326756613));
#34249=CARTESIAN_POINT('Ctrl Pts',(3.74685230076666,-1.80467630663392,12.7528686971667));
#34250=CARTESIAN_POINT('Ctrl Pts',(2.83945852033214,-2.74372924270635,12.699904718672));
#34251=CARTESIAN_POINT('Ctrl Pts',(1.93206473989763,-3.68278217877878,12.6469407401774));
#34252=CARTESIAN_POINT('Ctrl Pts',(0.512671018450501,-4.127096698931,12.5939767616828));
#34253=CARTESIAN_POINT('Ctrl Pts',(-0.768203316346435,-3.8730399572846,
12.5410127831882));
#34254=CARTESIAN_POINT('Ctrl Pts',(-2.04907765114337,-3.6189832156382,12.4880488046935));
#34255=CARTESIAN_POINT('Ctrl Pts',(-3.19143259929011,-2.66655521219318,
12.4350848261989));
#34256=CARTESIAN_POINT('Ctrl Pts',(-3.67171788605172,-1.45226120626306,
12.3821208477043));
#34257=CARTESIAN_POINT('Ctrl Pts',(-3.85291381676684,-0.994147791942479,
12.3621392708327));
#34258=CARTESIAN_POINT('Ctrl Pts',(-3.93987696773182,-0.498762829361246,
12.3421576939612));
#34259=CARTESIAN_POINT('Ctrl Pts',(-3.93708098219134,-0.00243404615490106,
12.3221761170896));
#34260=CARTESIAN_POINT('Ctrl Pts',(-3.93670434321626,-0.00217448122624482,
12.1778238829104));
#34261=CARTESIAN_POINT('Ctrl Pts',(-3.93929057014649,-0.519542192545187,
12.1986474873488));
#34262=CARTESIAN_POINT('Ctrl Pts',(-3.84460194542603,-1.03600077131728,
12.2194710917872));
#34263=CARTESIAN_POINT('Ctrl Pts',(-3.64821869509448,-1.51035790430073,
12.2402946962256));
#34264=CARTESIAN_POINT('Ctrl Pts',(-3.14849673769996,-2.71741947700787,
12.2932829849538));
#34265=CARTESIAN_POINT('Ctrl Pts',(-1.99028963961311,-3.65186903814713,
12.3462712736821));
#34266=CARTESIAN_POINT('Ctrl Pts',(-0.704859028994106,-3.8850810024459,
12.3992595624103));
#34267=CARTESIAN_POINT('Ctrl Pts',(0.580571581624919,-4.11829296674466,
12.4522478511386));
#34268=CARTESIAN_POINT('Ctrl Pts',(1.99322570477611,-3.6502673342029,12.5052361398668));
#34269=CARTESIAN_POINT('Ctrl Pts',(2.88512861233689,-2.6956842427472,12.5582244285951));
#34270=CARTESIAN_POINT('Ctrl Pts',(3.77703151989765,-1.74110115129151,12.6112127173233));
#34271=CARTESIAN_POINT('Ctrl Pts',(4.148183211868,-0.299960600921891,12.6642010060516));
#34272=CARTESIAN_POINT('Ctrl Pts',(3.82833896043004,0.966696152042594,12.7171892947798));
#34273=CARTESIAN_POINT('Ctrl Pts',(3.50849470899208,2.23335290500708,12.7701775835081));
#34274=CARTESIAN_POINT('Ctrl Pts',(2.4976545141458,3.32552586056643,12.8231658722363));
#34275=CARTESIAN_POINT('Ctrl Pts',(1.259483819326,3.74224279746471,12.8761541609646));
#34276=CARTESIAN_POINT('Ctrl Pts',(0.0213131245061955,4.158959734363,12.9291424496928));
#34277=CARTESIAN_POINT('Ctrl Pts',(-1.44418807028713,3.90022065260022,12.9821307384211));
#34278=CARTESIAN_POINT('Ctrl Pts',(-2.46480444872359,3.08470738901973,13.0351190271493));
#34279=CARTESIAN_POINT('Ctrl Pts',(-3.38102522484729,2.35261038265819,13.082687312403));
#34280=CARTESIAN_POINT('Ctrl Pts',(-3.93871824071251,1.17181521210322,13.1302555976567));
#34281=CARTESIAN_POINT('Ctrl Pts',(-3.94682996399265,-0.00229165249276323,
13.1778238829104));
#34282=CARTESIAN_POINT('Origin',(0.,0.,0.));
#34283=CARTESIAN_POINT('',(-3.9429197498326,0.0035503728418125,14.3221761170896));
#34284=CARTESIAN_POINT('',(-3.94377660893062,0.00343048778150908,14.1778238829104));
#34285=CARTESIAN_POINT('',(-3.942,-4.82755768223887E-16,0.));
#34286=CARTESIAN_POINT('Ctrl Pts',(-3.9429197498326,0.0035503728418125,
14.3221761170896));
#34287=CARTESIAN_POINT('Ctrl Pts',(-3.94546599449794,0.278662013094457,
14.31105876923));
#34288=CARTESIAN_POINT('Ctrl Pts',(-3.91912941936741,0.553289499978031,
14.2999414213704));
#34289=CARTESIAN_POINT('Ctrl Pts',(-3.86210967795079,0.821391308358944,
14.2888240735108));
#34290=CARTESIAN_POINT('Ctrl Pts',(-3.59046284308573,2.09865083039248,14.2358600950161));
#34291=CARTESIAN_POINT('Ctrl Pts',(-2.62241565120338,3.22780031721448,14.1828961165215));
#34292=CARTESIAN_POINT('Ctrl Pts',(-1.40163175876062,3.69134166107696,14.1299321380269));
#34293=CARTESIAN_POINT('Ctrl Pts',(-0.18084786631787,4.15488300493943,14.0769681595322));
#34294=CARTESIAN_POINT('Ctrl Pts',(1.29267272668526,3.95281620584241,14.0240041810376));
#34295=CARTESIAN_POINT('Ctrl Pts',(2.34360392082064,3.17775007014128,13.971040202543));
#34296=CARTESIAN_POINT('Ctrl Pts',(3.39453511495603,2.40268393444014,13.9180762240484));
#34297=CARTESIAN_POINT('Ctrl Pts',(4.02287691022366,1.05461846213484,13.8651122455537));
#34298=CARTESIAN_POINT('Ctrl Pts',(3.9406553103857,-0.24861731777516,13.8121482670591));
#34299=CARTESIAN_POINT('Ctrl Pts',(3.85843371054775,-1.55185309768514,13.7591842885645));
#34300=CARTESIAN_POINT('Ctrl Pts',(3.06564871560427,-2.81025918519985,13.7062203100699));
#34301=CARTESIAN_POINT('Ctrl Pts',(1.92563993605177,-3.44709815390442,13.6532563315753));
#34302=CARTESIAN_POINT('Ctrl Pts',(0.7856311564993,-4.08393712260898,13.6002923530807));
#34303=CARTESIAN_POINT('Ctrl Pts',(-0.701601407662154,-4.09920897250343,
13.547328374586));
#34304=CARTESIAN_POINT('Ctrl Pts',(-1.85444735256939,-3.48591449443573,
13.4943643960914));
#34305=CARTESIAN_POINT('Ctrl Pts',(-3.00729329747666,-2.87262001636802,
13.4414004175968));
#34306=CARTESIAN_POINT('Ctrl Pts',(-3.82575262312968,-1.63075921033812,
13.3884364391021));
#34307=CARTESIAN_POINT('Ctrl Pts',(-3.93471897094859,-0.329486669876098,
13.3354724606075));
#34308=CARTESIAN_POINT('Ctrl Pts',(-3.94383745759853,-0.22059400231727,
13.3310403461016));
#34309=CARTESIAN_POINT('Ctrl Pts',(-3.94798763243564,-0.111285296783124,
13.3266082315956));
#34310=CARTESIAN_POINT('Ctrl Pts',(-3.94733077553239,-0.00192598462593618,
13.3221761170896));
#34311=CARTESIAN_POINT('Ctrl Pts',(-3.94682996399265,-0.00229165249276323,
13.1778238829104));
#34312=CARTESIAN_POINT('Ctrl Pts',(-3.94775422620073,-0.13607119177326,
13.183243886385));
#34313=CARTESIAN_POINT('Ctrl Pts',(-3.94154345388817,-0.269763898960769,
13.1886638898595));
#34314=CARTESIAN_POINT('Ctrl Pts',(-3.92791502810543,-0.402696136440426,
13.1940838933341));
#34315=CARTESIAN_POINT('Ctrl Pts',(-3.79467766697122,-1.70229895292184,
13.2470721820623));
#34316=CARTESIAN_POINT('Ctrl Pts',(-2.95247138262324,-2.92921714048647,
13.3000604707906));
#34317=CARTESIAN_POINT('Ctrl Pts',(-1.78761040384536,-3.52067176691954,
13.3530487595188));
#34318=CARTESIAN_POINT('Ctrl Pts',(-0.622749425067479,-4.1121263933526,
13.4060370482471));
#34319=CARTESIAN_POINT('Ctrl Pts',(0.864766248140306,-4.0681174586541,13.4590253369753));
#34320=CARTESIAN_POINT('Ctrl Pts',(1.99262340964458,-3.4088315584166,13.5120136257036));
#34321=CARTESIAN_POINT('Ctrl Pts',(3.12048057114885,-2.7495456581791,13.5650019144318));
#34322=CARTESIAN_POINT('Ctrl Pts',(3.8886792209496,-1.4749827924026,13.6179902031601));
#34323=CARTESIAN_POINT('Ctrl Pts',(3.94485192310407,-0.169776179432411,
13.6709784918883));
#34324=CARTESIAN_POINT('Ctrl Pts',(4.00102462525853,1.13543043353777,13.7239667806165));
#34325=CARTESIAN_POINT('Ctrl Pts',(3.34517137976671,2.47128079370165,13.7769550693448));
#34326=CARTESIAN_POINT('Ctrl Pts',(2.27812755848019,3.2250295306576,13.829943358073));
#34327=CARTESIAN_POINT('Ctrl Pts',(1.21108373719365,3.97877826761357,13.8829316468013));
#34328=CARTESIAN_POINT('Ctrl Pts',(-0.267150659887593,4.15042538136161,
13.9359199355295));
#34329=CARTESIAN_POINT('Ctrl Pts',(-1.47851968414005,3.66123752164906,13.9889082242578));
#34330=CARTESIAN_POINT('Ctrl Pts',(-2.68988870839249,3.17204966193652,14.041896512986));
#34331=CARTESIAN_POINT('Ctrl Pts',(-3.63439235981614,2.02202682876341,14.0948848017143));
#34332=CARTESIAN_POINT('Ctrl Pts',(-3.87879331109071,0.738676584276535,
14.1478730904425));
#34333=CARTESIAN_POINT('Ctrl Pts',(-3.92484123568096,0.496878772227051,
14.1578566879318));
#34334=CARTESIAN_POINT('Ctrl Pts',(-3.9460363164428,0.250347989813759,14.1678402854211));
#34335=CARTESIAN_POINT('Ctrl Pts',(-3.94377660893062,0.00343048778150908,
14.1778238829104));
#34336=CARTESIAN_POINT('Origin',(0.,0.,0.));
#34337=CARTESIAN_POINT('',(-3.935515150562,-7.56757525427476E-5,15.3221761170896));
#34338=CARTESIAN_POINT('',(-3.93554762371472,0.000453016733568931,15.1778238829104));
#34339=CARTESIAN_POINT('',(-3.942,-4.82755768223887E-16,0.));
#34340=CARTESIAN_POINT('Ctrl Pts',(-3.935515150562,-7.56757525427476E-5,
15.3221761170896));
#34341=CARTESIAN_POINT('Ctrl Pts',(-3.93540179088204,0.662968867054025,
15.2955093068644));
#34342=CARTESIAN_POINT('Ctrl Pts',(-3.77682343808938,1.32606434282809,15.2688424966392));
#34343=CARTESIAN_POINT('Ctrl Pts',(-3.46008318945363,1.90220902322252,15.242175686414));
#34344=CARTESIAN_POINT('Ctrl Pts',(-2.83099318673311,3.04651215526165,15.1892117079193));
#34345=CARTESIAN_POINT('Ctrl Pts',(-1.57799465489921,3.84781647231203,15.1362477294247));
#34346=CARTESIAN_POINT('Ctrl Pts',(-0.275346694985541,3.93887789142153,
15.0832837509301));
#34347=CARTESIAN_POINT('Ctrl Pts',(1.02730126492813,4.02993931053103,15.0303197724355));
#34348=CARTESIAN_POINT('Ctrl Pts',(2.37959865292158,3.41075783169958,14.9773557939409));
#34349=CARTESIAN_POINT('Ctrl Pts',(3.16177691968707,2.36510920595707,14.9243918154462));
#34350=CARTESIAN_POINT('Ctrl Pts',(3.94395518645256,1.31946058021456,14.8714278369516));
#34351=CARTESIAN_POINT('Ctrl Pts',(4.15601433199016,-0.152655192438981,
14.818463858457));
#34352=CARTESIAN_POINT('Ctrl Pts',(3.70076597882895,-1.37655585281198,14.7654998799624));
#34353=CARTESIAN_POINT('Ctrl Pts',(3.24551762566774,-2.60045651318499,14.7125359014677));
#34354=CARTESIAN_POINT('Ctrl Pts',(2.1229617738077,-3.57614206127742,14.6595719229731));
#34355=CARTESIAN_POINT('Ctrl Pts',(0.847574616134508,-3.85644812178943,
14.6066079444785));
#34356=CARTESIAN_POINT('Ctrl Pts',(-0.427812541538684,-4.13675418230144,
14.5536439659839));
#34357=CARTESIAN_POINT('Ctrl Pts',(-1.85603100502504,-3.72168075523303,
14.5006799874892));
#34358=CARTESIAN_POINT('Ctrl Pts',(-2.78251699784433,-2.80145926307632,
14.4477160089946));
#34359=CARTESIAN_POINT('Ctrl Pts',(-3.5145299287451,-2.07439588945562,14.4058693783596));
#34360=CARTESIAN_POINT('Ctrl Pts',(-3.93333547115731,-1.0319929364451,14.3640227477246));
#34361=CARTESIAN_POINT('Ctrl Pts',(-3.9429197498326,0.0035503728418125,
14.3221761170896));
#34362=CARTESIAN_POINT('Ctrl Pts',(-3.94377660893062,0.00343048778150908,
14.1778238829104));
#34363=CARTESIAN_POINT('Ctrl Pts',(-3.93404284072175,-1.06017518620376,
14.2208285741494));
#34364=CARTESIAN_POINT('Ctrl Pts',(-3.48910890040614,-2.13095638625906,
14.2638332653883));
#34365=CARTESIAN_POINT('Ctrl Pts',(-2.72071532173612,-2.86153608825589,
14.3068379566273));
#34366=CARTESIAN_POINT('Ctrl Pts',(-1.77393812998146,-3.7617208605008,14.3598262453555));
#34367=CARTESIAN_POINT('Ctrl Pts',(-0.336085495346666,-4.14541274918995,
14.4128145340838));
#34368=CARTESIAN_POINT('Ctrl Pts',(0.933309470178012,-3.83661492453915,
14.465802822812));
#34369=CARTESIAN_POINT('Ctrl Pts',(2.20270443570267,-3.52781709988836,14.5187911115403));
#34370=CARTESIAN_POINT('Ctrl Pts',(3.30364173211722,-2.5265295618976,14.5717794002685));
#34371=CARTESIAN_POINT('Ctrl Pts',(3.73112899530853,-1.29203601601831,14.6247676889968));
#34372=CARTESIAN_POINT('Ctrl Pts',(4.15861625849985,-0.0575424701390118,
14.677755977725));
#34373=CARTESIAN_POINT('Ctrl Pts',(3.91265348846795,1.41015708362883,14.7307442664533));
#34374=CARTESIAN_POINT('Ctrl Pts',(3.10606211575817,2.43783895681654,14.7837325551815));
#34375=CARTESIAN_POINT('Ctrl Pts',(2.29947074304839,3.46552083000428,14.8367208439098));
#34376=CARTESIAN_POINT('Ctrl Pts',(0.932250767660721,4.05318502261185,14.889709132638));
#34377=CARTESIAN_POINT('Ctrl Pts',(-0.368463413303181,3.93127401224813,
14.9426974213663));
#34378=CARTESIAN_POINT('Ctrl Pts',(-1.66917759426705,3.80936300188441,14.9956857100945));
#34379=CARTESIAN_POINT('Ctrl Pts',(-2.90338598080718,2.9778767885494,15.0486739988228));
#34380=CARTESIAN_POINT('Ctrl Pts',(-3.50496567659063,1.81821237820066,15.101662287551));
#34381=CARTESIAN_POINT('Ctrl Pts',(-3.79318829122445,1.26260601250841,15.1270494860042));
#34382=CARTESIAN_POINT('Ctrl Pts',(-3.93619350756073,0.631667647738924,
15.1524366844573));
#34383=CARTESIAN_POINT('Ctrl Pts',(-3.93554762371472,0.000453016733568931,
15.1778238829104));
#34384=CARTESIAN_POINT('Origin',(0.,0.,0.));
#34385=CARTESIAN_POINT('',(-3.94319808732824,-0.00351593218956836,16.3221761170896));
#34386=CARTESIAN_POINT('',(-3.94210945089404,-0.00361990150021516,16.1778238829104));
#34387=CARTESIAN_POINT('',(-3.942,-4.82755768223887E-16,0.));
#34388=CARTESIAN_POINT('Ctrl Pts',(-3.94319808732824,-0.00351593218956836,
16.3221761170896));
#34389=CARTESIAN_POINT('Ctrl Pts',(-3.93355225073649,1.04098512265698,16.2799598444988));
#34390=CARTESIAN_POINT('Ctrl Pts',(-3.50650185007344,2.09245600266764,16.237743571908));
#34391=CARTESIAN_POINT('Ctrl Pts',(-2.76293020390983,2.82077853336478,16.1955272993172));
#34392=CARTESIAN_POINT('Ctrl Pts',(-1.83005502901329,3.73452236922869,16.1425633208226));
#34393=CARTESIAN_POINT('Ctrl Pts',(-0.398979196739877,4.13963456552086,
16.089599342328));
#34394=CARTESIAN_POINT('Ctrl Pts',(0.87442396179839,3.85044901031056,16.0366353638333));
#34395=CARTESIAN_POINT('Ctrl Pts',(2.14782712033666,3.56126345510026,15.9836713853387));
#34396=CARTESIAN_POINT('Ctrl Pts',(3.26355760513978,2.57778014838748,15.9307074068441));
#34397=CARTESIAN_POINT('Ctrl Pts',(3.7102673428296,1.35073723969577,15.8777434283495));
#34398=CARTESIAN_POINT('Ctrl Pts',(4.15697708051941,0.123694331004073,15.8247794498548));
#34399=CARTESIAN_POINT('Ctrl Pts',(3.93466607109594,-1.34690817966655,15.7718154713602));
#34400=CARTESIAN_POINT('Ctrl Pts',(3.14522120203587,-2.38708157301605,15.7188514928656));
#34401=CARTESIAN_POINT('Ctrl Pts',(2.3557763329758,-3.42725496636555,15.665887514371));
#34402=CARTESIAN_POINT('Ctrl Pts',(0.999197604279134,-4.03699924239392,
15.6129235358763));
#34403=CARTESIAN_POINT('Ctrl Pts',(-0.302784262564327,-3.93686379448313,
15.5599595573817));
#34404=CARTESIAN_POINT('Ctrl Pts',(-1.60476612940779,-3.83672834657235,
15.5069955788871));
#34405=CARTESIAN_POINT('Ctrl Pts',(-2.85215113439804,-3.02671317472241,
15.4540316003925));
#34406=CARTESIAN_POINT('Ctrl Pts',(-3.47325290008964,-1.8780546152835,15.4010676218978));
#34407=CARTESIAN_POINT('Ctrl Pts',(-3.78163641109193,-1.30773364846388,
15.3747704536284));
#34408=CARTESIAN_POINT('Ctrl Pts',(-3.9356269389069,-0.653929427477854,
15.348473285359));
#34409=CARTESIAN_POINT('Ctrl Pts',(-3.935515150562,-7.56757525427476E-5,
15.3221761170896));
#34410=CARTESIAN_POINT('Ctrl Pts',(-3.93554762371472,0.000453016733568931,
15.1778238829104));
#34411=CARTESIAN_POINT('Ctrl Pts',(-3.93484541553788,-0.685806715529583,
15.2054249731855));
#34412=CARTESIAN_POINT('Ctrl Pts',(-3.76434547901772,-1.37239299857592,
15.2330260634607));
#34413=CARTESIAN_POINT('Ctrl Pts',(-3.42606065206783,-1.96285227530577,
15.2606271537358));
#34414=CARTESIAN_POINT('Ctrl Pts',(-2.77662492673475,-3.09640991110095,
15.313615442464));
#34415=CARTESIAN_POINT('Ctrl Pts',(-1.5088024710418,-3.87568257532879,15.3666037311923));
#34416=CARTESIAN_POINT('Ctrl Pts',(-0.204134723598678,-3.94322325781103,
15.4195920199205));
#34417=CARTESIAN_POINT('Ctrl Pts',(1.10053302384446,-4.01076394029327,15.4725803086488));
#34418=CARTESIAN_POINT('Ctrl Pts',(2.44204606303776,-3.36657264102987,15.525568597377));
#34419=CARTESIAN_POINT('Ctrl Pts',(3.2050615916644,-2.30613547736428,15.5785568861053));
#34420=CARTESIAN_POINT('Ctrl Pts',(3.96807712029102,-1.24569831369873,15.6315451748335));
#34421=CARTESIAN_POINT('Ctrl Pts',(4.15259513835105,0.230984714368973,15.6845334635618));
#34422=CARTESIAN_POINT('Ctrl Pts',(3.67397850032763,1.44656926050946,15.73752175229));
#34423=CARTESIAN_POINT('Ctrl Pts',(3.1953618623042,2.66215380664994,15.7905100410183));
#34424=CARTESIAN_POINT('Ctrl Pts',(2.05361056819728,3.6166398708632,15.8434983297465));
#34425=CARTESIAN_POINT('Ctrl Pts',(0.772438082086977,3.87221126175501,15.8964866184748));
#34426=CARTESIAN_POINT('Ctrl Pts',(-0.508734404023323,4.12778265264681,
15.949474907203));
#34427=CARTESIAN_POINT('Ctrl Pts',(-1.92932808213704,3.68443937021718,16.0024631959313));
#34428=CARTESIAN_POINT('Ctrl Pts',(-2.83772640488938,2.74553992819521,16.0554514846595));
#34429=CARTESIAN_POINT('Ctrl Pts',(-3.53701854402849,2.02276778870165,16.0962422840765));
#34430=CARTESIAN_POINT('Ctrl Pts',(-3.93278162022236,1.00632704174549,16.1370330834934));
#34431=CARTESIAN_POINT('Ctrl Pts',(-3.94210945089404,-0.00361990150021516,
16.1778238829104));
#34432=CARTESIAN_POINT('Origin',(0.,0.,0.));
#34433=CARTESIAN_POINT('',(-3.94714763575412,0.00206509481356407,17.3221761170896));
#34434=CARTESIAN_POINT('',(-3.94786894067556,0.00143683566665543,17.1778238829104));
#34435=CARTESIAN_POINT('',(-3.942,-4.82755768223887E-16,0.));
#34436=CARTESIAN_POINT('Ctrl Pts',(-3.94714763575412,0.00206509481356407,
17.3221761170896));
#34437=CARTESIAN_POINT('Ctrl Pts',(-3.94790115726501,0.120559580499713,
17.3173743606278));
#34438=CARTESIAN_POINT('Ctrl Pts',(-3.94302847934562,0.238991236972465,
17.3125726041661));
#34439=CARTESIAN_POINT('Ctrl Pts',(-3.93232775304421,0.356893945881719,
17.3077708477043));
#34440=CARTESIAN_POINT('Ctrl Pts',(-3.81429739431669,1.6573756735258,17.2548068692097));
#34441=CARTESIAN_POINT('Ctrl Pts',(-2.98720523271932,2.89350369502107,17.201842890715));
#34442=CARTESIAN_POINT('Ctrl Pts',(-1.83011412357382,3.49875079716524,17.1488789122204));
#34443=CARTESIAN_POINT('Ctrl Pts',(-0.67302301442832,4.10399789930941,17.0959149337258));
#34444=CARTESIAN_POINT('Ctrl Pts',(0.814067042265299,4.07836408210249,17.0429509552312));
#34445=CARTESIAN_POINT('Ctrl Pts',(1.94961095493928,3.43359752597032,16.9899869767366));
#34446=CARTESIAN_POINT('Ctrl Pts',(3.08515486761327,2.78883096983815,16.9370229982419));
#34447=CARTESIAN_POINT('Ctrl Pts',(3.86915263626762,1.52493167478073,16.8840590197473));
#34448=CARTESIAN_POINT('Ctrl Pts',(3.94229190545934,0.221154647517415,16.8310950412527));
#34449=CARTESIAN_POINT('Ctrl Pts',(4.01543117465106,-1.08262237974594,16.7781310627581));
#34450=CARTESIAN_POINT('Ctrl Pts',(3.37771194438013,-2.42627713921516,16.7251670842634));
#34451=CARTESIAN_POINT('Ctrl Pts',(2.32140596324251,-3.19400206634104,16.6722031057688));
#34452=CARTESIAN_POINT('Ctrl Pts',(1.26509998210492,-3.96172699346691,16.6192391272742));
#34453=CARTESIAN_POINT('Ctrl Pts',(-0.209792749899407,-4.15352208824943,
16.5662751487796));
#34454=CARTESIAN_POINT('Ctrl Pts',(-1.42731727122521,-3.68148614736372,
16.5133111702849));
#34455=CARTESIAN_POINT('Ctrl Pts',(-2.64484179255099,-3.20945020647802,
16.4603471917903));
#34456=CARTESIAN_POINT('Ctrl Pts',(-3.60499810319833,-2.07358322992414,
16.4073832132957));
#34457=CARTESIAN_POINT('Ctrl Pts',(-3.86773899976216,-0.794462003929412,
16.3544192348011));
#34458=CARTESIAN_POINT('Ctrl Pts',(-3.92105564940663,-0.534896556939351,
16.3436715288973));
#34459=CARTESIAN_POINT('Ctrl Pts',(-3.94565379003534,-0.269432117224103,
16.3329238229934));
#34460=CARTESIAN_POINT('Ctrl Pts',(-3.94319808732824,-0.00351593218956836,
16.3221761170896));
#34461=CARTESIAN_POINT('Ctrl Pts',(-3.94210945089404,-0.00361990150021516,
16.1778238829104));
#34462=CARTESIAN_POINT('Ctrl Pts',(-3.94489871015204,-0.305619794154464,
16.1900213722217));
#34463=CARTESIAN_POINT('Ctrl Pts',(-3.91313437834161,-0.607039035223508,
16.202218861533));
#34464=CARTESIAN_POINT('Ctrl Pts',(-3.84459973154587,-0.899851960334574,
16.2144163508443));
#34465=CARTESIAN_POINT('Ctrl Pts',(-3.54687176805904,-2.17188880522799,
16.2674046395725));
#34466=CARTESIAN_POINT('Ctrl Pts',(-2.55521287369446,-3.2815068934005,16.3203929283008));
#34467=CARTESIAN_POINT('Ctrl Pts',(-1.32449016131116,-3.71973204127804,
16.373381217029));
#34468=CARTESIAN_POINT('Ctrl Pts',(-0.0937674489278181,-4.15795718915558,
16.4263695057573));
#34469=CARTESIAN_POINT('Ctrl Pts',(1.37601908147424,-3.9247893967381,16.4793577944855));
#34470=CARTESIAN_POINT('Ctrl Pts',(2.4106884596013,-3.12718112636055,16.5323460832138));
#34471=CARTESIAN_POINT('Ctrl Pts',(3.44535783772833,-2.32957285598302,16.585334371942));
#34472=CARTESIAN_POINT('Ctrl Pts',(4.04491006358037,-0.967524107645474,
16.6383226606703));
#34473=CARTESIAN_POINT('Ctrl Pts',(3.93433465569921,0.334202727823592,16.6913109493985));
#34474=CARTESIAN_POINT('Ctrl Pts',(3.82375924781804,1.63592956329268,16.7442992381268));
#34475=CARTESIAN_POINT('Ctrl Pts',(3.00305620620361,2.87733448589332,16.797287526855));
#34476=CARTESIAN_POINT('Ctrl Pts',(1.84867637012666,3.48899359770921,16.8502758155833));
#34477=CARTESIAN_POINT('Ctrl Pts',(0.694296534049695,4.10065270952511,16.9032641043115));
#34478=CARTESIAN_POINT('Ctrl Pts',(-0.793760096489806,4.08256601055629,
16.9562523930398));
#34479=CARTESIAN_POINT('Ctrl Pts',(-1.93293218195181,3.44302974519471,17.009240681768));
#34480=CARTESIAN_POINT('Ctrl Pts',(-3.0721042674138,2.80349347983313,17.0622289704962));
#34481=CARTESIAN_POINT('Ctrl Pts',(-3.86239180779829,1.54250764807881,17.1152172592245));
#34482=CARTESIAN_POINT('Ctrl Pts',(-3.94129534500935,0.238477776172487,
17.1682055479527));
#34483=CARTESIAN_POINT('Ctrl Pts',(-3.94606948578935,0.159576089253736,
17.1714116596053));
#34484=CARTESIAN_POINT('Ctrl Pts',(-3.9482392631182,0.0805168189138495,
17.1746177712579));
#34485=CARTESIAN_POINT('Ctrl Pts',(-3.94786894067556,0.00143683566665543,
17.1778238829104));
#34486=CARTESIAN_POINT('Origin',(0.,0.,0.));
#34487=CARTESIAN_POINT('',(-3.93691309430117,0.00231896033839218,18.3221761170896));
#34488=CARTESIAN_POINT('',(-3.93777174659584,0.00283174072808758,18.1778238829104));
#34489=CARTESIAN_POINT('',(-3.942,-4.82755768223887E-16,0.));
#34490=CARTESIAN_POINT('Ctrl Pts',(-3.93691309430117,0.00231896033839218,
18.3221761170896));
#34491=CARTESIAN_POINT('Ctrl Pts',(-3.93961914157867,0.507883428428715,
18.3018248982623));
#34492=CARTESIAN_POINT('Ctrl Pts',(-3.84930447301574,1.01251781158405,18.2814736794349));
#34493=CARTESIAN_POINT('Ctrl Pts',(-3.66151008646525,1.47780876052409,18.2611224606075));
#34494=CARTESIAN_POINT('Ctrl Pts',(-3.17277582759625,2.68872688893964,18.2081584821129));
#34495=CARTESIAN_POINT('Ctrl Pts',(-2.02381253743022,3.63317238083008,18.1551945036183));
#34496=CARTESIAN_POINT('Ctrl Pts',(-0.741199145924524,3.87829842483136,
18.1022305251237));
#34497=CARTESIAN_POINT('Ctrl Pts',(0.541414245581171,4.12342446883263,18.049266546629));
#34498=CARTESIAN_POINT('Ctrl Pts',(1.95767773842654,3.66923106494473,17.9963025681344));
#34499=CARTESIAN_POINT('Ctrl Pts',(2.8585066133837,2.72387862930978,17.9433385896398));
#34500=CARTESIAN_POINT('Ctrl Pts',(3.75933548834084,1.77852619367486,17.8903746111452));
#34501=CARTESIAN_POINT('Ctrl Pts',(4.14472974540982,0.342014726292911,17.8374106326505));
#34502=CARTESIAN_POINT('Ctrl Pts',(3.83806015958749,-0.927291247319836,
17.7844466541559));
#34503=CARTESIAN_POINT('Ctrl Pts',(3.53139057376515,-2.19659722093258,17.7314826756613));
#34504=CARTESIAN_POINT('Ctrl Pts',(2.53265714505146,-3.29869770077617,17.6785186971667));
#34505=CARTESIAN_POINT('Ctrl Pts',(1.29958727405717,-3.72849135215269,17.625554718672));
#34506=CARTESIAN_POINT('Ctrl Pts',(0.0665174030628353,-4.15828500352923,
17.5725907401774));
#34507=CARTESIAN_POINT('Ctrl Pts',(-1.40088891021208,-3.91577182643871,
17.5196267616828));
#34508=CARTESIAN_POINT('Ctrl Pts',(-2.43010778892075,-3.11209752099697,
17.4666627831882));
#34509=CARTESIAN_POINT('Ctrl Pts',(-3.36601686459191,-2.38128496799525,
17.4185005611553));
#34510=CARTESIAN_POINT('Ctrl Pts',(-3.93958972010326,-1.18644951952042,
17.3703383391225));
#34511=CARTESIAN_POINT('Ctrl Pts',(-3.94714763575412,0.00206509481356407,
17.3221761170896));
#34512=CARTESIAN_POINT('Ctrl Pts',(-3.94786894067556,0.00143683566665543,
17.1778238829104));
#34513=CARTESIAN_POINT('Ctrl Pts',(-3.94211884229706,-1.22645980543112,
17.2276060599861));
#34514=CARTESIAN_POINT('Ctrl Pts',(-3.32396017207549,-2.45935025115224,
17.2773882370618));
#34515=CARTESIAN_POINT('Ctrl Pts',(-2.33396838579359,-3.18485042355784,
17.3271704141375));
#34516=CARTESIAN_POINT('Ctrl Pts',(-1.28021835532917,-3.95707483932351,
17.3801587028657));
#34517=CARTESIAN_POINT('Ctrl Pts',(0.194801239637294,-4.15444975879655,
17.433146991594));
#34518=CARTESIAN_POINT('Ctrl Pts',(1.41450905809659,-3.68644066422928,17.4861352803222));
#34519=CARTESIAN_POINT('Ctrl Pts',(2.63421687655591,-3.21843156966201,17.5391235690505));
#34520=CARTESIAN_POINT('Ctrl Pts',(3.59861291850804,-2.08503846105438,17.5921118577787));
#34521=CARTESIAN_POINT('Ctrl Pts',(3.86533535394433,-0.806140960297021,
17.645100146507));
#34522=CARTESIAN_POINT('Ctrl Pts',(4.13205778938061,0.472756540460342,17.6980884352352));
#34523=CARTESIAN_POINT('Ctrl Pts',(3.70110661830104,1.89715843336744,17.7510767239635));
#34524=CARTESIAN_POINT('Ctrl Pts',(2.77015617820835,2.81370136913189,17.8040650126917));
#34525=CARTESIAN_POINT('Ctrl Pts',(1.83920573811566,3.73024430489631,17.85705330142));
#34526=CARTESIAN_POINT('Ctrl Pts',(0.408256029009864,4.13892828351809,17.9100415901482));
#34527=CARTESIAN_POINT('Ctrl Pts',(-0.866326161571161,3.85229277549071,
17.9630298788765));
#34528=CARTESIAN_POINT('Ctrl Pts',(-2.14090835215219,3.56565726746332,18.0160181676047));
#34529=CARTESIAN_POINT('Ctrl Pts',(-3.25912302420844,2.58370227278676,18.069006456333));
#34530=CARTESIAN_POINT('Ctrl Pts',(-3.70805280027739,1.35684379228987,18.1219947450612));
#34531=CARTESIAN_POINT('Ctrl Pts',(-3.86571884909867,0.925965870186712,
18.1406044576776));
#34532=CARTESIAN_POINT('Ctrl Pts',(-3.94083233343714,0.464880467044514,
18.159214170294));
#34533=CARTESIAN_POINT('Ctrl Pts',(-3.93777174659584,0.00283174072808758,
18.1778238829104));
#34534=CARTESIAN_POINT('Origin',(0.,0.,0.));
#34535=CARTESIAN_POINT('',(-3.93868067607543,-0.00317875339515938,19.3221761170896));
#34536=CARTESIAN_POINT('',(-3.93757571821786,-0.00273443803236162,19.1778238829104));
#34537=CARTESIAN_POINT('',(-3.942,-4.82755768223887E-16,0.));
#34538=CARTESIAN_POINT('Ctrl Pts',(-3.93868067607543,-0.00317875339515938,
19.3221761170896));
#34539=CARTESIAN_POINT('Ctrl Pts',(-3.93194593082782,0.887659399123926,
19.2862754358966));
#34540=CARTESIAN_POINT('Ctrl Pts',(-3.63268362464169,1.78259416274328,19.2503747547037));
#34541=CARTESIAN_POINT('Ctrl Pts',(-3.07838529125365,2.47267443157326,19.2144740735107));
#34542=CARTESIAN_POINT('Ctrl Pts',(-2.26063353742526,3.4907441534662,19.1615100950161));
#34543=CARTESIAN_POINT('Ctrl Pts',(-0.887799511314515,4.06295099197559,
19.1085461165215));
#34544=CARTESIAN_POINT('Ctrl Pts',(0.410936134697139,3.92704804390779,19.0555821380269));
#34545=CARTESIAN_POINT('Ctrl Pts',(1.70967178070872,3.79114509584001,19.0026181595322));
#34546=CARTESIAN_POINT('Ctrl Pts',(2.93430904662124,2.94713236119515,18.9496541810376));
#34547=CARTESIAN_POINT('Ctrl Pts',(3.52358702306116,1.78182752725689,18.896690202543));
#34548=CARTESIAN_POINT('Ctrl Pts',(4.11286499950109,0.616522693318613,18.8437262240484));
#34549=CARTESIAN_POINT('Ctrl Pts',(4.06678368646841,-0.870074239913033,
18.7907622455538));
#34550=CARTESIAN_POINT('Ctrl Pts',(3.40646251285886,-1.99664418323714,18.7377982670591));
#34551=CARTESIAN_POINT('Ctrl Pts',(2.74614133924929,-3.1232141265613,18.6848342885645));
#34552=CARTESIAN_POINT('Ctrl Pts',(1.47158030506274,-3.88975707997784,18.6318703100699));
#34553=CARTESIAN_POINT('Ctrl Pts',(0.166920776077049,-3.94496036741581,
18.5789063315753));
#34554=CARTESIAN_POINT('Ctrl Pts',(-1.1377387529086,-4.00016365485379,18.5259423530806));
#34555=CARTESIAN_POINT('Ctrl Pts',(-2.47249677669342,-3.34402727631325,
18.472978374586));
#34556=CARTESIAN_POINT('Ctrl Pts',(-3.22562317479983,-2.27726370457266,
18.4200143960914));
#34557=CARTESIAN_POINT('Ctrl Pts',(-3.689363454866,-1.62040021025458,18.3874016364241));
#34558=CARTESIAN_POINT('Ctrl Pts',(-3.93257666264772,-0.807846398012042,
18.3547888767569));
#34559=CARTESIAN_POINT('Ctrl Pts',(-3.93691309430117,0.00231896033839218,
18.3221761170896));
#34560=CARTESIAN_POINT('Ctrl Pts',(-3.93777174659584,0.00283174072808758,
18.1778238829104));
#34561=CARTESIAN_POINT('Ctrl Pts',(-3.93211778407426,-0.850732074710112,
18.2122024590223));
#34562=CARTESIAN_POINT('Ctrl Pts',(-3.65968019788323,-1.70758341046428,
18.2465810351341));
#34563=CARTESIAN_POINT('Ctrl Pts',(-3.14806281812505,-2.38335501750349,
18.280959611246));
#34564=CARTESIAN_POINT('Ctrl Pts',(-2.3594981798221,-3.42493338048278,18.3339478999742));
#34565=CARTESIAN_POINT('Ctrl Pts',(-1.00272402313454,-4.03632814012413,
18.3869361887025));
#34566=CARTESIAN_POINT('Ctrl Pts',(0.299916680013111,-3.93709672618929,
18.4399244774307));
#34567=CARTESIAN_POINT('Ctrl Pts',(1.60255738316074,-3.83786531225445,18.492912766159));
#34568=CARTESIAN_POINT('Ctrl Pts',(2.85106463276846,-3.02800772474346,18.5459010548872));
#34569=CARTESIAN_POINT('Ctrl Pts',(3.47275674238136,-1.8790000677396,18.5988893436155));
#34570=CARTESIAN_POINT('Ctrl Pts',(4.09444885199426,-0.729992410735758,
18.6518776323437));
#34571=CARTESIAN_POINT('Ctrl Pts',(4.08932582161236,0.758165315760947,18.704865921072));
#34572=CARTESIAN_POINT('Ctrl Pts',(3.45973755002874,1.90286540019034,18.7578542098002));
#34573=CARTESIAN_POINT('Ctrl Pts',(2.83014927844509,3.04756548461977,18.8108424985285));
#34574=CARTESIAN_POINT('Ctrl Pts',(1.57609576565968,3.84880792698187,18.8638307872567));
#34575=CARTESIAN_POINT('Ctrl Pts',(0.272802730892003,3.93906833100647,18.916819075985));
#34576=CARTESIAN_POINT('Ctrl Pts',(-1.03049030387567,4.02932873503108,18.9698073647132));
#34577=CARTESIAN_POINT('Ctrl Pts',(-2.3830228606256,3.4086071007182,19.0227956534415));
#34578=CARTESIAN_POINT('Ctrl Pts',(-3.16439756014476,2.36162417155469,19.0757839421697));
#34579=CARTESIAN_POINT('Ctrl Pts',(-3.66596391218726,1.68956324002662,19.10979725575));
#34580=CARTESIAN_POINT('Ctrl Pts',(-3.93219107470607,0.841866122485371,
19.1438105693302));
#34581=CARTESIAN_POINT('Ctrl Pts',(-3.93757571821786,-0.00273443803236162,
19.1778238829104));
#34582=CARTESIAN_POINT('Origin',(0.,0.,0.));
#34583=CARTESIAN_POINT('',(-3.94834041879863,-0.000694519400761262,20.3221761170896));
#34584=CARTESIAN_POINT('',(-3.94772619292891,-0.00158826883248112,20.1778238829104));
#34585=CARTESIAN_POINT('',(-3.942,-4.82755768223887E-16,0.));
#34586=CARTESIAN_POINT('Ctrl Pts',(-3.94834041879863,-0.000694519400761262,
20.3221761170896));
#34587=CARTESIAN_POINT('Ctrl Pts',(-3.94525718695861,1.26793825937276,20.270725973531));
#34588=CARTESIAN_POINT('Ctrl Pts',(-3.27892645249503,2.53935361509062,20.2192758299725));
#34589=CARTESIAN_POINT('Ctrl Pts',(-2.23269077785256,3.25663426508529,20.167825686414));
#34590=CARTESIAN_POINT('Ctrl Pts',(-1.15567135789659,3.9950197056954,20.1148617079193));
#34591=CARTESIAN_POINT('Ctrl Pts',(0.323938040913112,4.14618172311401,20.0618977294247));
#34592=CARTESIAN_POINT('Ctrl Pts',(1.52802077187684,3.64084157388599,20.0089337509301));
#34593=CARTESIAN_POINT('Ctrl Pts',(2.73210350284056,3.13550142465798,19.9559697724355));
#34594=CARTESIAN_POINT('Ctrl Pts',(3.66065956595831,1.97365910878334,19.9030057939409));
#34595=CARTESIAN_POINT('Ctrl Pts',(3.88812440006945,0.687796115025536,19.8500418154462));
#34596=CARTESIAN_POINT('Ctrl Pts',(4.11558923418059,-0.598066878732264,
19.7970778369516));
#34597=CARTESIAN_POINT('Ctrl Pts',(3.64196283928513,-2.00795055037323,19.744113858457));
#34598=CARTESIAN_POINT('Ctrl Pts',(2.68431192455269,-2.89569410291512,19.6911498799624));
#34599=CARTESIAN_POINT('Ctrl Pts',(1.72666100982023,-3.78343765545704,19.6381859014677));
#34600=CARTESIAN_POINT('Ctrl Pts',(0.284985575250775,-4.14904108889985,
19.5852219229731));
#34601=CARTESIAN_POINT('Ctrl Pts',(-0.979983166843207,-3.82494546870956,
19.5322579444785));
#34602=CARTESIAN_POINT('Ctrl Pts',(-2.24495190893719,-3.50084984851927,
19.4792939659839));
#34603=CARTESIAN_POINT('Ctrl Pts',(-3.3332139585557,-2.48705517469588,19.4263299874892));
#34604=CARTESIAN_POINT('Ctrl Pts',(-3.74601024259189,-1.24819153514592,
19.3733660089946));
#34605=CARTESIAN_POINT('Ctrl Pts',(-3.87899998240626,-0.849069354397836,
19.3563027116929));
#34606=CARTESIAN_POINT('Ctrl Pts',(-3.94188164487581,-0.426586770708422,
19.3392394143913));
#34607=CARTESIAN_POINT('Ctrl Pts',(-3.93868067607543,-0.00317875339515938,
19.3221761170896));
#34608=CARTESIAN_POINT('Ctrl Pts',(-3.93757571821786,-0.00273443803236162,
19.1778238829104));
#34609=CARTESIAN_POINT('Ctrl Pts',(-3.9405796442122,-0.473910955663478,
19.1967988580584));
#34610=CARTESIAN_POINT('Ctrl Pts',(-3.86240471339523,-0.944123769370189,
19.2157738332064));
#34611=CARTESIAN_POINT('Ctrl Pts',(-3.69862306761181,-1.38234150992047,
19.2347488083545));
#34612=CARTESIAN_POINT('Ctrl Pts',(-3.24125703327134,-2.60608003821792,
19.2877370970827));
#34613=CARTESIAN_POINT('Ctrl Pts',(-2.11630812230202,-3.58031287079873,
19.340725385811));
#34614=CARTESIAN_POINT('Ctrl Pts',(-0.839782661227222,-3.85816610946462,
19.3937136745392));
#34615=CARTESIAN_POINT('Ctrl Pts',(0.436742799847613,-4.13601934813052,
19.4467019632675));
#34616=CARTESIAN_POINT('Ctrl Pts',(1.86484481102796,-3.71749299288145,19.4996902519957));
#34617=CARTESIAN_POINT('Ctrl Pts',(2.78946280422149,-2.79456220367197,19.552678540724));
#34618=CARTESIAN_POINT('Ctrl Pts',(3.714080797415,-1.8716314144625,19.6056668294522));
#34619=CARTESIAN_POINT('Ctrl Pts',(4.13521477262173,-0.444296191292658,
19.6586551181805));
#34620=CARTESIAN_POINT('Ctrl Pts',(3.85969347255442,0.832734618130101,19.7116434069087));
#34621=CARTESIAN_POINT('Ctrl Pts',(3.5841721724871,2.10976542755288,19.764631695637));
#34622=CARTESIAN_POINT('Ctrl Pts',(2.6119955971457,3.23649182322855,19.8176199843652));
#34623=CARTESIAN_POINT('Ctrl Pts',(1.38909445367046,3.69609215863147,19.8706082730935));
#34624=CARTESIAN_POINT('Ctrl Pts',(0.166193310195227,4.1556924940344,19.9235965618217));
#34625=CARTESIAN_POINT('Ctrl Pts',(-1.30743240141386,3.94816676916459,19.97658485055));
#34626=CARTESIAN_POINT('Ctrl Pts',(-2.35584070483748,3.16870560636289,20.0295731392782));
#34627=CARTESIAN_POINT('Ctrl Pts',(-3.33358701031412,2.44177958936821,20.0789900538223));
#34628=CARTESIAN_POINT('Ctrl Pts',(-3.94150300763008,1.21741613169822,20.1284069683663));
#34629=CARTESIAN_POINT('Ctrl Pts',(-3.94772619292891,-0.00158826883248112,
20.1778238829104));
#34630=CARTESIAN_POINT('Origin',(0.,0.,0.));
#34631=CARTESIAN_POINT('',(-3.94074044801927,0.00358039056613663,21.3221761170896));
#34632=CARTESIAN_POINT('',(-3.94238528018782,0.00360576479228953,21.1778238829104));
#34633=CARTESIAN_POINT('',(-3.942,-4.82755768223887E-16,0.));
#34634=CARTESIAN_POINT('Ctrl Pts',(-3.94074044801927,0.00358039056613663,
21.3221761170896));
#34635=CARTESIAN_POINT('Ctrl Pts',(-3.94382356658785,0.35139917714199,21.3081404896601));
#34636=CARTESIAN_POINT('Ctrl Pts',(-3.90159553870986,0.69848167363253,21.2941048622306));
#34637=CARTESIAN_POINT('Ctrl Pts',(-3.81110742902655,1.03248974691214,21.2800692348011));
#34638=CARTESIAN_POINT('Ctrl Pts',(-3.46964707612424,2.29288202357064,21.2271052563065));
#34639=CARTESIAN_POINT('Ctrl Pts',(-2.44098286072968,3.36709985140295,21.1741412778118));
#34640=CARTESIAN_POINT('Ctrl Pts',(-1.19655973690358,3.76282070551412,21.1211772993172));
#34641=CARTESIAN_POINT('Ctrl Pts',(0.0478633869225303,4.15854155962529,
21.0682133208226));
#34642=CARTESIAN_POINT('Ctrl Pts',(1.50804541918014,3.87576544001532,21.0152493423279));
#34643=CARTESIAN_POINT('Ctrl Pts',(2.51477344786687,3.04409088599763,20.9622853638333));
#34644=CARTESIAN_POINT('Ctrl Pts',(3.52150147655357,2.21241633197998,20.9093213853387));
#34645=CARTESIAN_POINT('Ctrl Pts',(4.07477550166942,0.831843343554564,20.8563574068441));
#34646=CARTESIAN_POINT('Ctrl Pts',(3.92102566715379,-0.464900607518139,
20.8033934283495));
#34647=CARTESIAN_POINT('Ctrl Pts',(3.76727583263815,-1.76164455859092,20.7504294498548));
#34648=CARTESIAN_POINT('Ctrl Pts',(2.90650213849103,-2.97455947231102,20.6974654713602));
#34649=CARTESIAN_POINT('Ctrl Pts',(1.73320395728241,-3.54775688148229,20.6445014928656));
#34650=CARTESIAN_POINT('Ctrl Pts',(0.559905776073817,-4.12095429065355,
20.5915375143709));
#34651=CARTESIAN_POINT('Ctrl Pts',(-0.925916892196226,-4.05443419527599,
20.5385735358763));
#34652=CARTESIAN_POINT('Ctrl Pts',(-2.04329981292238,-3.37868328145881,
20.4856095573817));
#34653=CARTESIAN_POINT('Ctrl Pts',(-3.16068273364853,-2.70293236764162,
20.4326455788871));
#34654=CARTESIAN_POINT('Ctrl Pts',(-3.90962590683076,-1.41795063538484,
20.3796816003925));
#34655=CARTESIAN_POINT('Ctrl Pts',(-3.94688277287076,-0.11265533735563,
20.3267176218978));
#34656=CARTESIAN_POINT('Ctrl Pts',(-3.94794766163145,-0.0753469311478099,
20.3252037869617));
#34657=CARTESIAN_POINT('Ctrl Pts',(-3.94843113776951,-0.0380219297583325,
20.3236899520257));
#34658=CARTESIAN_POINT('Ctrl Pts',(-3.94834041879863,-0.000694519400761262,
20.3221761170896));
#34659=CARTESIAN_POINT('Ctrl Pts',(-3.94772619292891,-0.00158826883248112,
20.1778238829104));
#34660=CARTESIAN_POINT('Ctrl Pts',(-3.94817594426456,-0.0896860565358013,
20.1813952570946));
#34661=CARTESIAN_POINT('Ctrl Pts',(-3.9454830581488,-0.177755853920253,
20.1849666312788));
#34662=CARTESIAN_POINT('Ctrl Pts',(-3.93956001409796,-0.265607871813588,
20.188538005463));
#34663=CARTESIAN_POINT('Ctrl Pts',(-3.85168012469672,-1.56906358645505,
20.2415262941912));
#34664=CARTESIAN_POINT('Ctrl Pts',(-3.05272945065598,-2.82457841500438,
20.2945145829195));
#34665=CARTESIAN_POINT('Ctrl Pts',(-1.90918116982076,-3.45625634279478,
20.3475028716477));
#34666=CARTESIAN_POINT('Ctrl Pts',(-0.765632888985623,-4.08793427058512,
20.4004911603759));
#34667=CARTESIAN_POINT('Ctrl Pts',(0.722512998643886,-4.09577529761664,
20.4534794491042));
#34668=CARTESIAN_POINT('Ctrl Pts',(1.87265421179595,-3.47618279865318,20.5064677378324));
#34669=CARTESIAN_POINT('Ctrl Pts',(3.0227954249481,-2.85659029968967,20.5594560265607));
#34670=CARTESIAN_POINT('Ctrl Pts',(3.8349319636227,-1.60956427473106,20.6124443152889));
#34671=CARTESIAN_POINT('Ctrl Pts',(3.9365423847422,-0.307106982824769,20.6654326040172));
#34672=CARTESIAN_POINT('Ctrl Pts',(4.03815280586171,0.995350309081448,20.7184208927454));
#34673=CARTESIAN_POINT('Ctrl Pts',(3.4292371094262,2.35323886793535,20.7714091814737));
#34674=CARTESIAN_POINT('Ctrl Pts',(2.38910073600262,3.14370455348999,20.8243974702019));
#34675=CARTESIAN_POINT('Ctrl Pts',(1.348964362579,3.93417023904466,20.8773857589302));
#34676=CARTESIAN_POINT('Ctrl Pts',(-0.12239268783275,4.15721305130006,20.9303740476584));
#34677=CARTESIAN_POINT('Ctrl Pts',(-1.35006905738725,3.71052478612394,20.9833623363867));
#34678=CARTESIAN_POINT('Ctrl Pts',(-2.57774542694174,3.26383652094782,21.0363506251149));
#34679=CARTESIAN_POINT('Ctrl Pts',(-3.56174111563901,2.14741717834018,21.0893389138432));
#34680=CARTESIAN_POINT('Ctrl Pts',(-3.85070407192177,0.873360631535526,
21.1423272025715));
#34681=CARTESIAN_POINT('Ctrl Pts',(-3.91522918325707,0.588865201437585,
21.1541594293511));
#34682=CARTESIAN_POINT('Ctrl Pts',(-3.94509829421553,0.296509601950098,
21.1659916561308));
#34683=CARTESIAN_POINT('Ctrl Pts',(-3.94238528018782,0.00360576479228953,
21.1778238829104));
#34684=CARTESIAN_POINT('Origin',(0.,0.,0.));
#34685=CARTESIAN_POINT('',(-3.93587951376728,-0.00124481178566893,22.3221761170896));
#34686=CARTESIAN_POINT('',(-3.93552176014147,-0.00030393483444853,22.1778238829104));
#34687=CARTESIAN_POINT('',(-3.942,-4.82755768223887E-16,0.));
#34688=CARTESIAN_POINT('Ctrl Pts',(-3.93587951376728,-0.00124481178566893,
22.3221761170896));
#34689=CARTESIAN_POINT('Ctrl Pts',(-3.9337992464037,0.734189273701127,22.2925910272945));
#34690=CARTESIAN_POINT('Ctrl Pts',(-3.73627980596971,1.47066093628887,22.2630059374994));
#34691=CARTESIAN_POINT('Ctrl Pts',(-3.35026562609245,2.08956860583238,22.2334208477043));
#34692=CARTESIAN_POINT('Ctrl Pts',(-2.65921324588212,3.19755282108702,22.1804568692097));
#34693=CARTESIAN_POINT('Ctrl Pts',(-1.36405277538343,3.92875538432108,22.1274928907151));
#34694=CARTESIAN_POINT('Ctrl Pts',(-0.0583683106578484,3.94805897547177,
22.0745289122204));
#34695=CARTESIAN_POINT('Ctrl Pts',(1.2473161540677,3.96736256662245,22.0215649337258));
#34696=CARTESIAN_POINT('Ctrl Pts',(2.56352461302015,3.27476718568979,21.9686009552312));
#34697=CARTESIAN_POINT('Ctrl Pts',(3.28702932421304,2.18769549882087,21.9156369767366));
#34698=CARTESIAN_POINT('Ctrl Pts',(4.01053403540591,1.10062381195199,21.8626729982419));
#34699=CARTESIAN_POINT('Ctrl Pts',(4.14133499883926,-0.380924180853135,
21.8097090197473));
#34700=CARTESIAN_POINT('Ctrl Pts',(3.6194845960222,-1.57794374981529,21.7567450412527));
#34701=CARTESIAN_POINT('Ctrl Pts',(3.09763419320511,-2.77496331877751,21.7037810627581));
#34702=CARTESIAN_POINT('Ctrl Pts',(1.92313242413752,-3.68745446389673,21.6508170842634));
#34703=CARTESIAN_POINT('Ctrl Pts',(0.634262969967227,-3.89721509840628,
21.5978531057688));
#34704=CARTESIAN_POINT('Ctrl Pts',(-0.654606484203027,-4.10697573291583,
21.5448891272742));
#34705=CARTESIAN_POINT('Ctrl Pts',(-2.05784362347597,-3.61400585681575,
21.4919251487796));
#34706=CARTESIAN_POINT('Ctrl Pts',(-2.93233394790743,-2.64423755602338,
21.4389611702849));
#34707=CARTESIAN_POINT('Ctrl Pts',(-3.57508147783416,-1.93146102491564,
21.4000328192198));
#34708=CARTESIAN_POINT('Ctrl Pts',(-3.93218930040467,-0.961108355901809,
21.3611044681547));
#34709=CARTESIAN_POINT('Ctrl Pts',(-3.94074044801927,0.00358039056613663,
21.3221761170896));
#34710=CARTESIAN_POINT('Ctrl Pts',(-3.94238528018782,0.00360576479228953,
21.1778238829104));
#34711=CARTESIAN_POINT('Ctrl Pts',(-3.93294859718036,-1.0152023337623,21.218979944859));
#34712=CARTESIAN_POINT('Ctrl Pts',(-3.52931423770067,-2.04064333351309,
21.2601360068076));
#34713=CARTESIAN_POINT('Ctrl Pts',(-2.81875615331693,-2.76501254901743,
21.3012920687562));
#34714=CARTESIAN_POINT('Ctrl Pts',(-1.90391505456104,-3.69763543176414,
21.3542803574844));
#34715=CARTESIAN_POINT('Ctrl Pts',(-0.480302633180845,-4.13118744625593,
21.4072686462127));
#34716=CARTESIAN_POINT('Ctrl Pts',(0.799079880925017,-3.86680126221775,
21.4602569349409));
#34717=CARTESIAN_POINT('Ctrl Pts',(2.07846239503088,-3.60241507817958,21.5132452236692));
#34718=CARTESIAN_POINT('Ctrl Pts',(3.21361500186243,-2.64009069561159,21.5662335123974));
#34719=CARTESIAN_POINT('Ctrl Pts',(3.68385102080785,-1.42123969585553,21.6192218011257));
#34720=CARTESIAN_POINT('Ctrl Pts',(4.15408703975328,-0.202388696099407,
21.6722100898539));
#34721=CARTESIAN_POINT('Ctrl Pts',(3.95940647081237,1.27298892084472,21.7251983785822));
#34722=CARTESIAN_POINT('Ctrl Pts',(3.18910793065139,2.32814760557936,21.7781866673104));
#34723=CARTESIAN_POINT('Ctrl Pts',(2.41880939049046,3.38330629031394,21.8311749560387));
#34724=CARTESIAN_POINT('Ctrl Pts',(1.07289287910942,4.01824604283911,21.8841632447669));
#34725=CARTESIAN_POINT('Ctrl Pts',(-0.231278918613751,3.94172434024104,
21.9371515334952));
#34726=CARTESIAN_POINT('Ctrl Pts',(-1.53545071633696,3.86520263764296,21.9901398222234));
#34727=CARTESIAN_POINT('Ctrl Pts',(-2.79787780040235,3.07721947992169,22.0431281109517));
#34728=CARTESIAN_POINT('Ctrl Pts',(-3.43949362875525,1.93921737114795,22.0961163996799));
#34729=CARTESIAN_POINT('Ctrl Pts',(-3.76928231599023,1.35428756589898,22.1233522274234));
#34730=CARTESIAN_POINT('Ctrl Pts',(-3.93505699138564,0.676885190519015,
22.1505880551669));
#34731=CARTESIAN_POINT('Ctrl Pts',(-3.93552176014147,-0.00030393483444853,
22.1778238829104));
#34732=CARTESIAN_POINT('Origin',(0.,0.,0.));
#34733=CARTESIAN_POINT('',(-3.94525314071248,-0.00295827654940184,23.3221761170896));
#34734=CARTESIAN_POINT('',(-3.94350653563855,-0.00347714007584369,23.1778238829104));
#34735=CARTESIAN_POINT('',(-3.942,-4.82755768223887E-16,0.));
#34736=CARTESIAN_POINT('Ctrl Pts',(-3.94525314071248,-0.00295827654940184,
23.3221761170896));
#34737=CARTESIAN_POINT('Ctrl Pts',(-3.93582062597525,1.11220231279806,23.2770415649289));
#34738=CARTESIAN_POINT('Ctrl Pts',(-3.44025122786987,2.23463092251658,23.2319070127682));
#34739=CARTESIAN_POINT('Ctrl Pts',(-2.60368934111206,2.9683990932166,23.1867724606075));
#34740=CARTESIAN_POINT('Ctrl Pts',(-1.62201025804696,3.82945298103697,23.1338084821129));
#34741=CARTESIAN_POINT('Ctrl Pts',(-0.170774803008089,4.15531037113838,
23.0808445036183));
#34742=CARTESIAN_POINT('Ctrl Pts',(1.08481479710351,3.79655919604497,23.0278805251236));
#34743=CARTESIAN_POINT('Ctrl Pts',(2.34040439721512,3.43780802095157,22.974916546629));
#34744=CARTESIAN_POINT('Ctrl Pts',(3.40034814239945,2.39444828066336,22.9219525681344));
#34745=CARTESIAN_POINT('Ctrl Pts',(3.77891236751962,1.14469612557038,22.8689885896398));
#34746=CARTESIAN_POINT('Ctrl Pts',(4.15747659263979,-0.105056029522605,
22.8160246111452));
#34747=CARTESIAN_POINT('Ctrl Pts',(3.85466129769578,-1.56120059942036,22.7630606326505));
#34748=CARTESIAN_POINT('Ctrl Pts',(3.00922455792002,-2.55639398676302,22.7100966541559));
#34749=CARTESIAN_POINT('Ctrl Pts',(2.16378781814425,-3.55158737410568,22.6571326756613));
#34750=CARTESIAN_POINT('Ctrl Pts',(0.77572963353673,-4.08582957889326,22.6041686971666));
#34751=CARTESIAN_POINT('Ctrl Pts',(-0.518779131279689,-3.91426327466899,
22.551204718672));
#34752=CARTESIAN_POINT('Ctrl Pts',(-1.81328789609611,-3.74269697044473,
22.4982407401774));
#34753=CARTESIAN_POINT('Ctrl Pts',(-3.01424724112142,-2.86532215720863,
22.4452767616828));
#34754=CARTESIAN_POINT('Ctrl Pts',(-3.57125476867308,-1.684251816953,22.3923127831882));
#34755=CARTESIAN_POINT('Ctrl Pts',(-3.81712408139379,-1.16291424345579,
22.3689338944886));
#34756=CARTESIAN_POINT('Ctrl Pts',(-3.9375233938263,-0.582403488318747,
22.3455550057891));
#34757=CARTESIAN_POINT('Ctrl Pts',(-3.93587951376728,-0.00124481178566893,
22.3221761170896));
#34758=CARTESIAN_POINT('Ctrl Pts',(-3.93552176014147,-0.00030393483444853,
22.1778238829104));
#34759=CARTESIAN_POINT('Ctrl Pts',(-3.93596121582331,-0.640610765021898,
22.2035763438952));
#34760=CARTESIAN_POINT('Ctrl Pts',(-3.78860721752551,-1.28072694143294,
22.2293288048799));
#34761=CARTESIAN_POINT('Ctrl Pts',(-3.49236428582461,-1.84230088118771,
22.2550812658647));
#34762=CARTESIAN_POINT('Ctrl Pts',(-2.88281454190065,-2.99779596492355,
22.3080695545929));
#34763=CARTESIAN_POINT('Ctrl Pts',(-1.64291048141232,-3.82076507256913,
22.3610578433212));
#34764=CARTESIAN_POINT('Ctrl Pts',(-0.341387846963322,-3.93371775192091,
22.4140461320494));
#34765=CARTESIAN_POINT('Ctrl Pts',(0.96013478748571,-4.04667043127269,22.4670344207777));
#34766=CARTESIAN_POINT('Ctrl Pts',(2.3232759958954,-3.44960668233064,22.5200227095059));
#34767=CARTESIAN_POINT('Ctrl Pts',(3.12277281794346,-2.41639589080571,22.5730109982342));
#34768=CARTESIAN_POINT('Ctrl Pts',(3.92226963999152,-1.38318509928078,22.6259992869624));
#34769=CARTESIAN_POINT('Ctrl Pts',(4.15812207567794,0.0861727348270178,
22.6789875756907));
#34770=CARTESIAN_POINT('Ctrl Pts',(3.72214521454942,1.31769395259273,22.7319758644189));
#34771=CARTESIAN_POINT('Ctrl Pts',(3.28616835342092,2.5492151703584,22.7849641531472));
#34772=CARTESIAN_POINT('Ctrl Pts',(2.17836219547751,3.54289977178199,22.8379524418754));
#34773=CARTESIAN_POINT('Ctrl Pts',(0.906871753871591,3.84295018391872,22.8909407306037));
#34774=CARTESIAN_POINT('Ctrl Pts',(-0.364618687734369,4.14300059605545,
22.9439290193319));
#34775=CARTESIAN_POINT('Ctrl Pts',(-1.79979341300285,3.74941681890528,22.9969173080602));
#34776=CARTESIAN_POINT('Ctrl Pts',(-2.74035137198678,2.84273547234742,23.0499055967884));
#34777=CARTESIAN_POINT('Ctrl Pts',(-3.49721397313409,2.11313322315816,23.0925450254957));
#34778=CARTESIAN_POINT('Ctrl Pts',(-3.9337951138205,1.05128255440302,23.1351844542031));
#34779=CARTESIAN_POINT('Ctrl Pts',(-3.94350653563855,-0.00347714007584369,
23.1778238829104));
#34780=CARTESIAN_POINT('Origin',(0.,0.,-1.84858989190503));
#34781=CARTESIAN_POINT('',(-3.37453254114594,-0.00253033205341837,23.651410108095));
#34782=CARTESIAN_POINT('',(-3.37610896110192,0.00188753811008129,23.848589891905));
#34783=CARTESIAN_POINT('',(-3.37175,2.08693528006523E-13,-1.84858989190503));
#34784=CARTESIAN_POINT('',(-3.33611311329475,0.488924695431507,24.62825));
#34785=CARTESIAN_POINT('Ctrl Pts',(-3.37453254114594,-0.00253033205341877,
23.651410108095));
#34786=CARTESIAN_POINT('Ctrl Pts',(-3.37593208671392,-0.167991834513083,
23.6592395344289));
#34787=CARTESIAN_POINT('Ctrl Pts',(-3.28964411790747,-1.45130369571974,
23.7200329392575));
#34788=CARTESIAN_POINT('Ctrl Pts',(-1.64345961820725,-3.63211696072943,
23.8337903225806));
#34789=CARTESIAN_POINT('Ctrl Pts',(2.163389782855,-3.34808861530533,23.9926822580645));
#34790=CARTESIAN_POINT('Ctrl Pts',(3.98513370400483,0.0032270738820094,
24.1515741935484));
#34791=CARTESIAN_POINT('Ctrl Pts',(2.15811323746268,3.35470758430291,24.3104661290323));
#34792=CARTESIAN_POINT('Ctrl Pts',(-1.65524532662936,3.62504834974875,24.4693580645161));
#34793=CARTESIAN_POINT('Ctrl Pts',(-3.1734075349997,1.59912472915632,24.5752860215054));
#34794=CARTESIAN_POINT('Ctrl Pts',(-3.33611311329483,0.488924695430968,
24.62825));
#34795=CARTESIAN_POINT('',(-0.624728334461187,3.31336876465952,24.62825));
#34796=CARTESIAN_POINT('Origin',(0.,0.,24.62825));
#34797=CARTESIAN_POINT('Ctrl Pts',(-3.37610896110192,0.00188753811008135,
23.848589891905));
#34798=CARTESIAN_POINT('Ctrl Pts',(-3.36932955763165,-1.01002015324007,
23.8965234396903));
#34799=CARTESIAN_POINT('Ctrl Pts',(-2.34697770975975,-3.15243101165571,
23.997445276204));
#34800=CARTESIAN_POINT('Ctrl Pts',(1.29650641132588,-3.76899081084458,24.1513554014457));
#34801=CARTESIAN_POINT('Ctrl Pts',(3.87454091099827,-0.951014904317504,
24.3103202676305));
#34802=CARTESIAN_POINT('Ctrl Pts',(2.88961752940844,2.74513957150359,24.4692851338152));
#34803=CARTESIAN_POINT('Ctrl Pts',(0.478408881098333,3.52136284087264,24.5752617112718));
#34804=CARTESIAN_POINT('Ctrl Pts',(-0.624728334461281,3.3133687646595,24.62825));
#34805=CARTESIAN_POINT('Origin',(0.,0.,-1.84858989190503));
#34806=CARTESIAN_POINT('',(-3.36651490374044,-0.00106473722420811,22.651410108095));
#34807=CARTESIAN_POINT('',(-3.37303860008607,-0.00297413674536479,22.848589891905));
#34808=CARTESIAN_POINT('',(-3.37175,2.08693528006523E-13,-1.84858989190503));
#34809=CARTESIAN_POINT('Ctrl Pts',(-3.36651490374044,-0.00106473722420751,
22.651410108095));
#34810=CARTESIAN_POINT('Ctrl Pts',(-3.36792097999337,-0.498152958330381,
22.6747889967945));
#34811=CARTESIAN_POINT('Ctrl Pts',(-3.03163608822923,-2.11956584279889,
22.7511318639887));
#34812=CARTESIAN_POINT('Ctrl Pts',(-0.52374905937927,-3.95173187129016,
22.8804387096774));
#34813=CARTESIAN_POINT('Ctrl Pts',(3.03803570770629,-2.58085580280275,23.0393306451613));
#34814=CARTESIAN_POINT('Ctrl Pts',(3.81506574631169,1.15563997615671,23.1982225806452));
#34815=CARTESIAN_POINT('Ctrl Pts',(1.095229123157,3.83292171460177,23.357114516129));
#34816=CARTESIAN_POINT('Ctrl Pts',(-2.44517403763626,3.03796695389969,23.508177025279));
#34817=CARTESIAN_POINT('Ctrl Pts',(-3.36646453466052,0.951311047229191,
23.6062755559343));
#34818=CARTESIAN_POINT('Ctrl Pts',(-3.37453254114594,-0.00253033205341877,
23.651410108095));
#34819=CARTESIAN_POINT('Ctrl Pts',(-3.37303860008607,-0.00297413674536527,
22.848589891905));
#34820=CARTESIAN_POINT('Ctrl Pts',(-3.3750546565899,-0.221938484280555,
22.8589387519259));
#34821=CARTESIAN_POINT('Ctrl Pts',(-3.25576106932785,-1.5598586434856,22.9222759006751));
#34822=CARTESIAN_POINT('Ctrl Pts',(-1.46739644894177,-3.70704069007233,
23.0386013381526));
#34823=CARTESIAN_POINT('Ctrl Pts',(2.32262200499063,-3.24046036848089,23.1975662043372));
#34824=CARTESIAN_POINT('Ctrl Pts',(3.98198637087808,0.198816238648098,23.3565310705221));
#34825=CARTESIAN_POINT('Ctrl Pts',(1.98816433058814,3.45581133218519,23.5154959367067));
#34826=CARTESIAN_POINT('Ctrl Pts',(-1.82925354411967,3.5422830008711,23.6744608028915));
#34827=CARTESIAN_POINT('Ctrl Pts',(-3.3238940749889,1.33320070540347,23.7854921212909));
#34828=CARTESIAN_POINT('Ctrl Pts',(-3.37682387017652,0.108596335481547,
23.8435351509621));
#34829=CARTESIAN_POINT('Ctrl Pts',(-3.37610896110192,0.00188753811008135,
23.848589891905));
#34830=CARTESIAN_POINT('Origin',(0.,0.,-1.84858989190503));
#34831=CARTESIAN_POINT('',(-3.37067265489827,0.00306245101284196,21.651410108095));
#34832=CARTESIAN_POINT('',(-3.36620890277955,-0.000259967599581801,21.848589891905));
#34833=CARTESIAN_POINT('',(-3.37175,2.08693528006523E-13,-1.84858989190503));
#34834=CARTESIAN_POINT('Ctrl Pts',(-3.37067265489827,0.00306245101284172,
21.651410108095));
#34835=CARTESIAN_POINT('Ctrl Pts',(-3.36335851690506,-0.822074352869367,
21.6903384591601));
#34836=CARTESIAN_POINT('Ctrl Pts',(-2.64233179033033,-2.78128712935246,
21.7822307887199));
#34837=CARTESIAN_POINT('Ctrl Pts',(0.640333691332285,-3.93451715048184,
21.9270870967742));
#34838=CARTESIAN_POINT('Ctrl Pts',(3.6541284705207,-1.59304681672573,22.0859790322581));
#34839=CARTESIAN_POINT('Ctrl Pts',(3.31849061020388,2.20863464806944,22.2448709677419));
#34840=CARTESIAN_POINT('Ctrl Pts',(-0.058926339166703,3.98584809986529,
22.4037629032258));
#34841=CARTESIAN_POINT('Ctrl Pts',(-2.89333741463138,2.3856381715614,22.5392759500101));
#34842=CARTESIAN_POINT('Ctrl Pts',(-3.36473556800141,0.627981401218202,
22.6218250182999));
#34843=CARTESIAN_POINT('Ctrl Pts',(-3.36651490374044,-0.00106473722420751,
22.651410108095));
#34844=CARTESIAN_POINT('Ctrl Pts',(-3.36620890277955,-0.00025996759958187,
21.848589891905));
#34845=CARTESIAN_POINT('Ctrl Pts',(-3.36658478677126,-0.547939966251195,
21.8743423528898));
#34846=CARTESIAN_POINT('Ctrl Pts',(-2.98121161418831,-2.22202824736231,
21.9530831026028));
#34847=CARTESIAN_POINT('Ctrl Pts',(-0.344707483447601,-3.97197126386073,
22.0848121410441));
#34848=CARTESIAN_POINT('Ctrl Pts',(3.15313982968432,-2.43989387002868,22.2437770072288));
#34849=CARTESIAN_POINT('Ctrl Pts',(3.75834184644668,1.33050740634341,22.4027418734136));
#34850=CARTESIAN_POINT('Ctrl Pts',(0.915689325102905,3.88032175554439,22.5617067395983));
#34851=CARTESIAN_POINT('Ctrl Pts',(-2.52724878310966,2.93612690507347,22.7103227457621));
#34852=CARTESIAN_POINT('Ctrl Pts',(-3.36473203323799,0.899203945410642,
22.8059504631977));
#34853=CARTESIAN_POINT('Ctrl Pts',(-3.37303860008607,-0.00297413674536527,
22.848589891905));
#34854=CARTESIAN_POINT('Origin',(0.,0.,-1.84858989190503));
#34855=CARTESIAN_POINT('',(-3.37717321336486,-0.000594050174885632,20.651410108095));
#34856=CARTESIAN_POINT('',(-3.37207954552848,0.0030841546013495,20.848589891905));
#34857=CARTESIAN_POINT('',(-3.37175,2.08693528006523E-13,-1.84858989190503));
#34858=CARTESIAN_POINT('Ctrl Pts',(-3.37717321336486,-0.000594050174885286,
20.651410108095));
#34859=CARTESIAN_POINT('Ctrl Pts',(-3.37725080892297,-0.0325216746987667,
20.6529239430311));
#34860=CARTESIAN_POINT('Ctrl Pts',(-3.36236902703727,-1.18141504466881,
20.7074017564618));
#34861=CARTESIAN_POINT('Ctrl Pts',(-2.06285714434356,-3.41102216294582,
20.8148435483871));
#34862=CARTESIAN_POINT('Ctrl Pts',(1.74979322227715,-3.58171404391184,20.9737354838709));
#34863=CARTESIAN_POINT('Ctrl Pts',(3.95855555351044,-0.46935037546761,21.1326274193549));
#34864=CARTESIAN_POINT('Ctrl Pts',(2.53884345747981,3.07322723010567,21.2915193548387));
#34865=CARTESIAN_POINT('Ctrl Pts',(-1.20801252978399,3.79883634829061,21.4504112903226));
#34866=CARTESIAN_POINT('Ctrl Pts',(-3.20089281760442,1.71770287259066,21.5703748747413));
#34867=CARTESIAN_POINT('Ctrl Pts',(-3.3733097693157,0.300565747216989,21.6373744806655));
#34868=CARTESIAN_POINT('Ctrl Pts',(-3.37067265489827,0.00306245101284172,
21.651410108095));
#34869=CARTESIAN_POINT('Ctrl Pts',(-3.37207954552848,0.00308415460134954,
20.848589891905));
#34870=CARTESIAN_POINT('Ctrl Pts',(-3.36400797375518,-0.868343092050458,
20.8897459538536));
#34871=CARTESIAN_POINT('Ctrl Pts',(-2.57426217007386,-2.87470778191459,
20.9838903045305));
#34872=CARTESIAN_POINT('Ctrl Pts',(0.806850527235046,-3.9044039261228,21.1310229439355));
#34873=CARTESIAN_POINT('Ctrl Pts',(3.71967457752779,-1.43506051902692,21.2899878101203));
#34874=CARTESIAN_POINT('Ctrl Pts',(3.22012038549849,2.35078763921597,21.448952676305));
#34875=CARTESIAN_POINT('Ctrl Pts',(-0.233528014234224,3.98005560769136,
21.6079175424898));
#34876=CARTESIAN_POINT('Ctrl Pts',(-2.94815289437509,2.2856379957105,21.7411299476898));
#34877=CARTESIAN_POINT('Ctrl Pts',(-3.36581136750493,0.578966930779549,
21.8213540641615));
#34878=CARTESIAN_POINT('Ctrl Pts',(-3.36620890277955,-0.00025996759958187,
21.848589891905));
#34879=CARTESIAN_POINT('Origin',(0.,0.,-1.84858989190503));
#34880=CARTESIAN_POINT('',(-3.36891084971013,-0.00271891470300727,19.651410108095));
#34881=CARTESIAN_POINT('',(-3.37664784145308,-0.00135850975013785,19.848589891905));
#34882=CARTESIAN_POINT('',(-3.37175,2.08693528006523E-13,-1.84858989190503));
#34883=CARTESIAN_POINT('Ctrl Pts',(-3.36891084971013,-0.00271891470300756,
19.651410108095));
#34884=CARTESIAN_POINT('Ctrl Pts',(-3.3716487661365,-0.364876698157186,
19.6684734053967));
#34885=CARTESIAN_POINT('Ctrl Pts',(-3.15091588331813,-1.84791316659487,
19.738500681193));
#34886=CARTESIAN_POINT('Ctrl Pts',(-0.989363022110038,-3.86155572506565,
19.8614919354839));
#34887=CARTESIAN_POINT('Ctrl Pts',(2.71000466929749,-2.92341008068914,20.0203838709678));
#34888=CARTESIAN_POINT('Ctrl Pts',(3.92533937020224,0.694379317983201,20.1792758064516));
#34889=CARTESIAN_POINT('Ctrl Pts',(1.54264613898669,3.6756896897871,20.3381677419355));
#34890=CARTESIAN_POINT('Ctrl Pts',(-2.21788792003282,3.29150051432633,20.4955458424833));
#34891=CARTESIAN_POINT('Ctrl Pts',(-3.37453600206181,1.08451822071036,20.5999599645364));
#34892=CARTESIAN_POINT('Ctrl Pts',(-3.37717321336486,-0.000594050174885286,
20.651410108095));
#34893=CARTESIAN_POINT('Ctrl Pts',(-3.37664784145308,-0.0013585097501378,
19.848589891905));
#34894=CARTESIAN_POINT('Ctrl Pts',(-3.37703253172857,-0.0767120652268113,
19.8521612660892));
#34895=CARTESIAN_POINT('Ctrl Pts',(-3.3405547692736,-1.26970315744226,19.9087209290016));
#34896=CARTESIAN_POINT('Ctrl Pts',(-1.92774697870435,-3.4898666651324,20.0182688806423));
#34897=CARTESIAN_POINT('Ctrl Pts',(1.89086481476229,-3.50998689564495,20.1772337468271));
#34898=CARTESIAN_POINT('Ctrl Pts',(3.97482324267393,-0.310093440809367,
20.3361986130118));
#34899=CARTESIAN_POINT('Ctrl Pts',(2.41233351706024,3.17427546962878,20.4951634791965));
#34900=CARTESIAN_POINT('Ctrl Pts',(-1.36319778790607,3.74660773920425,20.6541283453813));
#34901=CARTESIAN_POINT('Ctrl Pts',(-3.23443909431523,1.62353950510727,20.7719371496175));
#34902=CARTESIAN_POINT('Ctrl Pts',(-3.37440009475423,0.25361650187097,20.8367576651254));
#34903=CARTESIAN_POINT('Ctrl Pts',(-3.37207954552848,0.00308415460134954,
20.848589891905));
#34904=CARTESIAN_POINT('Origin',(0.,0.,-1.84858989190503));
#34905=CARTESIAN_POINT('',(-3.36739896644089,0.00198349937115513,18.651410108095));
#34906=CARTESIAN_POINT('',(-3.36796573513472,-0.00233887403243982,18.848589891905));
#34907=CARTESIAN_POINT('',(-3.37175,2.08693528006523E-13,-1.84858989190503));
#34908=CARTESIAN_POINT('Ctrl Pts',(-3.36739896644089,0.00198349937115483,
18.651410108095));
#34909=CARTESIAN_POINT('Ctrl Pts',(-3.36368984329845,-0.690983280694315,
18.6840228677623));
#34910=CARTESIAN_POINT('Ctrl Pts',(-2.81781374229535,-2.51470704523694,
18.7695996059241));
#34911=CARTESIAN_POINT('Ctrl Pts',(0.168518449156949,-3.98271933982683,
18.9081403225806));
#34912=CARTESIAN_POINT('Ctrl Pts',(3.43906728250426,-2.01575495384355,19.0670322580645));
#34913=CARTESIAN_POINT('Ctrl Pts',(3.55731284355299,1.79888219198906,19.2259241935484));
#34914=CARTESIAN_POINT('Ctrl Pts',(0.41486938743375,3.96463556949202,19.3848161290323));
#34915=CARTESIAN_POINT('Ctrl Pts',(-2.72954745140897,2.65402060505441,19.5266447672144));
#34916=CARTESIAN_POINT('Ctrl Pts',(-3.36315035318836,0.75925052739643,19.615509426902));
#34917=CARTESIAN_POINT('Ctrl Pts',(-3.36891084971013,-0.00271891470300756,
19.651410108095));
#34918=CARTESIAN_POINT('Ctrl Pts',(-3.36796573513472,-0.00233887403243996,
18.848589891905));
#34919=CARTESIAN_POINT('Ctrl Pts',(-3.37053511298134,-0.405354963155371,
18.867564867053));
#34920=CARTESIAN_POINT('Ctrl Pts',(-3.11694291466331,-1.93068155902232,
18.9395281309293));
#34921=CARTESIAN_POINT('Ctrl Pts',(-0.847949117405149,-3.89568479841959,
19.0644796835338));
#34922=CARTESIAN_POINT('Ctrl Pts',(2.81658890100978,-2.82173788950715,19.2234445497186));
#34923=CARTESIAN_POINT('Ctrl Pts',(3.89722701433046,0.840832535700663,19.3824094159033));
#34924=CARTESIAN_POINT('Ctrl Pts',(1.40260268563389,3.73203476143841,19.5413742820881));
#34925=CARTESIAN_POINT('Ctrl Pts',(-2.29379652508948,3.21148336255172,19.6967677740886));
#34926=CARTESIAN_POINT('Ctrl Pts',(-3.37132490258154,1.04130462761393,19.799172977361));
#34927=CARTESIAN_POINT('Ctrl Pts',(-3.37664784145308,-0.0013585097501378,
19.848589891905));
#34928=CARTESIAN_POINT('Origin',(0.,0.,-1.84858989190503));
#34929=CARTESIAN_POINT('',(-3.3761529784003,0.00176635805113218,17.651410108095));
#34930=CARTESIAN_POINT('',(-3.36813340603362,0.00242210091315795,17.848589891905));
#34931=CARTESIAN_POINT('',(-3.37175,2.08693528006523E-13,-1.84858989190503));
#34932=CARTESIAN_POINT('Ctrl Pts',(-3.3761529784003,0.00176635805113214,
17.651410108095));
#34933=CARTESIAN_POINT('Ctrl Pts',(-3.36968839136432,-1.01481764775316,
17.6995723301278));
#34934=CARTESIAN_POINT('Ctrl Pts',(-2.33957623769215,-3.16069067030928,
17.8006985306553));
#34935=CARTESIAN_POINT('Ctrl Pts',(1.31202620257783,-3.7641784032229,17.9547887096774));
#34936=CARTESIAN_POINT('Ctrl Pts',(3.87479594250582,-0.936166764781103,
18.1136806451613));
#34937=CARTESIAN_POINT('Ctrl Pts',(2.88586665310525,2.74995008464444,18.2725725806452));
#34938=CARTESIAN_POINT('Ctrl Pts',(-0.748293493014444,3.91541934610488,
18.431464516129));
#34939=CARTESIAN_POINT('Ctrl Pts',(-3.09142162050251,1.98937278233,18.5577436919457));
#34940=CARTESIAN_POINT('Ctrl Pts',(-3.36971355672701,0.434412975597321,
18.6310588892676));
#34941=CARTESIAN_POINT('Ctrl Pts',(-3.36739896644089,0.00198349937115483,
18.651410108095));
#34942=CARTESIAN_POINT('Ctrl Pts',(-3.36813340603362,0.00242210091315778,
17.848589891905));
#34943=CARTESIAN_POINT('Ctrl Pts',(-3.36329734613199,-0.727665112355139,
17.8829684680169));
#34944=CARTESIAN_POINT('Ctrl Pts',(-2.77110248260437,-2.59019431375764,
17.970335332857));
#34945=CARTESIAN_POINT('Ctrl Pts',(0.302833216085013,-3.97538297495793,
18.1106904864254));
#34946=CARTESIAN_POINT('Ctrl Pts',(3.5065275226793,-1.89727238082542,18.2696553526101));
#34947=CARTESIAN_POINT('Ctrl Pts',(3.49338172535042,1.92136979140851,18.4286202187948));
#34948=CARTESIAN_POINT('Ctrl Pts',(0.275455597698851,3.97737375262188,18.5875850849796));
#34949=CARTESIAN_POINT('Ctrl Pts',(-2.78089559275923,2.57471376007135,18.7275749760163));
#34950=CARTESIAN_POINT('Ctrl Pts',(-3.36336003453583,0.720081709408907,
18.8145765783248));
#34951=CARTESIAN_POINT('Ctrl Pts',(-3.36796573513472,-0.00233887403243996,
18.848589891905));
#34952=CARTESIAN_POINT('Origin',(0.,0.,-1.84858989190503));
#34953=CARTESIAN_POINT('',(-3.37277477193024,-0.0030073171892592,16.651410108095));
#34954=CARTESIAN_POINT('',(-3.37676993930056,0.00122898291704077,16.848589891905));
#34955=CARTESIAN_POINT('',(-3.37175,2.08693528006523E-13,-1.84858989190503));
#34956=CARTESIAN_POINT('Ctrl Pts',(-3.37277477193024,-0.0030073171892591,
16.651410108095));
#34957=CARTESIAN_POINT('Ctrl Pts',(-3.3748752325093,-0.230456048008689,
16.6621578139988));
#34958=CARTESIAN_POINT('Ctrl Pts',(-3.25015286697033,-1.5764664391,16.7258694983973));
#34959=CARTESIAN_POINT('Ctrl Pts',(-1.44097876042837,-3.71672329068694,
16.8425451612903));
#34960=CARTESIAN_POINT('Ctrl Pts',(2.34362517346463,-3.22457328244272,17.0014370967742));
#34961=CARTESIAN_POINT('Ctrl Pts',(3.980025336833,0.223271417131382,17.1603290322581));
#34962=CARTESIAN_POINT('Ctrl Pts',(1.96827154957251,3.46646201691059,17.3192209677419));
#34963=CARTESIAN_POINT('Ctrl Pts',(-1.84763096082072,3.53223889907763,17.4781129032258));
#34964=CARTESIAN_POINT('Ctrl Pts',(-3.32665838484882,1.32176305576882,17.5888426166768));
#34965=CARTESIAN_POINT('Ctrl Pts',(-3.3767974954359,0.103119423021283,17.6466083516332));
#34966=CARTESIAN_POINT('Ctrl Pts',(-3.3761529784003,0.00176635805113214,
17.651410108095));
#34967=CARTESIAN_POINT('Ctrl Pts',(-3.37676993930056,0.00122898291704094,
16.848589891905));
#34968=CARTESIAN_POINT('Ctrl Pts',(-3.37185165056191,-1.0490400428621,16.8983720689807));
#34969=CARTESIAN_POINT('Ctrl Pts',(-2.28032799824397,-3.22603625281427,
17.0011425347847));
#34970=CARTESIAN_POINT('Ctrl Pts',(1.42826443406275,-3.7222894112013,17.1569012893169));
#34971=CARTESIAN_POINT('Ctrl Pts',(3.90292376012977,-0.813980268166524,
17.3158661555016));
#34972=CARTESIAN_POINT('Ctrl Pts',(2.79709452794753,2.84106317354542,17.4748310216864));
#34973=CARTESIAN_POINT('Ctrl Pts',(-0.87475073969136,3.88975434928213,17.6337958878711));
#34974=CARTESIAN_POINT('Ctrl Pts',(-3.12356865319579,1.91496539554474,17.758382177944));
#34975=CARTESIAN_POINT('Ctrl Pts',(-3.37075124816507,0.397630825661392,
17.8299801792886));
#34976=CARTESIAN_POINT('Ctrl Pts',(-3.36813340603362,0.00242210091315778,
17.848589891905));
#34977=CARTESIAN_POINT('Origin',(0.,0.,-1.84858989190503));
#34978=CARTESIAN_POINT('',(-3.36620324934232,-6.47284927745773E-5,15.651410108095));
#34979=CARTESIAN_POINT('',(-3.37184361771993,-0.00309624629213801,15.848589891905));
#34980=CARTESIAN_POINT('',(-3.37175,2.08693528006523E-13,-1.84858989190503));
#34981=CARTESIAN_POINT('Ctrl Pts',(-3.36620324934232,-6.47284927745434E-5,
15.651410108095));
#34982=CARTESIAN_POINT('Ctrl Pts',(-3.36629886637731,-0.559331950050314,
15.6777072763644));
#34983=CARTESIAN_POINT('Ctrl Pts',(-2.969304704679,-2.24486717295088,15.7569684231284));
#34984=CARTESIAN_POINT('Ctrl Pts',(-0.30568234557457,-3.97454527098943,
15.8891935483871));
#34985=CARTESIAN_POINT('Ctrl Pts',(3.17532551476257,-2.40992939374543,16.048085483871));
#34986=CARTESIAN_POINT('Ctrl Pts',(3.74577996379122,1.36366574731522,16.2069774193548));
#34987=CARTESIAN_POINT('Ctrl Pts',(0.882793462927545,3.88730337243608,16.3658693548387));
#34988=CARTESIAN_POINT('Ctrl Pts',(-2.54098403241842,2.91809266432718,16.5140135844188));
#34989=CARTESIAN_POINT('Ctrl Pts',(-3.36452430274498,0.890396140872364,
16.6091938355042));
#34990=CARTESIAN_POINT('Ctrl Pts',(-3.37277477193024,-0.0030073171892591,
16.651410108095));
#34991=CARTESIAN_POINT('Ctrl Pts',(-3.37184361771993,-0.00309624629213769,
15.848589891905));
#34992=CARTESIAN_POINT('Ctrl Pts',(-3.37422938253555,-0.261408813023958,
15.8607873812163));
#34993=CARTESIAN_POINT('Ctrl Pts',(-3.22903130121081,-1.63922767409008,
15.9259731592558));
#34994=CARTESIAN_POINT('Ctrl Pts',(-1.33737014962086,-3.75590452983738,
16.0441472260236));
#34995=CARTESIAN_POINT('Ctrl Pts',(2.43413116992486,-3.15759136082396,16.2031120922084));
#34996=CARTESIAN_POINT('Ctrl Pts',(3.97259404474729,0.337452678146523,16.3620769583931));
#34997=CARTESIAN_POINT('Ctrl Pts',(1.86665380078734,3.52292227310739,16.5210418245779));
#34998=CARTESIAN_POINT('Ctrl Pts',(-1.95172895721992,3.47651144567355,16.6800066907626));
#34999=CARTESIAN_POINT('Ctrl Pts',(-3.34455787065121,1.25410828714709,16.7891893798717));
#35000=CARTESIAN_POINT('Ctrl Pts',(-3.37708669087234,0.0688692501706657,
16.8453837802525));
#35001=CARTESIAN_POINT('Ctrl Pts',(-3.37676993930056,0.00122898291704094,
16.848589891905));
#35002=CARTESIAN_POINT('Origin',(0.,0.,-1.84858989190503));
#35003=CARTESIAN_POINT('',(-3.37253669875649,0.00303677565441225,14.651410108095));
#35004=CARTESIAN_POINT('',(-3.36623102492646,0.000387483300791081,14.848589891905));
#35005=CARTESIAN_POINT('',(-3.37175,2.08693528006523E-13,-1.84858989190503));
#35006=CARTESIAN_POINT('Ctrl Pts',(-3.37253669875649,0.00303677565441206,
14.651410108095));
#35007=CARTESIAN_POINT('Ctrl Pts',(-3.36433888251516,-0.882704764956481,
14.69325673873));
#35008=CARTESIAN_POINT('Ctrl Pts',(-2.55272847437535,-2.90279523765218,
14.7880673478596));
#35009=CARTESIAN_POINT('Ctrl Pts',(0.8556871302199,-3.8933599040824,14.9358419354839));
#35010=CARTESIAN_POINT('Ctrl Pts',(3.73618765800463,-1.38973148187494,15.0947338709677));
#35011=CARTESIAN_POINT('Ctrl Pts',(3.19203969455987,2.38774671937678,15.2536258064516));
#35012=CARTESIAN_POINT('Ctrl Pts',(-0.277982160818163,3.97657864574653,
15.4125177419355));
#35013=CARTESIAN_POINT('Ctrl Pts',(-2.9610712487067,2.26071800063538,15.54511250915));
#35014=CARTESIAN_POINT('Ctrl Pts',(-3.3661062882817,0.567063743655371,15.6247432978698));
#35015=CARTESIAN_POINT('Ctrl Pts',(-3.36620324934232,-6.47284927745434E-5,
15.651410108095));
#35016=CARTESIAN_POINT('Ctrl Pts',(-3.36623102492646,0.000387483300790976,
14.848589891905));
#35017=CARTESIAN_POINT('Ctrl Pts',(-3.36563039823437,-0.58659786734821,
14.8761909821801));
#35018=CARTESIAN_POINT('Ctrl Pts',(-2.93982168940875,-2.30128717837213,
14.9567803611835));
#35019=CARTESIAN_POINT('Ctrl Pts',(-0.206119829211681,-3.98156908396121,
15.0903580289152));
#35020=CARTESIAN_POINT('Ctrl Pts',(3.23622917375625,-2.32856146349605,15.2493228950999));
#35021=CARTESIAN_POINT('Ctrl Pts',(3.70970605913983,1.46063640552025,15.4082877612846));
#35022=CARTESIAN_POINT('Ctrl Pts',(0.779949646731194,3.90986653262151,15.5672526274694));
#35023=CARTESIAN_POINT('Ctrl Pts',(-2.58561751919903,2.85952988987219,15.7140200043429));
#35024=CARTESIAN_POINT('Ctrl Pts',(-3.36386515169579,0.8607517004072,15.8077990924881));
#35025=CARTESIAN_POINT('Ctrl Pts',(-3.37184361771993,-0.00309624629213769,
15.848589891905));
#35026=CARTESIAN_POINT('Origin',(0.,0.,-1.84858989190503));
#35027=CARTESIAN_POINT('',(-3.37630962516523,-0.00164737155311467,13.651410108095));
#35028=CARTESIAN_POINT('',(-3.37326960455653,0.00293423317535069,13.848589891905));
#35029=CARTESIAN_POINT('',(-3.37175,2.08693528006523E-13,-1.84858989190503));
#35030=CARTESIAN_POINT('Ctrl Pts',(-3.37630962516523,-0.00164737155311456,
13.651410108095));
#35031=CARTESIAN_POINT('Ctrl Pts',(-3.3768714611022,-0.0951867578458431,
13.6558422226009));
#35032=CARTESIAN_POINT('Ctrl Pts',(-3.33090125004588,-1.30596569148795,
13.7132383156015));
#35033=CARTESIAN_POINT('Ctrl Pts',(-1.87219709398698,-3.51927973437849,
13.8235983870968));
#35034=CARTESIAN_POINT('Ctrl Pts',(1.94407109338865,-3.48009186536664,13.9824903225806));
#35035=CARTESIAN_POINT('Ctrl Pts',(3.97837307717912,-0.25099694483561,14.1413822580645));
#35036=CARTESIAN_POINT('Ctrl Pts',(2.36603559757979,3.20816573115008,14.3002741935484));
#35037=CARTESIAN_POINT('Ctrl Pts',(-1.41504740048591,3.7266731359107,14.4591661290323));
#35038=CARTESIAN_POINT('Ctrl Pts',(-3.24486867351568,1.59233323105557,14.5762114338811));
#35039=CARTESIAN_POINT('Ctrl Pts',(-3.37471460348768,0.238350746486947,
14.6402927602354));
#35040=CARTESIAN_POINT('Ctrl Pts',(-3.37253669875649,0.00303677565441206,
14.651410108095));
#35041=CARTESIAN_POINT('Ctrl Pts',(-3.37326960455653,0.00293423317535065,
13.848589891905));
#35042=CARTESIAN_POINT('Ctrl Pts',(-3.36494392394814,-0.906810168463347,
13.891594583144));
#35043=CARTESIAN_POINT('Ctrl Pts',(-2.51545460624217,-2.95119723051152,
13.9875875631112));
#35044=CARTESIAN_POINT('Ctrl Pts',(0.942385426660244,-3.87392403926152,
14.1365688318067));
#35045=CARTESIAN_POINT('Ctrl Pts',(3.76741231340739,-1.30460040439068,14.2955336979914));
#35046=CARTESIAN_POINT('Ctrl Pts',(3.1362669786623,2.46154569181692,14.4544985641762));
#35047=CARTESIAN_POINT('Ctrl Pts',(-0.372046531241306,3.96950363810656,
14.6134634303609));
#35048=CARTESIAN_POINT('Ctrl Pts',(-2.98916250729706,2.20635255558199,14.7448272062705));
#35049=CARTESIAN_POINT('Ctrl Pts',(-3.36678347516941,0.540290560949759,
14.8232026934519));
#35050=CARTESIAN_POINT('Ctrl Pts',(-3.36623102492646,0.000387483300790976,
14.848589891905));
#35051=CARTESIAN_POINT('Origin',(0.,0.,-1.84858989190503));
#35052=CARTESIAN_POINT('',(-3.36754256765694,-0.00208193686516585,12.651410108095));
#35053=CARTESIAN_POINT('',(-3.3758812610584,-0.00196014188030613,12.848589891905));
#35054=CARTESIAN_POINT('',(-3.37175,2.08693528006523E-13,-1.84858989190503));
#35055=CARTESIAN_POINT('Ctrl Pts',(-3.36754256765694,-0.00208193686516537,
12.651410108095));
#35056=CARTESIAN_POINT('Ctrl Pts',(-3.36993408573054,-0.426611763038696,
12.6713916849665));
#35057=CARTESIAN_POINT('Ctrl Pts',(-3.09838828538505,-1.97347045721629,
12.7443372403327));
#35058=CARTESIAN_POINT('Ctrl Pts',(-0.775556132376715,-3.9101105474236,
12.8702467741936));
#35059=CARTESIAN_POINT('Ctrl Pts',(2.86663624227273,-2.76999069710151,13.0291387096774));
#35060=CARTESIAN_POINT('Ctrl Pts',(3.88122465785174,0.909146282412278,13.1880306451613));
#35061=CARTESIAN_POINT('Ctrl Pts',(1.33822138229676,3.75494545093591,13.3469225806451));
#35062=CARTESIAN_POINT('Ctrl Pts',(-2.32626682514693,3.17552839905125,13.5013824016231));
#35063=CARTESIAN_POINT('Ctrl Pts',(-3.37015749501604,1.02261334351231,13.6028782441063));
#35064=CARTESIAN_POINT('Ctrl Pts',(-3.37630962516523,-0.00164737155311456,
13.651410108095));
#35065=CARTESIAN_POINT('Ctrl Pts',(-3.3758812610584,-0.00196014188030577,
12.848589891905));
#35066=CARTESIAN_POINT('Ctrl Pts',(-3.37667181942981,-0.11638712350615,
12.8540098953796));
#35067=CARTESIAN_POINT('Ctrl Pts',(-3.31942395404611,-1.34870119310656,
12.9124181875824));
#35068=CARTESIAN_POINT('Ctrl Pts',(-1.80499399926681,-3.5549084962852,13.0238147685134));
#35069=CARTESIAN_POINT('Ctrl Pts',(2.01200065152342,-3.44198069904803,13.1827796346982));
#35070=CARTESIAN_POINT('Ctrl Pts',(3.98321358718988,-0.171427165804589,
13.3417445008829));
#35071=CARTESIAN_POINT('Ctrl Pts',(2.30028118194861,3.25639129072706,13.5007093670677));
#35072=CARTESIAN_POINT('Ctrl Pts',(-1.49289753065309,3.69684118097057,13.6596742332524));
#35073=CARTESIAN_POINT('Ctrl Pts',(-3.26085313565002,1.54418744509758,13.7756344081982));
#35074=CARTESIAN_POINT('Ctrl Pts',(-3.37520242261949,0.214132631825097,
13.8386062944157));
#35075=CARTESIAN_POINT('Ctrl Pts',(-3.37326960455653,0.00293423317535065,
13.848589891905));
#35076=CARTESIAN_POINT('Origin',(0.,0.,-1.84858989190503));
#35077=CARTESIAN_POINT('',(-3.36871665678573,0.00265343926576773,11.651410108095));
#35078=CARTESIAN_POINT('',(-3.36722041330275,-0.00185992061757206,11.848589891905));
#35079=CARTESIAN_POINT('',(-3.37175,2.08693528006523E-13,-1.84858989190503));
#35080=CARTESIAN_POINT('Ctrl Pts',(-3.36871665678573,0.00265343926576761,
11.651410108095));
#35081=CARTESIAN_POINT('Ctrl Pts',(-3.36317444447066,-0.751580168678052,
11.6869411473321));
#35082=CARTESIAN_POINT('Ctrl Pts',(-2.7398020033052,-2.63841079513441,11.7754361650639));
#35083=CARTESIAN_POINT('Ctrl Pts',(0.38723559847199,-3.96742994882286,11.9168951612903));
#35084=CARTESIAN_POINT('Ctrl Pts',(3.54469272874429,-1.82362421192741,12.0757870967742));
#35085=CARTESIAN_POINT('Ctrl Pts',(3.45302863798842,1.9917442187119,12.2346790322581));
#35086=CARTESIAN_POINT('Ctrl Pts',(0.196264076456207,3.98144850774605,12.3935709677419));
#35087=CARTESIAN_POINT('Ctrl Pts',(-2.80821900811,2.53041799939006,12.5324813263542));
#35088=CARTESIAN_POINT('Ctrl Pts',(-3.36359503087846,0.698664221349558,
12.6184277064719));
#35089=CARTESIAN_POINT('Ctrl Pts',(-3.36754256765694,-0.00208193686516537,
12.651410108095));
#35090=CARTESIAN_POINT('Ctrl Pts',(-3.36722041330275,-0.00185992061757217,
11.848589891905));
#35091=CARTESIAN_POINT('Ctrl Pts',(-3.36943251646156,-0.444385182068521,
11.8694134963434));
#35092=CARTESIAN_POINT('Ctrl Pts',(-3.08234983495276,-2.01021544013623,
11.9432253895101));
#35093=CARTESIAN_POINT('Ctrl Pts',(-0.711713421966334,-3.92286142494773,
12.0700255714049));
#35094=CARTESIAN_POINT('Ctrl Pts',(2.91318501009988,-2.72189839106446,12.2289904375897));
#35095=CARTESIAN_POINT('Ctrl Pts',(3.86556759564105,0.976096776902648,12.3879553037744));
#35096=CARTESIAN_POINT('Ctrl Pts',(1.27173165426137,3.77863419159615,12.5469201699592));
#35097=CARTESIAN_POINT('Ctrl Pts',(-2.36055670961755,3.13734167043916,12.7004650326694));
#35098=CARTESIAN_POINT('Ctrl Pts',(-3.36894298024411,1.00230034028648,12.8010216066513));
#35099=CARTESIAN_POINT('Ctrl Pts',(-3.3758812610584,-0.00196014188030577,
12.848589891905));
#35100=CARTESIAN_POINT('Origin',(0.,0.,-1.84858989190503));
#35101=CARTESIAN_POINT('',(-3.37710546106046,0.000736094683953019,10.651410108095));
#35102=CARTESIAN_POINT('',(-3.36907238740032,0.00277677980771746,10.848589891905));
#35103=CARTESIAN_POINT('',(-3.37175,2.08693528006523E-13,-1.84858989190503));
#35104=CARTESIAN_POINT('Ctrl Pts',(-3.37710546106046,0.000736094683952996,
10.651410108095));
#35105=CARTESIAN_POINT('Ctrl Pts',(-3.37391321273993,-1.07663815669567,
10.7024906096977));
#35106=CARTESIAN_POINT('Ctrl Pts',(-2.23194165802167,-3.27693130018453,
10.8065350897951));
#35107=CARTESIAN_POINT('Ctrl Pts',(1.51699821428175,-3.68634890174633,10.9635435483871));
#35108=CARTESIAN_POINT('Ctrl Pts',(3.92040597926993,-0.721712384018116,
11.122435483871));
#35109=CARTESIAN_POINT('Ctrl Pts',(2.73030783639792,2.90445707939446,11.2813274193548));
#35110=CARTESIAN_POINT('Ctrl Pts',(-0.962433500126168,3.86835540835836,
11.4402193548387));
#35111=CARTESIAN_POINT('Ctrl Pts',(-3.1445024192473,1.86381595651157,11.5635802510854));
#35112=CARTESIAN_POINT('Ctrl Pts',(-3.37143588630209,0.372710407919653,
11.6339771688375));
#35113=CARTESIAN_POINT('Ctrl Pts',(-3.36871665678573,0.00265343926576761,
11.651410108095));
#35114=CARTESIAN_POINT('Ctrl Pts',(-3.36907238740032,0.00277677980771742,
10.848589891905));
#35115=CARTESIAN_POINT('Ctrl Pts',(-3.36312082444251,-0.766029392039194,
10.8848170973072));
#35116=CARTESIAN_POINT('Ctrl Pts',(-2.72027913252513,-2.66834094208117,
10.9740325914377));
#35117=CARTESIAN_POINT('Ctrl Pts',(0.441146911493231,-3.96241935650807,
11.1162363742964));
#35118=CARTESIAN_POINT('Ctrl Pts',(3.57049754163045,-1.77395745708877,11.2752012404812));
#35119=CARTESIAN_POINT('Ctrl Pts',(3.42432285260543,2.04190860605321,11.4341661066659));
#35120=CARTESIAN_POINT('Ctrl Pts',(0.136721492950909,3.98455580808139,11.5931309728507));
#35121=CARTESIAN_POINT('Ctrl Pts',(-2.82921667119627,2.49618535096433,11.7312722345971));
#35122=CARTESIAN_POINT('Ctrl Pts',(-3.36380354088135,0.681676177418306,
11.8164252076152));
#35123=CARTESIAN_POINT('Ctrl Pts',(-3.36722041330275,-0.00185992061757217,
11.848589891905));
#35124=CARTESIAN_POINT('Origin',(0.,0.,-1.84858989190503));
#35125=CARTESIAN_POINT('',(-3.37090359896229,-0.00307926823583696,9.65141010809498));
#35126=CARTESIAN_POINT('',(-3.37720911693329,0.000534521222638907,9.84858989190502));
#35127=CARTESIAN_POINT('',(-3.37175,2.08693528006523E-13,-1.84858989190503));
#35128=CARTESIAN_POINT('Ctrl Pts',(-3.37090359896229,-0.0030792682358368,
9.65141010809498));
#35129=CARTESIAN_POINT('Ctrl Pts',(-3.37349992290045,-0.292697043198134,
9.6650760935687));
#35130=CARTESIAN_POINT('Ctrl Pts',(-3.20668744219234,-1.70181407180786,
9.73170605753704));
#35131=CARTESIAN_POINT('Ctrl Pts',(-1.23445173354738,-3.79032725830928,
9.85129999999999));
#35132=CARTESIAN_POINT('Ctrl Pts',(2.51736903674626,-3.09084210861242,10.0101919354839));
#35133=CARTESIAN_POINT('Ctrl Pts',(3.96172967315432,0.441757630821415,10.1690838709677));
#35134=CARTESIAN_POINT('Ctrl Pts',(1.77470645260886,3.56943536355667,10.3279758064516));
#35135=CARTESIAN_POINT('Ctrl Pts',(-2.03904067252446,3.42531238624034,10.4868677419355));
#35136=CARTESIAN_POINT('Ctrl Pts',(-3.35858003390563,1.1971743885357,10.5946791758166));
#35137=CARTESIAN_POINT('Ctrl Pts',(-3.37722316793013,0.0404618108125119,
10.6495266312031));
#35138=CARTESIAN_POINT('Ctrl Pts',(-3.37710546106046,0.000736094683952996,
10.651410108095));
#35139=CARTESIAN_POINT('Ctrl Pts',(-3.37720911693329,0.000534521222638742,
9.84858989190502));
#35140=CARTESIAN_POINT('Ctrl Pts',(-3.37481325646777,-1.08835732049462,
9.90022069827108));
#35141=CARTESIAN_POINT('Ctrl Pts',(-2.21074657312113,-3.29916896326091,
10.0048397933654));
#35142=CARTESIAN_POINT('Ctrl Pts',(1.55707745747673,-3.67027077281332,10.1624471771879));
#35143=CARTESIAN_POINT('Ctrl Pts',(3.928912558612,-0.677512997019795,10.3214120433727));
#35144=CARTESIAN_POINT('Ctrl Pts',(2.69641733534343,2.93678588051791,10.4803769095574));
#35145=CARTESIAN_POINT('Ctrl Pts',(-1.00973405207762,3.8569177977272,10.6393417757422));
#35146=CARTESIAN_POINT('Ctrl Pts',(-3.15606037844699,1.83542847981608,10.7620794365247));
#35147=CARTESIAN_POINT('Ctrl Pts',(-3.37182597111036,0.358476982592217,
10.831828808579));
#35148=CARTESIAN_POINT('Ctrl Pts',(-3.36907238740032,0.00277677980771742,
10.848589891905));
#35149=CARTESIAN_POINT('Origin',(0.,0.,-1.84858989190503));
#35150=CARTESIAN_POINT('',(-3.36644585084492,0.000942668595409863,8.65141010809498));
#35151=CARTESIAN_POINT('',(-3.37066808100933,-0.00306963188584058,8.84858989190501));
#35152=CARTESIAN_POINT('',(-3.37175,2.08693528006523E-13,-1.84858989190503));
#35153=CARTESIAN_POINT('Ctrl Pts',(-3.36644585084492,0.000942668595410034,
8.65141010809498));
#35154=CARTESIAN_POINT('Ctrl Pts',(-3.36489256340397,-0.620276501159167,
8.68062555593429));
#35155=CARTESIAN_POINT('Ctrl Pts',(-2.90218694538986,-2.36984060140867,
8.76280498226821));
#35156=CARTESIAN_POINT('Ctrl Pts',(-0.086697347329244,-3.9853400579507,
8.89794838709678));
#35157=CARTESIAN_POINT('Ctrl Pts',(3.30302181201077,-2.23170309784288,9.05684032258065));
#35158=CARTESIAN_POINT('Ctrl Pts',(3.66513912143678,1.56754809433529,9.21573225806451));
#35159=CARTESIAN_POINT('Ctrl Pts',(0.667732148006428,3.92995999802278,9.3746241935484));
#35160=CARTESIAN_POINT('Ctrl Pts',(-2.63128595375923,2.79674582771393,9.51985014355854));
#35161=CARTESIAN_POINT('Ctrl Pts',(-3.36343759366045,0.829747410900375,
9.61211211507407));
#35162=CARTESIAN_POINT('Ctrl Pts',(-3.37090359896229,-0.0030792682358368,
9.65141010809498));
#35163=CARTESIAN_POINT('Ctrl Pts',(-3.37066808100933,-0.0030696318858409,
8.84858989190502));
#35164=CARTESIAN_POINT('Ctrl Pts',(-3.37331082414,-0.300796169438093,8.86263601050667));
#35165=CARTESIAN_POINT('Ctrl Pts',(-3.20068977672434,-1.71866740211794,
8.92967041783657));
#35166=CARTESIAN_POINT('Ctrl Pts',(-1.20570712414377,-3.80021684712055,
9.04969311389473));
#35167=CARTESIAN_POINT('Ctrl Pts',(2.54266018034211,-3.07087234538534,9.20865798007948));
#35168=CARTESIAN_POINT('Ctrl Pts',(3.95842601916979,0.47564819468749,9.36762284626423));
#35169=CARTESIAN_POINT('Ctrl Pts',(1.74278629094578,3.58581562527152,9.52658771244896));
#35170=CARTESIAN_POINT('Ctrl Pts',(-2.07166160205713,3.40640513751843,9.68555257863373));
#35171=CARTESIAN_POINT('Ctrl Pts',(-3.36396169301834,1.17525404838138,9.7928866384524));
#35172=CARTESIAN_POINT('Ctrl Pts',(-3.377272109138,0.0291637752183697,9.84723240954283));
#35173=CARTESIAN_POINT('Ctrl Pts',(-3.37720911693329,0.000534521222638742,
9.84858989190502));
#35174=CARTESIAN_POINT('Origin',(0.,0.,-1.84858989190503));
#35175=CARTESIAN_POINT('',(-3.37436653161969,0.00264543560195785,7.65141010809498));
#35176=CARTESIAN_POINT('',(-3.36647579863201,0.00101859643942465,7.84858989190502));
#35177=CARTESIAN_POINT('',(-3.37175,2.08693528006523E-13,-1.84858989190503));
#35178=CARTESIAN_POINT('Ctrl Pts',(-3.37436653161969,0.00264543560195811,
7.65141010809498));
#35179=CARTESIAN_POINT('Ctrl Pts',(-3.36621424622869,-0.943539301975876,
7.69617501829988));
#35180=CARTESIAN_POINT('Ctrl Pts',(-2.45755376938072,-3.02292340440546,
7.7939039069994));
#35181=CARTESIAN_POINT('Ctrl Pts',(1.06845185659111,-3.84042477308012,7.94459677419355));
#35182=CARTESIAN_POINT('Ctrl Pts',(3.80694458147109,-1.18221180891932,8.10348870967742));
#35183=CARTESIAN_POINT('Ctrl Pts',(3.0559319039131,2.55963513145653,8.2623806451613));
#35184=CARTESIAN_POINT('Ctrl Pts',(-0.49619611955484,3.95528016940384,8.42127258064515));
#35185=CARTESIAN_POINT('Ctrl Pts',(-3.02400139141134,2.13545120331948,8.55094906828973));
#35186=CARTESIAN_POINT('Ctrl Pts',(-3.36770848062251,0.505916700748885,
8.62766157743967));
#35187=CARTESIAN_POINT('Ctrl Pts',(-3.36644585084492,0.000942668595410034,
8.65141010809498));
#35188=CARTESIAN_POINT('Ctrl Pts',(-3.36647579863201,0.00101859643942433,
7.84858989190502));
#35189=CARTESIAN_POINT('Ctrl Pts',(-3.36478428770786,-0.625167485996831,
7.87803961147051));
#35190=CARTESIAN_POINT('Ctrl Pts',(-2.8964828528491,-2.38038813746449,7.96047761976425));
#35191=CARTESIAN_POINT('Ctrl Pts',(-0.0672816548149041,-3.98633301836102,
8.09590391678625));
#35192=CARTESIAN_POINT('Ctrl Pts',(3.31538886833258,-2.21440159096907,8.25486878297098));
#35193=CARTESIAN_POINT('Ctrl Pts',(3.65656725922866,1.58899138861319,8.41383364915575));
#35194=CARTESIAN_POINT('Ctrl Pts',(0.643261156248369,3.93466553079316,8.57279851534047));
#35195=CARTESIAN_POINT('Ctrl Pts',(-2.64176562949924,2.78241271369441,8.71771726292358));
#35196=CARTESIAN_POINT('Ctrl Pts',(-3.36334120619684,0.822362489639698,
8.80964772177842));
#35197=CARTESIAN_POINT('Ctrl Pts',(-3.37066808100933,-0.0030696318858409,
8.84858989190502));
#35198=CARTESIAN_POINT('Origin',(0.,0.,-1.84858989190503));
#35199=CARTESIAN_POINT('',(-3.3748606436688,-0.00246557707590639,6.65141010809498));
#35200=CARTESIAN_POINT('',(-3.37441250761161,0.00263846066578283,6.84858989190502));
#35201=CARTESIAN_POINT('',(-3.37175,2.08693528006523E-13,-1.84858989190503));
#35202=CARTESIAN_POINT('Ctrl Pts',(-3.3748606436688,-0.00246557707590626,
6.65141010809497));
#35203=CARTESIAN_POINT('Ctrl Pts',(-3.37613613582624,-0.157769830059076,
6.65876050217084));
#35204=CARTESIAN_POINT('Ctrl Pts',(-3.29579272315184,-1.43080711580639,
6.71907487474133));
#35205=CARTESIAN_POINT('Ctrl Pts',(-1.67587337027072,-3.61689096522939,
6.83235322580646));
#35206=CARTESIAN_POINT('Ctrl Pts',(2.13246786040229,-3.36794189853266,6.99124516129032));
#35207=CARTESIAN_POINT('Ctrl Pts',(3.98615544163244,-0.0318842074478251,
7.15013709677419));
#35208=CARTESIAN_POINT('Ctrl Pts',(2.18607012156152,3.33339905069232,7.30902903225807));
#35209=CARTESIAN_POINT('Ctrl Pts',(-1.61780152532516,3.64323620318475,7.46792096774193));
#35210=CARTESIAN_POINT('Ctrl Pts',(-3.28487995770484,1.46716325720085,7.58204799302091));
#35211=CARTESIAN_POINT('Ctrl Pts',(-3.37585969097893,0.175947096268433,
7.64321103980526));
#35212=CARTESIAN_POINT('Ctrl Pts',(-3.37436653161969,0.00264543560195811,
7.65141010809498));
#35213=CARTESIAN_POINT('Ctrl Pts',(-3.37441250761161,0.00263846066578258,
6.84858989190502));
#35214=CARTESIAN_POINT('Ctrl Pts',(-3.36625911376211,-0.945381294583835,
6.89344321243435));
#35215=CARTESIAN_POINT('Ctrl Pts',(-2.45439078883877,-3.02709322103295,
6.99128482169193));
#35216=CARTESIAN_POINT('Ctrl Pts',(1.07677617223565,-3.83874078693202,7.14211471967776));
#35217=CARTESIAN_POINT('Ctrl Pts',(3.81057598656871,-1.17255635469506,7.3010795858625));
#35218=CARTESIAN_POINT('Ctrl Pts',(3.04860581952888,2.56931514444696,7.46004445204726));
#35219=CARTESIAN_POINT('Ctrl Pts',(-0.510113381387115,3.95413228059959,
7.619009318232));
#35220=CARTESIAN_POINT('Ctrl Pts',(-3.02827174132543,2.12695452322279,7.74852446485126));
#35221=CARTESIAN_POINT('Ctrl Pts',(-3.36782778932888,0.501516551178981,
7.82505132274226));
#35222=CARTESIAN_POINT('Ctrl Pts',(-3.36647579863201,0.00101859643942433,
7.84858989190502));
#35223=CARTESIAN_POINT('Origin',(0.,0.,-1.84858989190503));
#35224=CARTESIAN_POINT('',(-3.36661890683212,-0.00122158962200572,5.65141010809498));
#35225=CARTESIAN_POINT('',(-3.37491538366506,-0.00245188971244759,5.84858989190502));
#35226=CARTESIAN_POINT('',(-3.37175,2.08693528006523E-13,-1.84858989190503));
#35227=CARTESIAN_POINT('Ctrl Pts',(-3.36661890683212,-0.00122158962200539,
5.65141010809498));
#35228=CARTESIAN_POINT('Ctrl Pts',(-3.36820126338182,-0.488087448628749,
5.67430996453643));
#35229=CARTESIAN_POINT('Ctrl Pts',(-3.04142339082007,-2.09897775501084,
5.75017379947252));
#35230=CARTESIAN_POINT('Ctrl Pts',(-0.559403071098495,-3.94683670951677,
5.87900161290323));
#35231=CARTESIAN_POINT('Ctrl Pts',(3.01459581839321,-2.60819168376593,6.03789354838709));
#35232=CARTESIAN_POINT('Ctrl Pts',(3.82536866943663,1.12116294553142,6.19678548387097));
#35233=CARTESIAN_POINT('Ctrl Pts',(1.12974830864147,3.82284194895142,6.35567741935484));
#35234=CARTESIAN_POINT('Ctrl Pts',(-2.42881219485455,3.0575629803579,6.50721896076285));
#35235=CARTESIAN_POINT('Ctrl Pts',(-3.3669454531908,0.961290050298803,6.60579652367622));
#35236=CARTESIAN_POINT('Ctrl Pts',(-3.3748606436688,-0.00246557707590626,
6.65141010809497));
#35237=CARTESIAN_POINT('Ctrl Pts',(-3.37491538366506,-0.00245188971244781,
5.84858989190502));
#35238=CARTESIAN_POINT('Ctrl Pts',(-3.37617143803668,-0.156022125643285,
5.85585852466994));
#35239=CARTESIAN_POINT('Ctrl Pts',(-3.29681403413222,-1.42781289481916,
5.91611544616311));
#35240=CARTESIAN_POINT('Ctrl Pts',(-1.68004955900417,-3.61563427819245,
6.02936065638453));
#35241=CARTESIAN_POINT('Ctrl Pts',(2.13069369871068,-3.3697955600636,6.18832552256926));
#35242=CARTESIAN_POINT('Ctrl Pts',(3.98676787287831,-0.032552759256669,
6.34729038875402));
#35243=CARTESIAN_POINT('Ctrl Pts',(2.18543605335013,3.3345534950076,6.50625525493876));
#35244=CARTESIAN_POINT('Ctrl Pts',(-1.62078473268592,3.64258625218979,6.66522012112352));
#35245=CARTESIAN_POINT('Ctrl Pts',(-3.2856992999535,1.4649244081245,6.77933166677893));
#35246=CARTESIAN_POINT('Ctrl Pts',(-3.37589127437617,0.174579143538081,
6.8404549237061));
#35247=CARTESIAN_POINT('Ctrl Pts',(-3.37441250761161,0.00263846066578258,
6.84858989190502));
#35248=CARTESIAN_POINT('Origin',(0.,0.,-1.84858989190503));
#35249=CARTESIAN_POINT('',(-3.37037732776107,0.00303222645661923,4.65141010809497));
#35250=CARTESIAN_POINT('',(-3.36666513788771,-0.00130109466394523,4.84858989190502));
#35251=CARTESIAN_POINT('',(-3.37175,2.08693528006523E-13,-1.84858989190503));
#35252=CARTESIAN_POINT('Ctrl Pts',(-3.37037732776107,0.00303222645661912,
4.65141010809497));
#35253=CARTESIAN_POINT('Ctrl Pts',(-3.36327434274459,-0.812132332425157,
4.68985942690203));
#35254=CARTESIAN_POINT('Ctrl Pts',(-2.65651681547025,-2.76122659154967,
4.7812727242037));
#35255=CARTESIAN_POINT('Ctrl Pts',(0.604781303071069,-3.94013849796468,
4.92565));
#35256=CARTESIAN_POINT('Ctrl Pts',(3.63959495745868,-1.6259767381985,5.08454193548388));
#35257=CARTESIAN_POINT('Ctrl Pts',(3.3382985122726,2.17858092584818,5.24343387096774));
#35258=CARTESIAN_POINT('Ctrl Pts',(-0.0229349622598251,3.98621697792136,
5.40232580645161));
#35259=CARTESIAN_POINT('Ctrl Pts',(-2.88174731779988,2.40610117021057,5.53831788549402));
#35260=CARTESIAN_POINT('Ctrl Pts',(-3.36454150689018,0.637961221244742,
5.62134598604181));
#35261=CARTESIAN_POINT('Ctrl Pts',(-3.36661890683212,-0.00122158962200539,
5.65141010809498));
#35262=CARTESIAN_POINT('Ctrl Pts',(-3.36666513788771,-0.00130109466394548,
4.84858989190502));
#35263=CARTESIAN_POINT('Ctrl Pts',(-3.36833385037662,-0.483310565759833,
4.87126212563378));
#35264=CARTESIAN_POINT('Ctrl Pts',(-3.04595737613669,-2.0897168735396,4.94692264809078));
#35265=CARTESIAN_POINT('Ctrl Pts',(-0.574613628296617,-3.94527526701846,
5.07557145927603));
#35266=CARTESIAN_POINT('Ctrl Pts',(3.0062441927532,-2.61875420913902,5.2345363254608));
#35267=CARTESIAN_POINT('Ctrl Pts',(3.8292149534867,1.11017592945447,5.39350119164552));
#35268=CARTESIAN_POINT('Ctrl Pts',(1.13931660104628,3.82064594498541,5.55246605783029));
#35269=CARTESIAN_POINT('Ctrl Pts',(-2.42498889622798,3.06243800957472,5.7041622912501));
#35270=CARTESIAN_POINT('Ctrl Pts',(-3.36701480929308,0.963503961964746,
5.80287023594169));
#35271=CARTESIAN_POINT('Ctrl Pts',(-3.37491538366506,-0.00245188971244781,
5.84858989190502));
#35272=CARTESIAN_POINT('Origin',(0.,0.,-1.84858989190503));
#35273=CARTESIAN_POINT('',(-3.37724050405987,-0.000407706007126927,3.65141010809498));
#35274=CARTESIAN_POINT('',(-3.37013695473896,0.00300786229786701,3.84858989190502));
#35275=CARTESIAN_POINT('',(-3.37175,2.08693528006523E-13,-1.84858989190503));
#35276=CARTESIAN_POINT('Ctrl Pts',(-3.37724050405987,-0.000407706007126926,
3.65141010809498));
#35277=CARTESIAN_POINT('Ctrl Pts',(-3.37727770925144,-0.0222311044065494,
3.652444910773));
#35278=CARTESIAN_POINT('Ctrl Pts',(-3.36719553771294,-1.16099931030625,
3.70644369194564));
#35279=CARTESIAN_POINT('Ctrl Pts',(-2.09357261161725,-3.39225669930255,
3.8134064516129));
#35280=CARTESIAN_POINT('Ctrl Pts',(1.71738108280889,-3.59736765289132,3.97229838709678));
#35281=CARTESIAN_POINT('Ctrl Pts',(3.95415621068438,-0.505074716519562,
4.13119032258065));
#35282=CARTESIAN_POINT('Ctrl Pts',(2.56648943634972,3.05017766348832,4.29008225806451));
#35283=CARTESIAN_POINT('Ctrl Pts',(-1.17366200413909,3.8095891259482,4.44897419354839));
#35284=CARTESIAN_POINT('Ctrl Pts',(-3.19328501843251,1.73829700144105,4.56941681022521));
#35285=CARTESIAN_POINT('Ctrl Pts',(-3.37305871233378,0.310757734440618,
4.6368954484074));
#35286=CARTESIAN_POINT('Ctrl Pts',(-3.37037732776107,0.00303222645661912,
4.65141010809497));
#35287=CARTESIAN_POINT('Ctrl Pts',(-3.37013695473896,0.00300786229786694,
3.84858989190502));
#35288=CARTESIAN_POINT('Ctrl Pts',(-3.36320369751902,-0.804384073785939,
3.88666572659761));
#35289=CARTESIAN_POINT('Ctrl Pts',(-2.66732523950674,-2.7461115272218,3.97772985001845));
#35290=CARTESIAN_POINT('Ctrl Pts',(0.57892500607099,-3.94464492605495,4.12178226216755));
#35291=CARTESIAN_POINT('Ctrl Pts',(3.63013258458704,-1.64848875417016,4.2807471283523));
#35292=CARTESIAN_POINT('Ctrl Pts',(3.35110647594949,2.15996831943484,4.43971199453705));
#35293=CARTESIAN_POINT('Ctrl Pts',(-0.00217860669321579,3.9869001753454,
4.59867686072179));
#35294=CARTESIAN_POINT('Ctrl Pts',(-2.87549058156321,2.41739184906724,4.73496949317778));
#35295=CARTESIAN_POINT('Ctrl Pts',(-3.36443382798691,0.643215268868607,
4.81827383690552));
#35296=CARTESIAN_POINT('Ctrl Pts',(-3.36666513788771,-0.00130109466394548,
4.84858989190502));
#35297=CARTESIAN_POINT('Origin',(0.,0.,-1.84858989190503));
#35298=CARTESIAN_POINT('',(-3.36917031630593,-0.00279652979204336,2.65141010809498));
#35299=CARTESIAN_POINT('',(-3.37729882489346,-0.000194430141600699,2.84858989190502));
#35300=CARTESIAN_POINT('',(-3.37175,2.08693528006523E-13,-1.84858989190503));
#35301=CARTESIAN_POINT('Ctrl Pts',(-3.36917031630593,-0.00279652979204365,
2.65141010809498));
#35302=CARTESIAN_POINT('Ctrl Pts',(-3.37192195751912,-0.354718783760072,
2.66799437313859));
#35303=CARTESIAN_POINT('Ctrl Pts',(-3.15912528101716,-1.82730552094877,
2.73754261667682));
#35304=CARTESIAN_POINT('Ctrl Pts',(-1.02419029239979,-3.85246484135621,
2.86005483870968));
#35305=CARTESIAN_POINT('Ctrl Pts',(2.68349747959669,-2.94776072747231,3.01894677419354));
#35306=CARTESIAN_POINT('Ctrl Pts',(3.9314491981565,0.658907486316316,3.17783870967743));
#35307=CARTESIAN_POINT('Ctrl Pts',(1.57577260497388,3.66161063015511,3.33673064516129));
#35308=CARTESIAN_POINT('Ctrl Pts',(-2.19953367602677,3.310326581852,3.49458777796714));
#35309=CARTESIAN_POINT('Ctrl Pts',(-3.37537344768752,1.09474900016628,3.59948093227837));
#35310=CARTESIAN_POINT('Ctrl Pts',(-3.37724050405987,-0.000407706007126926,
3.65141010809498));
#35311=CARTESIAN_POINT('Ctrl Pts',(-3.37729882489346,-0.000194430141600942,
2.84858989190502));
#35312=CARTESIAN_POINT('Ctrl Pts',(-3.37730745906329,-0.0105519609168573,
2.8490810388332));
#35313=CARTESIAN_POINT('Ctrl Pts',(-3.3725690581147,-1.13834260190552,2.90256047448963));
#35314=CARTESIAN_POINT('Ctrl Pts',(-2.12700963248002,-3.37212213291773,
3.00902819887431));
#35315=CARTESIAN_POINT('Ctrl Pts',(1.68400001564517,-3.61379602896036,3.16799306505907));
#35316=CARTESIAN_POINT('Ctrl Pts',(3.95013122707835,-0.540223147458982,
3.32695793124381));
#35317=CARTESIAN_POINT('Ctrl Pts',(2.59246639543577,3.02894300530038,3.48592279742856));
#35318=CARTESIAN_POINT('Ctrl Pts',(-1.14349143614182,3.81939852540782,3.6448876636133));
#35319=CARTESIAN_POINT('Ctrl Pts',(-3.18684176799334,1.75591563149786,3.76577669510546));
#35320=CARTESIAN_POINT('Ctrl Pts',(-3.37285237464884,0.31922404594331,3.83367743786936));
#35321=CARTESIAN_POINT('Ctrl Pts',(-3.37013695473896,0.00300786229786694,
3.84858989190502));
#35322=CARTESIAN_POINT('Origin',(0.,0.,-1.84858989190503));
#35323=CARTESIAN_POINT('',(-3.36722314734446,0.00185482314707379,1.65141010809497));
#35324=CARTESIAN_POINT('',(-3.3695578818617,-0.00290129534754852,1.84858989190502));
#35325=CARTESIAN_POINT('',(-3.37175,2.08693528006523E-13,-1.84858989190503));
#35326=CARTESIAN_POINT('Ctrl Pts',(-3.36722314734446,0.00185482314707382,
1.65141010809497));
#35327=CARTESIAN_POINT('Ctrl Pts',(-3.36382382620938,-0.68102387856646,
1.68354383550418));
#35328=CARTESIAN_POINT('Ctrl Pts',(-2.83012682104856,-2.49433668358649,
1.768641541408));
#35329=CARTESIAN_POINT('Ctrl Pts',(0.13255069832671,-3.98407441119242,1.90670322580645));
#35330=CARTESIAN_POINT('Ctrl Pts',(3.42072557595435,-2.04672776701011,2.06559516129032));
#35331=CARTESIAN_POINT('Ctrl Pts',(3.57341090601276,1.76668952717683,2.2244870967742));
#35332=CARTESIAN_POINT('Ctrl Pts',(0.45065073371557,3.96072731387378,2.38337903225806));
#35333=CARTESIAN_POINT('Ctrl Pts',(-2.71613180302817,2.67422828685271,2.52568670269832));
#35334=CARTESIAN_POINT('Ctrl Pts',(-3.36313423821671,0.769190092631348,
2.61503039464396));
#35335=CARTESIAN_POINT('Ctrl Pts',(-3.36917031630593,-0.00279652979204365,
2.65141010809498));
#35336=CARTESIAN_POINT('Ctrl Pts',(-3.3695578818617,-0.00290129534754862,
1.84858989190502));
#35337=CARTESIAN_POINT('Ctrl Pts',(-3.37231432811694,-0.34009370411539,
1.86448463979704));
#35338=CARTESIAN_POINT('Ctrl Pts',(-3.1706964344189,-1.79816219768021,1.93336767641731));
#35339=CARTESIAN_POINT('Ctrl Pts',(-1.07258002819951,-3.83991470812214,
2.05523900176583));
#35340=CARTESIAN_POINT('Ctrl Pts',(2.6481020123777,-2.98042525524821,2.21420386795058));
#35341=CARTESIAN_POINT('Ctrl Pts',(3.9394520872816,0.613266379946328,2.37316873413532));
#35342=CARTESIAN_POINT('Ctrl Pts',(1.61680281711694,3.64435532093595,2.53213360032008));
#35343=CARTESIAN_POINT('Ctrl Pts',(-2.17732013669245,3.33312768965276,2.69060731957663));
#35344=CARTESIAN_POINT('Ctrl Pts',(-3.37637594578823,1.10688927659692,2.79609275010495));
#35345=CARTESIAN_POINT('Ctrl Pts',(-3.37729882489346,-0.000194430141600942,
2.84858989190502));
#35346=CARTESIAN_POINT('Origin',(0.,0.,-1.84858989190503));
#35347=CARTESIAN_POINT('',(-3.37589447807987,0.00214364281095937,0.651410108094974));
#35348=CARTESIAN_POINT('',(-3.36692593843476,0.00163208592380837,0.848589891905015));
#35349=CARTESIAN_POINT('',(-3.37175,2.08693528006523E-13,-1.84858989190503));
#35350=CARTESIAN_POINT('Ctrl Pts',(-3.37589447807987,0.0021436428109594,
0.651410108094974));
#35351=CARTESIAN_POINT('Ctrl Pts',(-3.36905382598057,-1.00443485423249,
0.699093297869767));
#35352=CARTESIAN_POINT('Ctrl Pts',(-2.35675364226999,-3.1417842761117,0.799740466139185));
#35353=CARTESIAN_POINT('Ctrl Pts',(1.27802196869812,-3.77566833700333,0.953351612903227));
#35354=CARTESIAN_POINT('Ctrl Pts',(3.86616524359544,-0.97122229991515,1.1122435483871));
#35355=CARTESIAN_POINT('Ctrl Pts',(2.91058978102209,2.72383605033175,1.27113548387097));
#35356=CARTESIAN_POINT('Ctrl Pts',(-0.71291441141164,3.92198718064885,1.43002741935484));
#35357=CARTESIAN_POINT('Ctrl Pts',(-3.08228566582866,2.00998594685298,1.55678562742951));
#35358=CARTESIAN_POINT('Ctrl Pts',(-3.36942671096663,0.444521639742584,
1.63057985700955));
#35359=CARTESIAN_POINT('Ctrl Pts',(-3.36722314734446,0.00185482314707382,
1.65141010809497));
#35360=CARTESIAN_POINT('Ctrl Pts',(-3.36692593843476,0.00163208592380858,
0.848589891905015));
#35361=CARTESIAN_POINT('Ctrl Pts',(-3.36407240691806,-0.663645509172373,
0.879888240760876));
#35362=CARTESIAN_POINT('Ctrl Pts',(-2.85117022634889,-2.45933226824664,
0.964174878344985));
#35363=CARTESIAN_POINT('Ctrl Pts',(0.0716483833591926,-3.98622915634864,
1.10144980465734));
#35364=CARTESIAN_POINT('Ctrl Pts',(3.39051798866077,-2.09756782602768,1.26041467084209));
#35365=CARTESIAN_POINT('Ctrl Pts',(3.59899177492058,1.71542482386315,1.41937953702684));
#35366=CARTESIAN_POINT('Ctrl Pts',(0.505790215469384,3.95468340129096,1.57834440321159));
#35367=CARTESIAN_POINT('Ctrl Pts',(-2.69572995999776,2.70483870003466,1.72141452150431));
#35368=CARTESIAN_POINT('Ctrl Pts',(-3.36312516884065,0.784003943368042,
1.81149635106879));
#35369=CARTESIAN_POINT('Ctrl Pts',(-3.3695578818617,-0.00290129534754862,
1.84858989190502));
#35370=CARTESIAN_POINT('Origin',(0.,0.,24.5));
#35371=CARTESIAN_POINT('',(-3.87097280197699,0.00213832761144025,24.1339652975667));
#35372=CARTESIAN_POINT('Ctrl Pts',(-0.624728334461281,3.3133687646595,24.62825));
#35373=CARTESIAN_POINT('Ctrl Pts',(-0.520138250042208,3.33634852849099,
24.625046902956));
#35374=CARTESIAN_POINT('Ctrl Pts',(-0.414648098080521,3.35389705620374,
24.6218539025135));
#35375=CARTESIAN_POINT('Ctrl Pts',(-0.308613703672553,3.36622114122732,
24.6186673709615));
#35376=CARTESIAN_POINT('Ctrl Pts',(-0.199986616426575,3.37884656778403,
24.6154029241484));
#35377=CARTESIAN_POINT('Ctrl Pts',(-0.0907876447210383,3.38598894312879,
24.6121452664408));
#35378=CARTESIAN_POINT('Ctrl Pts',(0.018614620750679,3.38781780937344,24.6088904974597));
#35379=CARTESIAN_POINT('Ctrl Pts',(0.0805633655032933,3.38885340006882,
24.6070474930945));
#35380=CARTESIAN_POINT('Ctrl Pts',(0.142577487054791,3.38818433590453,24.6052054149592));
#35381=CARTESIAN_POINT('Ctrl Pts',(0.204590631758452,3.38583417858992,24.6033635549037));
#35382=CARTESIAN_POINT('Ctrl Pts',(0.254638036250335,3.38393749564785,24.6018770907733));
#35383=CARTESIAN_POINT('Ctrl Pts',(0.304684819171919,3.38094577981049,24.600390768683));
#35384=CARTESIAN_POINT('Ctrl Pts',(0.354695913393206,3.3768690300029,24.5989042163964));
#35385=CARTESIAN_POINT('Ctrl Pts',(0.372494580510141,3.37541813767843,24.5983751607996));
#35386=CARTESIAN_POINT('Ctrl Pts',(0.39028796136771,3.37382978973891,24.5978460986132));
#35387=CARTESIAN_POINT('Ctrl Pts',(0.408061433233138,3.37210587416845,24.5973174010591));
#35388=CARTESIAN_POINT('Ctrl Pts',(0.519404457290808,3.36130629745725,24.5940053422263));
#35389=CARTESIAN_POINT('Ctrl Pts',(0.630100011901245,3.34518038635334,24.5907036020021));
#35390=CARTESIAN_POINT('Ctrl Pts',(0.739763436768937,3.32391000487198,24.5874081616821));
#35391=CARTESIAN_POINT('Ctrl Pts',(0.850257666159321,3.3024784800636,24.5840877552741));
#35392=CARTESIAN_POINT('Ctrl Pts',(0.95970493776685,3.27582407416606,24.5807737445874));
#35393=CARTESIAN_POINT('Ctrl Pts',(1.06770973553523,3.24407969544398,24.5774620188875));
#35394=CARTESIAN_POINT('Ctrl Pts',(1.1361584697924,3.22396149154746,24.5753631914553));
#35395=CARTESIAN_POINT('Ctrl Pts',(1.20402775637168,3.20179785912252,24.5732652817816));
#35396=CARTESIAN_POINT('Ctrl Pts',(1.27121405220256,3.17761217468148,24.5711672434934));
#35397=CARTESIAN_POINT('Ctrl Pts',(1.29774075436021,3.16806310757318,24.5703388894951));
#35398=CARTESIAN_POINT('Ctrl Pts',(1.32416095392457,3.15819874582631,24.5695105154476));
#35399=CARTESIAN_POINT('Ctrl Pts',(1.35046812449935,3.14802019412801,24.5686820569498));
#35400=CARTESIAN_POINT('Ctrl Pts',(1.36653976589062,3.14180188827438,24.5681759330454));
#35401=CARTESIAN_POINT('Ctrl Pts',(1.38256076287534,3.13546957145725,24.5676700437565));
#35402=CARTESIAN_POINT('Ctrl Pts',(1.39852700263983,3.12902498441374,24.5671644619047));
#35403=CARTESIAN_POINT('Ctrl Pts',(1.5038400459978,3.08651659892363,24.5638296526902));
#35404=CARTESIAN_POINT('Ctrl Pts',(1.60681042310701,3.03911282071154,24.5605069879339));
#35405=CARTESIAN_POINT('Ctrl Pts',(1.70704837153172,2.98697613057657,24.5571923886324));
#35406=CARTESIAN_POINT('Ctrl Pts',(1.80670371564138,2.935142469994,24.5538970544882));
#35407=CARTESIAN_POINT('Ctrl Pts',(1.90365915425284,2.87863046313165,24.5506096923149));
#35408=CARTESIAN_POINT('Ctrl Pts',(1.99751737945406,2.81755070396422,24.5473262938205));
#35409=CARTESIAN_POINT('Ctrl Pts',(2.09219867451912,2.7559353187613,24.5440141022572));
#35410=CARTESIAN_POINT('Ctrl Pts',(2.18372913512715,2.68967155408011,24.5407059441949));
#35411=CARTESIAN_POINT('Ctrl Pts',(2.271672791588,2.61882611527755,24.5373977049647));
#35412=CARTESIAN_POINT('Ctrl Pts',(2.31564461981842,2.58340339587627,24.5357435853496));
#35413=CARTESIAN_POINT('Ctrl Pts',(2.3587192214935,2.54683454512376,24.5340894454425));
#35414=CARTESIAN_POINT('Ctrl Pts',(2.40083835867941,2.50912376524234,24.5324347709098));
#35415=CARTESIAN_POINT('Ctrl Pts',(2.4199270309962,2.49203298969322,24.5316848614374));
#35416=CARTESIAN_POINT('Ctrl Pts',(2.43881941610424,2.47470762973993,24.5309348421549));
#35417=CARTESIAN_POINT('Ctrl Pts',(2.45750989027674,2.45714789797131,24.5301846651845));
#35418=CARTESIAN_POINT('Ctrl Pts',(2.47259728190695,2.4429732682819,24.5295791046386));
#35419=CARTESIAN_POINT('Ctrl Pts',(2.48755582869293,2.42864311414144,24.5289733271752));
#35420=CARTESIAN_POINT('Ctrl Pts',(2.50236326380812,2.41417672018039,24.528368102554));
#35421=CARTESIAN_POINT('Ctrl Pts',(2.5096874370137,2.40702123550619,24.5280687414615));
#35422=CARTESIAN_POINT('Ctrl Pts',(2.51697555679688,2.39983158202503,24.5277694793085));
#35423=CARTESIAN_POINT('Ctrl Pts',(2.52422733942721,2.39260786015533,24.5274703131481));
#35424=CARTESIAN_POINT('Ctrl Pts',(2.60073745914298,2.31639379621843,24.5243139528543));
#35425=CARTESIAN_POINT('Ctrl Pts',(2.67320522179129,2.23639118372509,24.5211682778273));
#35426=CARTESIAN_POINT('Ctrl Pts',(2.74161153441807,2.15302978874429,24.5180298269183));
#35427=CARTESIAN_POINT('Ctrl Pts',(2.81186762190031,2.06741421857952,24.5148065091695));
#35428=CARTESIAN_POINT('Ctrl Pts',(2.87784002551868,1.97825519814193,24.511590811516));
#35429=CARTESIAN_POINT('Ctrl Pts',(2.93947332195402,1.88597569204873,24.5083789843694));
#35430=CARTESIAN_POINT('Ctrl Pts',(3.00543439044467,1.78721649574186,24.5049416288708));
#35431=CARTESIAN_POINT('Ctrl Pts',(3.06642646008642,1.68488265861663,24.5015087065221));
#35432=CARTESIAN_POINT('Ctrl Pts',(3.12233208000985,1.57945276379857,24.4980756211074));
#35433=CARTESIAN_POINT('Ctrl Pts',(3.14679078872635,1.53332718481566,24.4965736462384));
#35434=CARTESIAN_POINT('Ctrl Pts',(3.1702752276744,1.48660856181708,24.4950716401576));
#35435=CARTESIAN_POINT('Ctrl Pts',(3.19277220676191,1.43933527974668,24.4935692179767));
#35436=CARTESIAN_POINT('Ctrl Pts',(3.20843753613705,1.40641745858516,24.4925230358101));
#35437=CARTESIAN_POINT('Ctrl Pts',(3.2236240268298,1.3732306769969,24.4914766518865));
#35438=CARTESIAN_POINT('Ctrl Pts',(3.23832660560595,1.33978769663366,24.4904299362547));
#35439=CARTESIAN_POINT('Ctrl Pts',(3.24466706730076,1.32536546913318,24.489978541947));
#35440=CARTESIAN_POINT('Ctrl Pts',(3.25091694288974,1.31089679039211,24.489527124135));
#35441=CARTESIAN_POINT('Ctrl Pts',(3.25707117071328,1.29639411279135,24.4890760252508));
#35442=CARTESIAN_POINT('Ctrl Pts',(3.30189883440903,1.19075597705509,24.4857902013176));
#35443=CARTESIAN_POINT('Ctrl Pts',(3.34172661274634,1.08315538243838,24.4825162404531));
#35444=CARTESIAN_POINT('Ctrl Pts',(3.37649898345667,0.974036565393082,24.4792502460069));
#35445=CARTESIAN_POINT('Ctrl Pts',(3.41163056334322,0.863790517745426,24.4759505128437));
#35446=CARTESIAN_POINT('Ctrl Pts',(3.44160210056879,0.751993878752548,24.47265891154));
#35447=CARTESIAN_POINT('Ctrl Pts',(3.46631080319639,0.639077130310462,24.4693714234329));
#35448=CARTESIAN_POINT('Ctrl Pts',(3.4909156460234,0.526635012655473,24.4660977538522));
#35449=CARTESIAN_POINT('Ctrl Pts',(3.51030206328578,0.41308129028903,24.4628281629622));
#35450=CARTESIAN_POINT('Ctrl Pts',(3.5243192195213,0.298826837120347,24.4595586825629));
#35451=CARTESIAN_POINT('Ctrl Pts',(3.5361116521245,0.202706203521802,24.4568081155714));
#35452=CARTESIAN_POINT('Ctrl Pts',(3.54410317841348,0.106089103613188,24.4540576267811));
#35453=CARTESIAN_POINT('Ctrl Pts',(3.54817462918724,0.00921931232785102,
24.451304853408));
#35454=CARTESIAN_POINT('Ctrl Pts',(3.54887956636703,-0.00755287067786807,
24.4508282340391));
#35455=CARTESIAN_POINT('Ctrl Pts',(3.54946687335721,-0.0243333324170402,
24.4503515260614));
#35456=CARTESIAN_POINT('Ctrl Pts',(3.5499355914206,-0.0411046474494315,
24.4498751757144));
#35457=CARTESIAN_POINT('Ctrl Pts',(3.55318741783251,-0.157459039234995,
24.4465703987905));
#35458=CARTESIAN_POINT('Ctrl Pts',(3.55074422185484,-0.273556149324447,
24.4432776009626));
#35459=CARTESIAN_POINT('Ctrl Pts',(3.54250561679224,-0.388968852721143,
24.4399928190226));
#35460=CARTESIAN_POINT('Ctrl Pts',(3.53438980253945,-0.502661408204027,
24.4367569945253));
#35461=CARTESIAN_POINT('Ctrl Pts',(3.52065018301948,-0.615690678667281,
24.4335289487538));
#35462=CARTESIAN_POINT('Ctrl Pts',(3.50114108221864,-0.727654569046081,
24.430304893079));
#35463=CARTESIAN_POINT('Ctrl Pts',(3.49384800416623,-0.769509977961124,
24.42909964585));
#35464=CARTESIAN_POINT('Ctrl Pts',(3.48574813528587,-0.811216498584334,
24.427894956231));
#35465=CARTESIAN_POINT('Ctrl Pts',(3.47683197850714,-0.852752977896645,
24.4266906262961));
#35466=CARTESIAN_POINT('Ctrl Pts',(3.4529871352566,-0.963835685722627,24.4234698374258));
#35467=CARTESIAN_POINT('Ctrl Pts',(3.42330774908946,-1.07370337125384,24.4202516210517));
#35468=CARTESIAN_POINT('Ctrl Pts',(3.38809113649622,-1.1820724034292,24.4170321914123));
#35469=CARTESIAN_POINT('Ctrl Pts',(3.37495661955853,-1.22249011495268,24.4158314611315));
#35470=CARTESIAN_POINT('Ctrl Pts',(3.36105136220375,-1.26269920199182,24.4146305620831));
#35471=CARTESIAN_POINT('Ctrl Pts',(3.34638908048464,-1.30268427759558,24.4134292978622));
#35472=CARTESIAN_POINT('Ctrl Pts',(3.33893812623189,-1.32300355496479,24.4128188495754));
#35473=CARTESIAN_POINT('Ctrl Pts',(3.33129166525305,-1.3432649771586,24.412208306987));
#35474=CARTESIAN_POINT('Ctrl Pts',(3.32345141301749,-1.36346647925837,24.411597644323));
#35475=CARTESIAN_POINT('Ctrl Pts',(3.31733644758331,-1.37922253956704,24.4111213610389));
#35476=CARTESIAN_POINT('Ctrl Pts',(3.31110676245958,-1.39493393196613,24.4106452528772));
#35477=CARTESIAN_POINT('Ctrl Pts',(3.30476515852903,-1.41059588192003,24.4101694268982));
#35478=CARTESIAN_POINT('Ctrl Pts',(3.26241982156158,-1.51517676644526,24.4069921531923));
#35479=CARTESIAN_POINT('Ctrl Pts',(3.21506671129281,-1.61761018296196,24.4038257550006));
#35480=CARTESIAN_POINT('Ctrl Pts',(3.16305493267433,-1.71764249367417,24.4006667076014));
#35481=CARTESIAN_POINT('Ctrl Pts',(3.10936292149889,-1.82090633289145,24.3974056076588));
#35482=CARTESIAN_POINT('Ctrl Pts',(3.05070610897566,-1.92161214375833,24.3941523411125));
#35483=CARTESIAN_POINT('Ctrl Pts',(2.98741482167415,-2.01946701686137,24.3909030304897));
#35484=CARTESIAN_POINT('Ctrl Pts',(2.92378476042904,-2.11784566950304,24.3876363275557));
#35485=CARTESIAN_POINT('Ctrl Pts',(2.85546994313465,-2.2133435033276,24.3843736230076));
#35486=CARTESIAN_POINT('Ctrl Pts',(2.78275913579883,-2.30563818528626,24.3811109767752));
#35487=CARTESIAN_POINT('Ctrl Pts',(2.73115118701869,-2.37114618050358,24.3787952484011));
#35488=CARTESIAN_POINT('Ctrl Pts',(2.67732765960473,-2.4350400215934,24.3764795494049));
#35489=CARTESIAN_POINT('Ctrl Pts',(2.62137984513178,-2.49719390809692,24.3741624709621));
#35490=CARTESIAN_POINT('Ctrl Pts',(2.60733587761121,-2.51279571795411,24.3735808401209));
#35491=CARTESIAN_POINT('Ctrl Pts',(2.59315801395097,-2.52828784255011,24.3729991223601));
#35492=CARTESIAN_POINT('Ctrl Pts',(2.5788476135988,-2.54366818796195,24.3724172953964));
#35493=CARTESIAN_POINT('Ctrl Pts',(2.56780240058981,-2.55553921791534,24.3719682232117));
#35494=CARTESIAN_POINT('Ctrl Pts',(2.55668178857907,-2.56733978704972,24.3715192315499));
#35495=CARTESIAN_POINT('Ctrl Pts',(2.54549189058683,-2.5790635828598,24.3710705218887));
#35496=CARTESIAN_POINT('Ctrl Pts',(2.46377857881438,-2.6646756396319,24.367793856412));
#35497=CARTESIAN_POINT('Ctrl Pts',(2.37828958660479,-2.74628708545935,24.3645287774285));
#35498=CARTESIAN_POINT('Ctrl Pts',(2.28935576945552,-2.82360475294287,24.3612714210233));
#35499=CARTESIAN_POINT('Ctrl Pts',(2.2004312170102,-2.9009143658379,24.358014403954));
#35500=CARTESIAN_POINT('Ctrl Pts',(2.10806196086699,-2.97393178300944,24.354765107854));
#35501=CARTESIAN_POINT('Ctrl Pts',(2.01253765634337,-3.04233309530011,24.3515196700154));
#35502=CARTESIAN_POINT('Ctrl Pts',(1.91831994223422,-3.10979880801304,24.3483186235807));
#35503=CARTESIAN_POINT('Ctrl Pts',(1.82103227216761,-3.17277441103138,24.345121330582));
#35504=CARTESIAN_POINT('Ctrl Pts',(1.72092180235263,-3.23090982550694,24.3419240846569));
#35505=CARTESIAN_POINT('Ctrl Pts',(1.63731823238491,-3.27945947471638,24.3392540225356));
#35506=CARTESIAN_POINT('Ctrl Pts',(1.55174530961941,-3.32463302100756,24.3365839932441));
#35507=CARTESIAN_POINT('Ctrl Pts',(1.46433480530475,-3.3662006160568,24.3339118381243));
#35508=CARTESIAN_POINT('Ctrl Pts',(1.44360953039847,-3.37605640903435,24.3332782626761));
#35509=CARTESIAN_POINT('Ctrl Pts',(1.42277595537401,-3.38571149112601,24.3326444189594));
#35510=CARTESIAN_POINT('Ctrl Pts',(1.40186473452666,-3.39514984035219,24.3320111514667));
#35511=CARTESIAN_POINT('Ctrl Pts',(1.33458120918284,-3.42551848377093,24.3299735626666));
#35512=CARTESIAN_POINT('Ctrl Pts',(1.2664465713012,-3.45366766831798,24.3279404681835));
#35513=CARTESIAN_POINT('Ctrl Pts',(1.19753254997869,-3.47952152342011,24.3259109394442));
#35514=CARTESIAN_POINT('Ctrl Pts',(1.09102290473056,-3.51947979145293,24.3227742136821));
#35515=CARTESIAN_POINT('Ctrl Pts',(0.982652679880705,-3.55395790982246,
24.3196460054332));
#35516=CARTESIAN_POINT('Ctrl Pts',(0.872822247400536,-3.58310705179026,
24.3165228865437));
#35517=CARTESIAN_POINT('Ctrl Pts',(0.760371906501168,-3.61295152091583,
24.3133252683986));
#35518=CARTESIAN_POINT('Ctrl Pts',(0.646390155341705,-3.6372098459968,24.3101329853132));
#35519=CARTESIAN_POINT('Ctrl Pts',(0.53128616178814,-3.6559936831665,24.3069423579087));
#35520=CARTESIAN_POINT('Ctrl Pts',(0.41453738712084,-3.67504593240137,24.3037061379619));
#35521=CARTESIAN_POINT('Ctrl Pts',(0.296633230443278,-3.68846615738096,
24.3004716213517));
#35522=CARTESIAN_POINT('Ctrl Pts',(0.177991630975357,-3.69631848981734,
24.2972349687049));
#35523=CARTESIAN_POINT('Ctrl Pts',(0.142360760405031,-3.69867673045107,
24.2962629255763));
#35524=CARTESIAN_POINT('Ctrl Pts',(0.1066633636693,-3.70053242315808,24.2952906897893));
#35525=CARTESIAN_POINT('Ctrl Pts',(0.0709107847277581,-3.70188639298558,
24.2943181573453));
#35526=CARTESIAN_POINT('Ctrl Pts',(0.0511417931589634,-3.70263505556873,
24.2937804063283));
#35527=CARTESIAN_POINT('Ctrl Pts',(0.0313540742527653,-3.70323026849973,
24.2932425143369));
#35528=CARTESIAN_POINT('Ctrl Pts',(0.0115717980804544,-3.70367187863094,
24.2927050676203));
#35529=CARTESIAN_POINT('Ctrl Pts',(-0.107433551546183,-3.70632849749549,
24.2894719192276));
#35530=CARTESIAN_POINT('Ctrl Pts',(-0.226418918411982,-3.7034386910525,
24.2862500321799));
#35531=CARTESIAN_POINT('Ctrl Pts',(-0.344959013740293,-3.6951464558983,
24.2830356970017));
#35532=CARTESIAN_POINT('Ctrl Pts',(-0.464907323931171,-3.68675571189142,
24.2797831766461));
#35533=CARTESIAN_POINT('Ctrl Pts',(-0.584400592051045,-3.67283340149898,
24.2765383886529));
#35534=CARTESIAN_POINT('Ctrl Pts',(-0.703006950795025,-3.65347561626452,
24.2732974897681));
#35535=CARTESIAN_POINT('Ctrl Pts',(-0.821420460393264,-3.63414930600648,
24.2700618604539));
#35536=CARTESIAN_POINT('Ctrl Pts',(-0.938950841911184,-3.6094050645999,
24.2668301076113));
#35537=CARTESIAN_POINT('Ctrl Pts',(-1.05516365811085,-3.57928709699041,
24.2635984067028));
#35538=CARTESIAN_POINT('Ctrl Pts',(-1.11307514573956,-3.56427862920126,
24.261987976689));
#35539=CARTESIAN_POINT('Ctrl Pts',(-1.17065929149193,-3.5479349386455,24.2603775595719));
#35540=CARTESIAN_POINT('Ctrl Pts',(-1.22786083460473,-3.53025684653982,
24.258766682079));
#35541=CARTESIAN_POINT('Ctrl Pts',(-1.27025654792723,-3.5171544845367,24.2575727579877));
#35542=CARTESIAN_POINT('Ctrl Pts',(-1.31244206756123,-3.50331904033182,
24.256378581001));
#35543=CARTESIAN_POINT('Ctrl Pts',(-1.35439435742328,-3.48874976896511,
24.2551839584315));
#35544=CARTESIAN_POINT('Ctrl Pts',(-1.37450122726203,-3.48176701679641,
24.2546114003997));
#35545=CARTESIAN_POINT('Ctrl Pts',(-1.39455787836581,-3.47461436152618,
24.2540386428268));
#35546=CARTESIAN_POINT('Ctrl Pts',(-1.4145370881139,-3.46730094250551,24.2534663728415));
#35547=CARTESIAN_POINT('Ctrl Pts',(-1.52840519986039,-3.42561935325375,
24.2502048172814));
#35548=CARTESIAN_POINT('Ctrl Pts',(-1.63991365982444,-3.37866812586214,
24.2469546926609));
#35549=CARTESIAN_POINT('Ctrl Pts',(-1.74863318528068,-3.32654324532194,
24.2437121916767));
#35550=CARTESIAN_POINT('Ctrl Pts',(-1.85558872732241,-3.27526409533814,
24.2405223005429));
#35551=CARTESIAN_POINT('Ctrl Pts',(-1.95984592910298,-3.2189775652086,24.2373397876639));
#35552=CARTESIAN_POINT('Ctrl Pts',(-2.06098377301333,-3.15772709883281,
24.2341610280672));
#35553=CARTESIAN_POINT('Ctrl Pts',(-2.15682437201784,-3.09968471667599,
24.2311487607293));
#35554=CARTESIAN_POINT('Ctrl Pts',(-2.24986433245661,-3.03718433413316,
24.2281398638026));
#35555=CARTESIAN_POINT('Ctrl Pts',(-2.33972491633012,-2.97022484402709,
24.2251312525923));
#35556=CARTESIAN_POINT('Ctrl Pts',(-2.39708388099203,-2.9274838906389,24.2232108241167));
#35557=CARTESIAN_POINT('Ctrl Pts',(-2.45314695486067,-2.88292530873872,
24.2212905120536));
#35558=CARTESIAN_POINT('Ctrl Pts',(-2.50788173230019,-2.8366336564438,24.2193695141552));
#35559=CARTESIAN_POINT('Ctrl Pts',(-2.53563831690701,-2.81315866990653,
24.2183953558013));
#35560=CARTESIAN_POINT('Ctrl Pts',(-2.56305323963533,-2.78923792330051,
24.2174210210771));
#35561=CARTESIAN_POINT('Ctrl Pts',(-2.59012178635459,-2.76488197889541,
24.2164464053624));
#35562=CARTESIAN_POINT('Ctrl Pts',(-2.60345465688749,-2.75288522647173,
24.2159663491083));
#35563=CARTESIAN_POINT('Ctrl Pts',(-2.61670472847459,-2.74078173073675,
24.2154861793416));
#35564=CARTESIAN_POINT('Ctrl Pts',(-2.62986751863965,-2.72857633888938,
24.2150060254729));
#35565=CARTESIAN_POINT('Ctrl Pts',(-2.71508215755265,-2.6495598047031,24.2118975554583));
#35566=CARTESIAN_POINT('Ctrl Pts',(-2.79636860051037,-2.56653035928709,
24.2087997059384));
#35567=CARTESIAN_POINT('Ctrl Pts',(-2.87364584295152,-2.47991615691849,
24.2057091871955));
#35568=CARTESIAN_POINT('Ctrl Pts',(-2.95372207710542,-2.39016477694134,
24.2025067294641));
#35569=CARTESIAN_POINT('Ctrl Pts',(-3.02949395217132,-2.29656378485085,
24.1993121431703));
#35570=CARTESIAN_POINT('Ctrl Pts',(-3.10083927390671,-2.19954365518354,
24.1961217680305));
#35571=CARTESIAN_POINT('Ctrl Pts',(-3.1729388167544,-2.1014978853154,24.1928976661062));
#35572=CARTESIAN_POINT('Ctrl Pts',(-3.24051817780072,-1.99995957525359,
24.1896778648424));
#35573=CARTESIAN_POINT('Ctrl Pts',(-3.30341172612255,-1.89533643715524,
24.1864585866407));
#35574=CARTESIAN_POINT('Ctrl Pts',(-3.34638934220069,-1.82384336382643,
24.1842587282087));
#35575=CARTESIAN_POINT('Ctrl Pts',(-3.38717808530971,-1.7509090628703,24.1820591140217));
#35576=CARTESIAN_POINT('Ctrl Pts',(-3.42571297641979,-1.67665668248674,
24.1798585386985));
#35577=CARTESIAN_POINT('Ctrl Pts',(-3.445014281687,-1.63946524845605,24.1787563174426));
#35578=CARTESIAN_POINT('Ctrl Pts',(-3.46374997985981,-1.60194306216562,
24.1776538550573));
#35579=CARTESIAN_POINT('Ctrl Pts',(-3.48191088985649,-1.56410523444394,
24.1765510000744));
#35580=CARTESIAN_POINT('Ctrl Pts',(-3.49096642636183,-1.54523823767566,
24.1760010858047));
#35581=CARTESIAN_POINT('Ctrl Pts',(-3.4998801459806,-1.52629016625364,24.1754509999921));
#35582=CARTESIAN_POINT('Ctrl Pts',(-3.50864077925426,-1.5072853111527,24.174901369431));
#35583=CARTESIAN_POINT('Ctrl Pts',(-3.56003841051657,-1.39578600463474,
24.171676749928));
#35584=CARTESIAN_POINT('Ctrl Pts',(-3.60624692934267,-1.28217850112835,
24.1684632179365));
#35585=CARTESIAN_POINT('Ctrl Pts',(-3.6471387300781,-1.1668916502069,24.1652570948759));
#35586=CARTESIAN_POINT('Ctrl Pts',(-3.6882879122029,-1.05087916017607,24.1620307918185));
#35587=CARTESIAN_POINT('Ctrl Pts',(-3.72405366249247,-0.933165324275529,
24.1588119912523));
#35588=CARTESIAN_POINT('Ctrl Pts',(-3.75426180619985,-0.814159485558989,
24.1555969446976));
#35589=CARTESIAN_POINT('Ctrl Pts',(-3.7841716362032,-0.696328862138458,
24.1524136476093));
#35590=CARTESIAN_POINT('Ctrl Pts',(-3.80863339059432,-0.577230809008665,
24.1492340307549));
#35591=CARTESIAN_POINT('Ctrl Pts',(-3.8274295805391,-0.457247749762826,
24.1460544556133));
#35592=CARTESIAN_POINT('Ctrl Pts',(-3.83933667583213,-0.381240339527709,
24.1440402439932));
#35593=CARTESIAN_POINT('Ctrl Pts',(-3.84896918346273,-0.304877515113294,
24.1420260491124));
#35594=CARTESIAN_POINT('Ctrl Pts',(-3.85626072121049,-0.2282555949368,24.14001094599));
#35595=CARTESIAN_POINT('Ctrl Pts',(-3.85942265273046,-0.195028959773208,
24.1391371086324));
#35596=CARTESIAN_POINT('Ctrl Pts',(-3.86214425712046,-0.161753603333563,
24.1382631004825));
#35597=CARTESIAN_POINT('Ctrl Pts',(-3.86441958153066,-0.128437410079632,
24.1373888461123));
#35598=CARTESIAN_POINT('Ctrl Pts',(-3.86591347492261,-0.106563236566722,
24.1368148432051));
#35599=CARTESIAN_POINT('Ctrl Pts',(-3.86721509040623,-0.0846675012688186,
24.1362406305225));
#35600=CARTESIAN_POINT('Ctrl Pts',(-3.86832155925171,-0.0627797067798542,
24.1356669009074));
#35601=CARTESIAN_POINT('Ctrl Pts',(-3.86941608558997,-0.0411281549512009,
24.1350993637576));
#35602=CARTESIAN_POINT('Ctrl Pts',(-3.87032006240666,-0.0194794249965481,
24.1345321693282));
#35603=CARTESIAN_POINT('Ctrl Pts',(-3.87103266938659,0.00216425178203038,
24.1339652975667));
#35604=CARTESIAN_POINT('',(0.349572399382967,3.92005776261121,24.058));
#35605=CARTESIAN_POINT('Ctrl Pts',(0.349418900843753,3.91916189049795,24.058));
#35606=CARTESIAN_POINT('Ctrl Pts',(0.226012228632792,3.91828850060595,24.0696807256992));
#35607=CARTESIAN_POINT('Ctrl Pts',(0.102952431902507,3.91191927543051,24.0813859465783));
#35608=CARTESIAN_POINT('Ctrl Pts',(-0.0193397180673949,3.90006603014558,
24.0931306202039));
#35609=CARTESIAN_POINT('Ctrl Pts',(-0.140580622517234,3.88831467750876,
24.1047743344831));
#35610=CARTESIAN_POINT('Ctrl Pts',(-0.261067870571708,3.87117297838718,
24.1164568261384));
#35611=CARTESIAN_POINT('Ctrl Pts',(-0.380377476123202,3.84860347157658,
24.1281926703091));
#35612=CARTESIAN_POINT('Ctrl Pts',(-0.496161715673067,3.82670084964599,
24.1395817431879));
#35613=CARTESIAN_POINT('Ctrl Pts',(-0.610837511562959,3.79968611836398,
24.1510210622381));
#35614=CARTESIAN_POINT('Ctrl Pts',(-0.723993462162786,3.76748283972913,
24.1625239483983));
#35615=CARTESIAN_POINT('Ctrl Pts',(-0.796757989013667,3.74677463728383,
24.1699208379514));
#35616=CARTESIAN_POINT('Ctrl Pts',(-0.868893538246561,3.72392009045816,
24.177344013056));
#35617=CARTESIAN_POINT('Ctrl Pts',(-0.940283456718533,3.69889010045098,
24.1847970158196));
#35618=CARTESIAN_POINT('Ctrl Pts',(-0.958852956027486,3.69237945592175,
24.1867356443071));
#35619=CARTESIAN_POINT('Ctrl Pts',(-0.977371972215163,3.6857215872702,24.188676290909));
#35620=CARTESIAN_POINT('Ctrl Pts',(-0.995838377017294,3.67891590798256,
24.1906190179632));
#35621=CARTESIAN_POINT('Ctrl Pts',(-1.01171569758055,3.67306441967942,24.1922893647652));
#35622=CARTESIAN_POINT('Ctrl Pts',(-1.0275456693922,3.66710676559807,24.1939603606721));
#35623=CARTESIAN_POINT('Ctrl Pts',(-1.04332469128769,3.6610438482036,24.1956317888384));
#35624=CARTESIAN_POINT('Ctrl Pts',(-1.15165978098886,3.619417269311,24.2071074253844));
#35625=CARTESIAN_POINT('Ctrl Pts',(-1.25763328276278,3.57281828211811,24.2186074516257));
#35626=CARTESIAN_POINT('Ctrl Pts',(-1.36087067794145,3.52121736057027,24.2301462409952));
#35627=CARTESIAN_POINT('Ctrl Pts',(-1.42681061365643,3.48825874665126,24.2375163129341));
#35628=CARTESIAN_POINT('Ctrl Pts',(-1.49163388388109,3.45325861360399,24.2449021988746));
#35629=CARTESIAN_POINT('Ctrl Pts',(-1.55523660610354,3.41620000588947,24.2523076441887));
#35630=CARTESIAN_POINT('Ctrl Pts',(-1.65681419035516,3.35701505726094,24.2641346103786));
#35631=CARTESIAN_POINT('Ctrl Pts',(-1.75528075449242,3.2925810923405,24.276011464936));
#35632=CARTESIAN_POINT('Ctrl Pts',(-1.8504118158475,3.22325698482629,24.2879534645915));
#35633=CARTESIAN_POINT('Ctrl Pts',(-1.94589009699015,3.15367985057672,24.2999390514679));
#35634=CARTESIAN_POINT('Ctrl Pts',(-2.03800893445419,3.07917596454707,24.3119902598576));
#35635=CARTESIAN_POINT('Ctrl Pts',(-2.12649675572721,3.00008130698686,24.3241225141588));
#35636=CARTESIAN_POINT('Ctrl Pts',(-2.15464819134299,2.97491820399908,24.3279822585951));
#35637=CARTESIAN_POINT('Ctrl Pts',(-2.18243175770649,2.94929030687597,24.3318502058895));
#35638=CARTESIAN_POINT('Ctrl Pts',(-2.20983765373967,2.92320808164845,24.3357268527022));
#35639=CARTESIAN_POINT('Ctrl Pts',(-2.22035441337321,2.91319926846847,24.3372144801333));
#35640=CARTESIAN_POINT('Ctrl Pts',(-2.23081386252428,2.90312511161636,24.3387031532638));
#35641=CARTESIAN_POINT('Ctrl Pts',(-2.24120927897093,2.89299245114185,24.3401919995702));
#35642=CARTESIAN_POINT('Ctrl Pts',(-2.32385350748897,2.81243714948096,24.3520284233442));
#35643=CARTESIAN_POINT('Ctrl Pts',(-2.40257000364209,2.72807711715171,24.3638921677319));
#35644=CARTESIAN_POINT('Ctrl Pts',(-2.47717616028223,2.64027648475023,24.3757991858546));
#35645=CARTESIAN_POINT('Ctrl Pts',(-2.55187618325755,2.55236538527792,24.3877211848877));
#35646=CARTESIAN_POINT('Ctrl Pts',(-2.62245590857137,2.46100416174114,24.3996865666148));
#35647=CARTESIAN_POINT('Ctrl Pts',(-2.68868744355177,2.36653097722017,24.4117113444476));
#35648=CARTESIAN_POINT('Ctrl Pts',(-2.75414075468922,2.27316785733437,24.4235948305405));
#35649=CARTESIAN_POINT('Ctrl Pts',(-2.81534772258566,2.17676464445494,24.4355363251252));
#35650=CARTESIAN_POINT('Ctrl Pts',(-2.8720401475082,2.07763370148774,24.4475512837449));
#35651=CARTESIAN_POINT('Ctrl Pts',(-2.90668546327039,2.01705377699881,24.4548937467957));
#35652=CARTESIAN_POINT('Ctrl Pts',(-2.93964383947717,1.95545494636204,24.462263645402));
#35653=CARTESIAN_POINT('Ctrl Pts',(-2.97084438937695,1.89290785453322,24.4696645068668));
#35654=CARTESIAN_POINT('Ctrl Pts',(-2.98845779797902,1.85759862156167,24.4738424587748));
#35655=CARTESIAN_POINT('Ctrl Pts',(-3.00551087593063,1.82198719162217,24.4780302780973));
#35656=CARTESIAN_POINT('Ctrl Pts',(-3.02198977071177,1.78608635326393,24.4822285994141));
#35657=CARTESIAN_POINT('Ctrl Pts',(-3.02877383007556,1.77130663521446,24.4839569714572));
#35658=CARTESIAN_POINT('Ctrl Pts',(-3.03545687173813,1.75648588102819,24.4856861859929));
#35659=CARTESIAN_POINT('Ctrl Pts',(-3.04203688563128,1.74162824455868,24.4874159221199));
#35660=CARTESIAN_POINT('Ctrl Pts',(-3.08710741956134,1.63985921800425,24.4992639412984));
#35661=CARTESIAN_POINT('Ctrl Pts',(-3.12737033179139,1.53631268431983,24.5111420689289));
#35662=CARTESIAN_POINT('Ctrl Pts',(-3.16262066493997,1.43129464400087,24.5230664886917));
#35663=CARTESIAN_POINT('Ctrl Pts',(-3.19738804194613,1.32771543001649,24.534827534913));
#35664=CARTESIAN_POINT('Ctrl Pts',(-3.22727942618041,1.22270400117247,24.5466336134818));
#35665=CARTESIAN_POINT('Ctrl Pts',(-3.2520488351859,1.1165476391786,24.5585002519648));
#35666=CARTESIAN_POINT('Ctrl Pts',(-3.27606482816892,1.01362025628536,24.5700059405533));
#35667=CARTESIAN_POINT('Ctrl Pts',(-3.29526569753493,0.909615922196257,
24.5815685609605));
#35668=CARTESIAN_POINT('Ctrl Pts',(-3.3093795070715,0.804800410213191,24.5932022664991));
#35669=CARTESIAN_POINT('Ctrl Pts',(-3.32346107752391,0.700224320202117,
24.6048093980635));
#35670=CARTESIAN_POINT('Ctrl Pts',(-3.33247901104835,0.594840172393064,
24.6164872903817));
#35671=CARTESIAN_POINT('Ctrl Pts',(-3.33611311329483,0.488924695430968,
24.62825));
#35672=CARTESIAN_POINT('',(-2.87185821835411,2.69480181882395,24.058));
#35673=CARTESIAN_POINT('Origin',(0.,0.,24.058));
#35674=CARTESIAN_POINT('Ctrl Pts',(-3.87103266938659,0.00216425178203038,
24.1339652975667));
#35675=CARTESIAN_POINT('Ctrl Pts',(-3.87507260628243,0.124867355795072,
24.1307515679672));
#35676=CARTESIAN_POINT('Ctrl Pts',(-3.87296594485587,0.247407050622043,
24.1275482085216));
#35677=CARTESIAN_POINT('Ctrl Pts',(-3.86453408452217,0.369385378863034,
24.1243515657403));
#35678=CARTESIAN_POINT('Ctrl Pts',(-3.85627040623579,0.488930725038259,
24.1212186832571));
#35679=CARTESIAN_POINT('Ctrl Pts',(-3.84193179212873,0.607937675272044,
24.1180922521689));
#35680=CARTESIAN_POINT('Ctrl Pts',(-3.82181791447054,0.726086832854309,
24.1149688332722));
#35681=CARTESIAN_POINT('Ctrl Pts',(-3.80134858411548,0.846323923823187,
24.1117902172779));
#35682=CARTESIAN_POINT('Ctrl Pts',(-3.77489779988944,0.965673358591756,
24.1086147208788));
#35683=CARTESIAN_POINT('Ctrl Pts',(-3.74272692791689,1.08379247292844,24.1054387192973));
#35684=CARTESIAN_POINT('Ctrl Pts',(-3.72259049299425,1.15772574589009,24.1034507921682));
#35685=CARTESIAN_POINT('Ctrl Pts',(-3.70021198877918,1.23117684933353,24.1014626671201));
#35686=CARTESIAN_POINT('Ctrl Pts',(-3.67564568396927,1.30405861901184,24.099473455278));
#35687=CARTESIAN_POINT('Ctrl Pts',(-3.66863540268018,1.32485628110409,24.0989058105034));
#35688=CARTESIAN_POINT('Ctrl Pts',(-3.66144692163609,1.3456075617141,24.0983380772297));
#35689=CARTESIAN_POINT('Ctrl Pts',(-3.65408139767167,1.36631038395308,24.097770234802));
#35690=CARTESIAN_POINT('Ctrl Pts',(-3.64822216373193,1.38277936556212,24.0973185192633));
#35691=CARTESIAN_POINT('Ctrl Pts',(-3.64225062386782,1.39921823302553,24.0968667189574));
#35692=CARTESIAN_POINT('Ctrl Pts',(-3.63617302699739,1.41561112341376,24.0964152327823));
#35693=CARTESIAN_POINT('Ctrl Pts',(-3.59274946073352,1.53273599648544,24.0931894281991));
#35694=CARTESIAN_POINT('Ctrl Pts',(-3.54385270980084,1.6476965516567,24.0899746657265));
#35695=CARTESIAN_POINT('Ctrl Pts',(-3.48981414813695,1.76015005122282,24.0867672641288));
#35696=CARTESIAN_POINT('Ctrl Pts',(-3.43581118825365,1.87252946397587,24.0835619756371));
#35697=CARTESIAN_POINT('Ctrl Pts',(-3.37667270383973,1.98240587688454,24.0803640383244));
#35698=CARTESIAN_POINT('Ctrl Pts',(-3.31267597495322,2.08942561654219,24.0771697782258));
#35699=CARTESIAN_POINT('Ctrl Pts',(-3.24861596071611,2.19655118632369,24.0739723593741));
#35700=CARTESIAN_POINT('Ctrl Pts',(-3.17968763174453,2.30081519811777,24.0707786250127));
#35701=CARTESIAN_POINT('Ctrl Pts',(-3.10612258128374,2.40183988004365,24.0675848902668));
#35702=CARTESIAN_POINT('Ctrl Pts',(-3.03255753082295,2.50286456196954,24.0643911555208));
#35703=CARTESIAN_POINT('Ctrl Pts',(-2.95435530373159,2.60065069905013,24.0611974203902));
#35704=CARTESIAN_POINT('Ctrl Pts',(-2.87170785494336,2.69478584831407,24.058));
#35705=CARTESIAN_POINT('',(-3.,-3.67394039744206E-16,25.));
#35706=CARTESIAN_POINT('',(-3.5,-4.28626379701574E-16,24.5));
#35707=CARTESIAN_POINT('Origin',(0.,0.,25.));
#35708=CARTESIAN_POINT('Ctrl Pts',(2.28870316125076,-3.20954854141214,-0.329233991005384));
#35709=CARTESIAN_POINT('Ctrl Pts',(3.35678472141098,-2.44790820113649,-0.27627001251076));
#35710=CARTESIAN_POINT('Ctrl Pts',(4.65420965805454,0.212376298523761,-0.170342055521513));
#35711=CARTESIAN_POINT('Ctrl Pts',(2.33824086975704,4.03501766412881,-0.011450120037642));
#35712=CARTESIAN_POINT('Ctrl Pts',(-2.12304297015552,4.14730362817999,0.147441815446229));
#35713=CARTESIAN_POINT('Ctrl Pts',(-4.6372363620278,0.464007918031343,0.3063337509301));
#35714=CARTESIAN_POINT('Ctrl Pts',(-2.9014296726223,-3.64766420030675,0.46522568641397));
#35715=CARTESIAN_POINT('Ctrl Pts',(1.49416848835415,-4.41423135892847,0.624117621897843));
#35716=CARTESIAN_POINT('Ctrl Pts',(4.52003362949604,-1.13548107251883,0.783009557381712));
#35717=CARTESIAN_POINT('Ctrl Pts',(3.40284567859094,3.18450706915039,0.941901492865584));
#35718=CARTESIAN_POINT('Ctrl Pts',(-0.833486649302243,4.58529649769934,
1.10079342834945));
#35719=CARTESIAN_POINT('Ctrl Pts',(-4.30580977810473,1.78325097864793,1.25968536383333));
#35720=CARTESIAN_POINT('Ctrl Pts',(-3.83137142736725,-2.65341337269076,
1.4185772993172));
#35721=CARTESIAN_POINT('Ctrl Pts',(0.154968444518143,-4.65788428232239,
1.57746923480107));
#35722=CARTESIAN_POINT('Ctrl Pts',(3.99925861063605,-2.3928822888867,1.73636117028494));
#35723=CARTESIAN_POINT('Ctrl Pts',(4.17776697308586,2.065482350747,1.89525310576881));
#35724=CARTESIAN_POINT('Ctrl Pts',(0.526867410782717,4.63058858791146,2.05414504125268));
#35725=CARTESIAN_POINT('Ctrl Pts',(-3.60696666633743,2.95122682044694,2.21303697673655));
#35726=CARTESIAN_POINT('Ctrl Pts',(-4.43459848935502,-1.43327725922984,
2.37192891222043));
#35727=CARTESIAN_POINT('Ctrl Pts',(-1.19740732042406,-4.50401613542707,
2.53082084770429));
#35728=CARTESIAN_POINT('Ctrl Pts',(3.13734620436576,-3.44630319202068,2.68971278318817));
#35729=CARTESIAN_POINT('Ctrl Pts',(4.59635878672289,0.770345758451563,2.84860471867204));
#35730=CARTESIAN_POINT('Ctrl Pts',(1.84227644659507,4.28088354832699,3.00749665415591));
#35731=CARTESIAN_POINT('Ctrl Pts',(-2.60046551010954,3.86749606027826,3.16638858963978));
#35732=CARTESIAN_POINT('Ctrl Pts',(-4.65957980074616,-0.0908992967115246,
3.32528052512365));
#35733=CARTESIAN_POINT('Ctrl Pts',(-2.44764980647886,-3.96597491173744,
3.48417246060752));
#35734=CARTESIAN_POINT('Ctrl Pts',(2.00783457505236,-4.20577542454142,3.64306439609139));
#35735=CARTESIAN_POINT('Ctrl Pts',(4.62290614147485,-0.590495894571063,
3.80195633157526));
#35736=CARTESIAN_POINT('Ctrl Pts',(3.00054907928836,3.56604147682096,3.96084826705914));
#35737=CARTESIAN_POINT('Ctrl Pts',(-1.37215855870585,4.45388902928383,4.119740202543));
#35738=CARTESIAN_POINT('Ctrl Pts',(-4.48712403609106,1.2592317017741,4.27863213802688));
#35739=CARTESIAN_POINT('Ctrl Pts',(-3.48912090296361,-3.08965724931931,
4.43752407351074));
#35740=CARTESIAN_POINT('Ctrl Pts',(0.707065439817984,-4.60651767152865,
4.59641600899462));
#35741=CARTESIAN_POINT('Ctrl Pts',(4.25514445682574,-1.9009713952631,4.75530794447848));
#35742=CARTESIAN_POINT('Ctrl Pts',(3.90289100181761,2.54703522197484,4.91419987996237));
#35743=CARTESIAN_POINT('Ctrl Pts',(-0.0268138566703869,4.6603892124167,
5.07309181544622));
#35744=CARTESIAN_POINT('Ctrl Pts',(-3.93194071153866,2.50195700103508,5.23198375093011));
#35745=CARTESIAN_POINT('Ctrl Pts',(-4.23298874115587,-1.9498084293931,5.39087568641397));
#35746=CARTESIAN_POINT('Ctrl Pts',(-0.654012576931896,-4.61434872363465,
5.54976762189785));
#35747=CARTESIAN_POINT('Ctrl Pts',(3.52444182282379,-3.04930425369769,5.70865955738171));
#35748=CARTESIAN_POINT('Ctrl Pts',(4.47233730108079,1.31078055350635,5.86755149286558));
#35749=CARTESIAN_POINT('Ctrl Pts',(1.32081792323409,4.46938324690933,6.02644342834946));
#35750=CARTESIAN_POINT('Ctrl Pts',(-3.04138397969982,3.531278816819,6.18533536383333));
#35751=CARTESIAN_POINT('Ctrl Pts',(-4.61580539333909,-0.643651431219671,
6.3442272993172));
#35752=CARTESIAN_POINT('Ctrl Pts',(-1.95930683639269,-4.22860063318286,
6.50311923480107));
#35753=CARTESIAN_POINT('Ctrl Pts',(2.4931232462982,-3.93754785023079,6.66201117028494));
#35754=CARTESIAN_POINT('Ctrl Pts',(4.66031726875216,-0.037276650332675,
6.82090310576881));
#35755=CARTESIAN_POINT('Ctrl Pts',(2.55579103409072,3.8971629147562,6.97979504125268));
#35756=CARTESIAN_POINT('Ctrl Pts',(-1.89141354276916,4.25940153123874,7.13868697673655));
#35757=CARTESIAN_POINT('Ctrl Pts',(-4.60491865684703,0.717405574212831,
7.29757891222042));
#35758=CARTESIAN_POINT('Ctrl Pts',(-3.09748275458741,-3.48217563875277,
7.45647084770429));
#35759=CARTESIAN_POINT('Ctrl Pts',(1.24915465816929,-4.48993978067229,7.61536278318817));
#35760=CARTESIAN_POINT('Ctrl Pts',(4.45079722404066,-1.38215435627192,7.77425471867203));
#35761=CARTESIAN_POINT('Ctrl Pts',(3.57276890790401,2.99253553442627,7.93314665415592));
#35762=CARTESIAN_POINT('Ctrl Pts',(-0.580115697571088,4.62422019063984,
8.09203858963977));
#35763=CARTESIAN_POINT('Ctrl Pts',(-4.20125711178304,2.01727174044104,8.25093052512366));
#35764=CARTESIAN_POINT('Ctrl Pts',(-3.97146004374031,-2.43873978010442,
8.40982246060752));
#35765=CARTESIAN_POINT('Ctrl Pts',(-0.101360107710164,-4.65936398263266,
8.56871439609139));
#35766=CARTESIAN_POINT('Ctrl Pts',(3.86164810052541,-2.60914172512687,8.72760633157527));
#35767=CARTESIAN_POINT('Ctrl Pts',(4.28500879860717,1.83266095881065,8.88649826705913));
#35768=CARTESIAN_POINT('Ctrl Pts',(0.78066289832912,4.59461772438818,9.04539020254301));
#35769=CARTESIAN_POINT('Ctrl Pts',(-3.43925091813584,3.14507547066701,9.20428213802687));
#35770=CARTESIAN_POINT('Ctrl Pts',(-4.50669313898401,-1.18729252719113,
9.36317407351076));
#35771=CARTESIAN_POINT('Ctrl Pts',(-1.44322940124376,-4.431369482392,9.52206600899461));
#35772=CARTESIAN_POINT('Ctrl Pts',(2.94312115158416,-3.61358332976944,9.6809579444785));
#35773=CARTESIAN_POINT('Ctrl Pts',(4.63176047203213,0.516470254526036,9.83984987996235));
#35774=CARTESIAN_POINT('Ctrl Pts',(2.07485514530555,4.17311906373262,9.99874181544625));
#35775=CARTESIAN_POINT('Ctrl Pts',(-2.3838951082054,4.00462116899514,10.1576337509301));
#35776=CARTESIAN_POINT('Ctrl Pts',(-4.65752953433707,0.165424396228235,
10.316525686414));
#35777=CARTESIAN_POINT('Ctrl Pts',(-2.6619989846541,-3.82540298528012,10.4754176218978));
#35778=CARTESIAN_POINT('Ctrl Pts',(1.77356178859607,-4.30980570050686,10.6343095573817));
#35779=CARTESIAN_POINT('Ctrl Pts',(4.58344787433293,-0.843772586282874,
10.7932014928656));
#35780=CARTESIAN_POINT('Ctrl Pts',(3.19207340137333,3.39567577874192,10.9520934283495));
#35781=CARTESIAN_POINT('Ctrl Pts',(-1.12520585971602,4.52259420768106,11.1109853638333));
#35782=CARTESIAN_POINT('Ctrl Pts',(-4.41110369606797,1.50403150785647,11.2698772993172));
#35783=CARTESIAN_POINT('Ctrl Pts',(-3.65371436373851,-2.89315017624395,
11.4287692348011));
#35784=CARTESIAN_POINT('Ctrl Pts',(0.452727138482009,-4.63842481152508,
11.5876611702849));
#35785=CARTESIAN_POINT('Ctrl Pts',(4.14419181039819,-2.13204616101957,11.7465531057688));
#35786=CARTESIAN_POINT('Ctrl Pts',(4.03702495468236,2.32859960262844,11.9054450412527));
#35787=CARTESIAN_POINT('Ctrl Pts',(0.229457400278859,4.65481427078963,12.0643369767365));
#35788=CARTESIAN_POINT('Ctrl Pts',(-3.78843442356625,2.7143528164975,12.2232289122204));
#35789=CARTESIAN_POINT('Ctrl Pts',(-4.33378754743687,-1.71412720874813,
12.3821208477043));
#35790=CARTESIAN_POINT('Ctrl Pts',(-0.906722702996628,-4.57141121908323,
12.5410127831882));
#35791=CARTESIAN_POINT('Ctrl Pts',(3.35145846134476,-3.23846765862655,12.699904718672));
#35792=CARTESIAN_POINT('Ctrl Pts',(4.53763997961045,1.06290639735133,12.8587966541559));
#35793=CARTESIAN_POINT('Ctrl Pts',(1.56454917743418,4.39000369766127,13.0176885896398));
#35794=CARTESIAN_POINT('Ctrl Pts',(-2.84263205873703,3.69315442037428,13.1765805251236));
#35795=CARTESIAN_POINT('Ctrl Pts',(-4.6442119487827,-0.388898404308158,
13.3354724606075));
#35796=CARTESIAN_POINT('Ctrl Pts',(-2.1888339718237,-4.11448082239789,13.4943643960914));
#35797=CARTESIAN_POINT('Ctrl Pts',(2.27286372066084,-4.06866527271454,13.6532563315753));
#35798=CARTESIAN_POINT('Ctrl Pts',(4.65121870549125,-0.293447010170337,
13.8121482670591));
#35799=CARTESIAN_POINT('Ctrl Pts',(2.76619331968842,3.75074940674537,13.971040202543));
#35800=CARTESIAN_POINT('Ctrl Pts',(-1.65436845932101,4.35694980403646,14.1299321380269));
#35801=CARTESIAN_POINT('Ctrl Pts',(-4.55851003496805,0.969501343570532,
14.2888240735108));
#35802=CARTESIAN_POINT('Ctrl Pts',(-3.28424946851144,-3.30660732816461,
14.4477160089946));
#35803=CARTESIAN_POINT('Ctrl Pts',(1.00040592194765,-4.55182760936985,14.6066079444785));
#35804=CARTESIAN_POINT('Ctrl Pts',(4.36807347752778,-1.62477096509257,14.7654998799624));
#35805=CARTESIAN_POINT('Ctrl Pts',(3.73189604091493,2.79157635286821,14.9243918154462));
#35806=CARTESIAN_POINT('Ctrl Pts',(-0.324996123065272,4.64912078936244,
15.0832837509301));
#35807=CARTESIAN_POINT('Ctrl Pts',(-4.08399171856711,2.24520783821119,15.242175686414));
#35808=CARTESIAN_POINT('Ctrl Pts',(-4.09953613938831,-2.21669800287246,
15.4010676218978));
#35809=CARTESIAN_POINT('Ctrl Pts',(-0.357381124417536,-4.64674351842229,
15.5599595573817));
#35810=CARTESIAN_POINT('Ctrl Pts',(3.71235506167248,-2.81751069033718,15.7188514928656));
#35811=CARTESIAN_POINT('Ctrl Pts',(4.37928808994288,1.59429684167472,15.8777434283495));
#35812=CARTESIAN_POINT('Ctrl Pts',(1.03209663553355,4.54474676181302,16.0366353638333));
#35813=CARTESIAN_POINT('Ctrl Pts',(-3.26113086128664,3.32941017293654,16.1955272993172));
#35814=CARTESIAN_POINT('Ctrl Pts',(-4.56515441384568,-0.937716253370267,
16.3544192348011));
#35815=CARTESIAN_POINT('Ctrl Pts',(-1.68468548190361,-4.34531718303195,
16.5133111702849));
#35816=CARTESIAN_POINT('Ctrl Pts',(2.7399927141092,-3.76993189868439,16.6722031057688));
#35817=CARTESIAN_POINT('Ctrl Pts',(4.65315040492198,0.261032379723303,16.8310950412527));
#35818=CARTESIAN_POINT('Ctrl Pts',(2.30115709895892,4.05273026489556,16.9899869767366));
#35819=CARTESIAN_POINT('Ctrl Pts',(-2.16011307112194,4.12963171651633,17.1488789122204));
#35820=CARTESIAN_POINT('Ctrl Pts',(-4.64138955591407,0.421247652030533,
17.3077708477043));
#35821=CARTESIAN_POINT('Ctrl Pts',(-2.86829522348703,-3.67325864934817,
17.4666627831881));
#35822=CARTESIAN_POINT('Ctrl Pts',(1.53392371633779,-4.40079818061975,17.6255547186721));
#35823=CARTESIAN_POINT('Ctrl Pts',(4.53012400247882,-1.09449674108904,17.7844466541559));
#35824=CARTESIAN_POINT('Ctrl Pts',(3.37394123127184,3.21503766105686,17.9433385896398));
#35825=CARTESIAN_POINT('Ctrl Pts',(-0.874849247264209,4.57761787272052,
18.1022305251236));
#35826=CARTESIAN_POINT('Ctrl Pts',(-4.32173911776226,1.7442813970492,18.2611224606075));
#35827=CARTESIAN_POINT('Ctrl Pts',(-3.80725480047823,-2.68789089777271,
18.4200143960914));
#35828=CARTESIAN_POINT('Ctrl Pts',(0.197019270876202,-4.65630003339433,
18.5789063315753));
#35829=CARTESIAN_POINT('Ctrl Pts',(4.02070237343572,-2.35667117314485,18.7377982670591));
#35830=CARTESIAN_POINT('Ctrl Pts',(4.15894631253379,2.10311962655031,18.896690202543));
#35831=CARTESIAN_POINT('Ctrl Pts',(0.485034514796087,4.63515783048493,19.0555821380269));
#35832=CARTESIAN_POINT('Ctrl Pts',(-3.63346756353596,2.9185373149568,19.2144740735107));
#35833=CARTESIAN_POINT('Ctrl Pts',(-4.42147600817412,-1.47326050087259,
19.3733660089946));
#35834=CARTESIAN_POINT('Ctrl Pts',(-1.15668985931864,-4.51464452234266,
19.5322579444785));
#35835=CARTESIAN_POINT('Ctrl Pts',(3.16833644438965,-3.41783422201423,19.6911498799624));
#35836=CARTESIAN_POINT('Ctrl Pts',(4.58921562907606,0.811816792908698,19.8500418154462));
#35837=CARTESIAN_POINT('Ctrl Pts',(1.80354743972281,4.29734374053261,20.0089337509301));
#35838=CARTESIAN_POINT('Ctrl Pts',(-2.63528075670629,3.84385768827679,20.167825686414));
#35839=CARTESIAN_POINT('Ctrl Pts',(-4.65856908001299,-0.132968903128038,
20.3267176218978));
#35840=CARTESIAN_POINT('Ctrl Pts',(-2.41173956046629,-3.98791409989842,
20.4856095573818));
#35841=CARTESIAN_POINT('Ctrl Pts',(2.04572844434392,-4.18747438603111,20.6445014928655));
#35842=CARTESIAN_POINT('Ctrl Pts',(4.62804952678526,-0.548729644870818,
20.8033934283495));
#35843=CARTESIAN_POINT('Ctrl Pts',(2.96822745143777,3.59298932040533,20.9622853638333));
#35844=CARTESIAN_POINT('Ctrl Pts',(-1.4123186453351,4.44131767923527,21.1211772993172));
#35845=CARTESIAN_POINT('Ctrl Pts',(-4.49831129151882,1.21866419573831,21.2800692348011));
#35846=CARTESIAN_POINT('Ctrl Pts',(-3.46108076274892,-3.12103598071567,
21.438961170285));
#35847=CARTESIAN_POINT('Ctrl Pts',(0.748630655069918,-4.59994560901591,
21.5978531057688));
#35848=CARTESIAN_POINT('Ctrl Pts',(4.2721359622726,-1.86247217365839,21.7567450412527));
#35849=CARTESIAN_POINT('Ctrl Pts',(3.8797330719726,2.58217180475713,21.9156369767366));
#35850=CARTESIAN_POINT('Ctrl Pts',(-0.0688923048847857,4.65995794755513,
22.0745289122204));
#35851=CARTESIAN_POINT('Ctrl Pts',(-3.95437371638077,2.46635025785298,22.2334208477043));
#35852=CARTESIAN_POINT('Ctrl Pts',(-4.21520658614674,-1.98794734397253,
22.3923127831882));
#35853=CARTESIAN_POINT('Ctrl Pts',(-0.612328551070793,-4.62007178368083,
22.551204718672));
#35854=CARTESIAN_POINT('Ctrl Pts',(3.55184600275178,-3.01734516931811,22.7100966541559));
#35855=CARTESIAN_POINT('Ctrl Pts',(4.46029188758379,1.35108854037515,22.8689885896398));
#35856=CARTESIAN_POINT('Ctrl Pts',(1.28046065203078,4.48116776123978,23.0278805251236));
#35857=CARTESIAN_POINT('Ctrl Pts',(-3.07324571308582,3.50359559093557,23.1867724606075));
#35858=CARTESIAN_POINT('Ctrl Pts',(-4.60961384635985,-0.685155565682453,
23.3456643960914));
#35859=CARTESIAN_POINT('Ctrl Pts',(-1.9214110817744,-4.24640173773129,23.5045563315753));
#35860=CARTESIAN_POINT('Ctrl Pts',(2.52927486439223,-3.91433686410129,23.6634482670591));
#35861=CARTESIAN_POINT('Ctrl Pts',(4.65912272890548,0.00377285541425606,
23.822340202543));
#35862=CARTESIAN_POINT('Ctrl Pts',(2.52310591890791,3.92207527169042,23.9812321380269));
#35863=CARTESIAN_POINT('Ctrl Pts',(-1.93519005785514,4.23813764208779,24.1401240735107));
#35864=CARTESIAN_POINT('Ctrl Pts',(-3.71011270200011,1.86957801804229,24.2460520305));
#35865=CARTESIAN_POINT('Ctrl Pts',(-3.90033599543508,0.571614487844223,
24.2990160089946));
#35866=CARTESIAN_POINT('Ctrl Pts',(2.17834184062643,-3.05478403475391,-0.219489327336923));
#35867=CARTESIAN_POINT('Ctrl Pts',(3.19492048266714,-2.32987000971945,-0.166525348842299));
#35868=CARTESIAN_POINT('Ctrl Pts',(4.42978355814708,0.202135508380576,-0.0605973918530519));
#35869=CARTESIAN_POINT('Ctrl Pts',(2.22549083965568,3.84044901682883,0.0982945436308193));
#35870=CARTESIAN_POINT('Ctrl Pts',(-2.02066978786809,3.94732054903492,0.25718647911469));
#35871=CARTESIAN_POINT('Ctrl Pts',(-4.41362871485661,0.441633445237732,
0.416078414598561));
#35872=CARTESIAN_POINT('Ctrl Pts',(-2.76152266511234,-3.4717737462035,0.574970350082432));
#35873=CARTESIAN_POINT('Ctrl Pts',(1.42211964846881,-4.20137701828676,0.733862285566304));
#35874=CARTESIAN_POINT('Ctrl Pts',(4.30207750086251,-1.08072814831761,0.892754221050174));
#35875=CARTESIAN_POINT('Ctrl Pts',(3.23876037940132,3.03095006287751,1.05164615653404));
#35876=CARTESIAN_POINT('Ctrl Pts',(-0.793295903338713,4.36419339201584,
1.21053809201792));
#35877=CARTESIAN_POINT('Ctrl Pts',(-4.09818352865738,1.69726257423614,1.36943002750179));
#35878=CARTESIAN_POINT('Ctrl Pts',(-3.64662260642559,-2.52546571703568,
1.52832196298566));
#35879=CARTESIAN_POINT('Ctrl Pts',(0.147495862454333,-4.43328099194573,
1.68721389846953));
#35880=CARTESIAN_POINT('Ctrl Pts',(3.80641426574215,-2.27749744826117,1.8461058339534));
#35881=CARTESIAN_POINT('Ctrl Pts',(3.97631495072816,1.96588474289028,2.00499776943727));
#35882=CARTESIAN_POINT('Ctrl Pts',(0.501461851760338,4.40730149656556,2.16388970492114));
#35883=CARTESIAN_POINT('Ctrl Pts',(-3.43303864828577,2.80891859328985,2.32278164040501));
#35884=CARTESIAN_POINT('Ctrl Pts',(-4.22076204520191,-1.36416459585457,
2.48167357588889));
#35885=CARTESIAN_POINT('Ctrl Pts',(-1.13966831108264,-4.28683237073678,
2.64056551137275));
#35886=CARTESIAN_POINT('Ctrl Pts',(2.98606329610941,-3.28012237050456,2.79945744685663));
#35887=CARTESIAN_POINT('Ctrl Pts',(4.37472225720076,0.733199667739815,2.9583493823405));
#35888=CARTESIAN_POINT('Ctrl Pts',(1.75344183272134,4.07445924226969,3.11724131782437));
#35889=CARTESIAN_POINT('Ctrl Pts',(-2.47507100164175,3.68100530868232,3.27613325330824));
#35890=CARTESIAN_POINT('Ctrl Pts',(-4.43489475243097,-0.0865161304718975,
3.43502518879211));
#35891=CARTESIAN_POINT('Ctrl Pts',(-2.32962407485832,-3.77473550759247,
3.59391712427598));
#35892=CARTESIAN_POINT('Ctrl Pts',(1.91101674430454,-4.00297283399139,3.75280905975985));
#35893=CARTESIAN_POINT('Ctrl Pts',(4.39998949787803,-0.562022168553895,
3.91170099524372));
#35894=CARTESIAN_POINT('Ctrl Pts',(2.85586253164215,3.39408687237674,4.07059293072759));
#35895=CARTESIAN_POINT('Ctrl Pts',(-1.30599304051693,4.23912239483862,4.22948486621146));
#35896=CARTESIAN_POINT('Ctrl Pts',(-4.27075480883071,1.19851151930018,4.38837680169534));
#35897=CARTESIAN_POINT('Ctrl Pts',(-3.32087541041203,-2.94067390360441,
4.5472687371792));
#35898=CARTESIAN_POINT('Ctrl Pts',(0.672970727569009,-4.38439128034066,
4.70616067266308));
#35899=CARTESIAN_POINT('Ctrl Pts',(4.04996129037005,-1.8093065095749,4.86505260814695));
#35900=CARTESIAN_POINT('Ctrl Pts',(3.7146935053026,2.42421712326595,5.02394454363082));
#35901=CARTESIAN_POINT('Ctrl Pts',(-0.0255208918668632,4.43566513425159,
5.18283647911469));
#35902=CARTESIAN_POINT('Ctrl Pts',(-3.7423424373331,2.38131257520723,5.34172841459856));
#35903=CARTESIAN_POINT('Ctrl Pts',(-4.02887392383437,-1.85578862076283,
5.50062035008243));
#35904=CARTESIAN_POINT('Ctrl Pts',(-0.622476074987428,-4.39184471892869,
5.6595122855663));
#35905=CARTESIAN_POINT('Ctrl Pts',(3.35449315468027,-2.90226673038711,5.81840422105018));
#35906=CARTESIAN_POINT('Ctrl Pts',(4.25668109053274,1.24757468418137,5.97729615653404));
#35907=CARTESIAN_POINT('Ctrl Pts',(1.25712805170321,4.25386948092336,6.13618809201792));
#35908=CARTESIAN_POINT('Ctrl Pts',(-2.89472837218891,3.36100046866316,6.29508002750178));
#35909=CARTESIAN_POINT('Ctrl Pts',(-4.3932311479855,-0.61261454396674,6.45397196298565));
#35910=CARTESIAN_POINT('Ctrl Pts',(-1.86482901435204,-4.0246974105317,6.61286389846953));
#35911=CARTESIAN_POINT('Ctrl Pts',(2.37290478433289,-3.74767919966474,6.77175583395341));
#35912=CARTESIAN_POINT('Ctrl Pts',(4.43559665971225,-0.0354791693710577,
6.93064776943726));
#35913=CARTESIAN_POINT('Ctrl Pts',(2.43255072991432,3.7092416267349,7.08953970492115));
#35914=CARTESIAN_POINT('Ctrl Pts',(-1.80020953695449,4.05401308855407,7.248431640405));
#35915=CARTESIAN_POINT('Ctrl Pts',(-4.38286937018484,0.682812260438543,
7.40732357588889));
#35916=CARTESIAN_POINT('Ctrl Pts',(-2.94812206282321,-3.31426504700587,
7.56621551137276));
#35917=CARTESIAN_POINT('Ctrl Pts',(1.18892039097656,-4.27343477814157,7.72510744685661));
#35918=CARTESIAN_POINT('Ctrl Pts',(4.23617967651747,-1.31550684048772,7.88399938234051));
#35919=CARTESIAN_POINT('Ctrl Pts',(3.40048990657371,2.84823540010302,8.04289131782437));
#35920=CARTESIAN_POINT('Ctrl Pts',(-0.552142504899003,4.40124018356118,
8.20178325330824));
#35921=CARTESIAN_POINT('Ctrl Pts',(-3.99867239438119,1.91999884935475,8.36067518879212));
#35922=CARTESIAN_POINT('Ctrl Pts',(-3.7799561464003,-2.3211436901666,8.51956712427598));
#35923=CARTESIAN_POINT('Ctrl Pts',(-0.0964725209165242,-4.43468934107201,
8.67845905975986));
#35924=CARTESIAN_POINT('Ctrl Pts',(3.67543933768719,-2.48332884936554,8.83735099524372));
#35925=CARTESIAN_POINT('Ctrl Pts',(4.0783855728837,1.74429000398553,8.9962429307276));
#35926=CARTESIAN_POINT('Ctrl Pts',(0.743019314888223,4.37306514893305,9.15513486621146));
#35927=CARTESIAN_POINT('Ctrl Pts',(-3.2734101574334,2.99341985700662,9.31402680169534));
#35928=CARTESIAN_POINT('Ctrl Pts',(-4.28938028911884,-1.13004125341886,
9.4729187371792));
#35929=CARTESIAN_POINT('Ctrl Pts',(-1.37363684534497,-4.2176887410311,9.63181067266308));
#35930=CARTESIAN_POINT('Ctrl Pts',(2.80120377997153,-3.43933625605043,9.79070260814695));
#35931=CARTESIAN_POINT('Ctrl Pts',(4.40841687240619,0.491566046624494,9.94959454363082));
#35932=CARTESIAN_POINT('Ctrl Pts',(1.97480558107332,3.97189116367397,10.1084864791147));
#35933=CARTESIAN_POINT('Ctrl Pts',(-2.26894362964508,3.81151824141021,10.2673784145986));
#35934=CARTESIAN_POINT('Ctrl Pts',(-4.43294334991667,0.157447627925427,
10.4262703500824));
#35935=CARTESIAN_POINT('Ctrl Pts',(-2.53363733058688,-3.6409419627572,10.5851622855663));
#35936=CARTESIAN_POINT('Ctrl Pts',(1.68804059715796,-4.10198676758668,10.7440542210502));
#35937=CARTESIAN_POINT('Ctrl Pts',(4.36243390931193,-0.803085852194621,
10.902946156534));
#35938=CARTESIAN_POINT('Ctrl Pts',(3.03815154638153,3.23193621229276,11.0618380920179));
#35939=CARTESIAN_POINT('Ctrl Pts',(-1.07094840651941,4.30451460790682,11.2207300275018));
#35940=CARTESIAN_POINT('Ctrl Pts',(-4.19840017140343,1.43150707293723,11.3796219629857));
#35941=CARTESIAN_POINT('Ctrl Pts',(-3.47753217061135,-2.75364240624537,
11.5385138984695));
#35942=CARTESIAN_POINT('Ctrl Pts',(0.430896625145342,-4.41475985729101,
11.6974058339534));
#35943=CARTESIAN_POINT('Ctrl Pts',(3.94435878318021,-2.02923884465551,11.8562977694373));
#35944=CARTESIAN_POINT('Ctrl Pts',(3.84235951578439,2.21631447465625,12.0151897049212));
#35945=CARTESIAN_POINT('Ctrl Pts',(0.218392959004639,4.43035901644177,12.174081640405));
#35946=CARTESIAN_POINT('Ctrl Pts',(-3.60575602596446,2.58346665941922,12.3329735758889));
#35947=CARTESIAN_POINT('Ctrl Pts',(-4.12481220928992,-1.63147195415751,
12.4918655113728));
#35948=CARTESIAN_POINT('Ctrl Pts',(-0.86300051278999,-4.35097766186335,
12.6507574468566));
#35949=CARTESIAN_POINT('Ctrl Pts',(3.18985105498742,-3.08230867145154,12.8096493823405));
#35950=CARTESIAN_POINT('Ctrl Pts',(4.31883487235755,1.01165302570498,12.9685413178244));
#35951=CARTESIAN_POINT('Ctrl Pts',(1.48910657905504,4.17831761541948,13.1274332533082));
#35952=CARTESIAN_POINT('Ctrl Pts',(-2.70556027356073,3.51507042678234,13.2863251887921));
#35953=CARTESIAN_POINT('Ctrl Pts',(-4.42026793865305,-0.3701457140446,13.445217124276));
#35954=CARTESIAN_POINT('Ctrl Pts',(-2.08328834587812,-3.91608045972475,
13.6041090597598));
#35955=CARTESIAN_POINT('Ctrl Pts',(2.16326617823678,-3.87247413693191,13.7630009952437));
#35956=CARTESIAN_POINT('Ctrl Pts',(4.4269368293872,-0.279296988392094,13.9218929307276));
#35957=CARTESIAN_POINT('Ctrl Pts',(2.63280741231888,3.56988818154694,14.0807848662115));
#35958=CARTESIAN_POINT('Ctrl Pts',(-1.57459477304264,4.14685758132787,14.2396768016953));
#35959=CARTESIAN_POINT('Ctrl Pts',(-4.33869857315167,0.922751965829036,
14.3985687371792));
#35960=CARTESIAN_POINT('Ctrl Pts',(-3.12588288137982,-3.14716264451114,
14.5574606726631));
#35961=CARTESIAN_POINT('Ctrl Pts',(0.952166324705068,-4.33233837427404,
14.716352608147));
#35962=CARTESIAN_POINT('Ctrl Pts',(4.15744487102007,-1.54642447068669,14.8752445436308));
#35963=CARTESIAN_POINT('Ctrl Pts',(3.55194392546324,2.65696647503773,15.0341364791147));
#35964=CARTESIAN_POINT('Ctrl Pts',(-0.309324802316237,4.4249400748238,15.1930284145986));
#35965=CARTESIAN_POINT('Ctrl Pts',(-3.88706154120257,2.13694386309366,15.3519203500824));
#35966=CARTESIAN_POINT('Ctrl Pts',(-3.90185640968376,-2.10980877268997,
15.5108122855663));
#35967=CARTESIAN_POINT('Ctrl Pts',(-0.340148198136544,-4.42267743594467,
15.6697042210502));
#35968=CARTESIAN_POINT('Ctrl Pts',(3.53334521270251,-2.68165025813993,15.8285961565341));
#35969=CARTESIAN_POINT('Ctrl Pts',(4.168118714559,1.51741981022156,15.9874880920179));
#35970=CARTESIAN_POINT('Ctrl Pts',(0.982328911331549,4.32559896535404,16.1463800275018));
#35971=CARTESIAN_POINT('Ctrl Pts',(-3.10387905394275,3.16886593556829,16.3052719629857));
#35972=CARTESIAN_POINT('Ctrl Pts',(-4.3450225599225,-0.892499553430768,
16.4641638984695));
#35973=CARTESIAN_POINT('Ctrl Pts',(-1.60344990807853,-4.13578588558361,
16.6230558339534));
#35974=CARTESIAN_POINT('Ctrl Pts',(2.60787020056101,-3.5881456932705,16.7819477694373));
#35975=CARTESIAN_POINT('Ctrl Pts',(4.42877538222566,0.248445392192659,16.9408397049211));
#35976=CARTESIAN_POINT('Ctrl Pts',(2.19019524916345,3.85730751556724,17.099731640405));
#35977=CARTESIAN_POINT('Ctrl Pts',(-2.0559523676882,3.9305007773701,17.2586235758889));
#35978=CARTESIAN_POINT('Ctrl Pts',(-4.41758164163537,0.400935080275903,
17.4175155113728));
#35979=CARTESIAN_POINT('Ctrl Pts',(-2.72998595989888,-3.49613403030616,
17.5764074468566));
#35980=CARTESIAN_POINT('Ctrl Pts',(1.4599578784178,-4.18859158815413,17.7352993823405));
#35981=CARTESIAN_POINT('Ctrl Pts',(4.31168131582116,-1.04172008231973,17.8941913178244));
#35982=CARTESIAN_POINT('Ctrl Pts',(3.2112497052163,3.06000846891939,18.0530832533082));
#35983=CARTESIAN_POINT('Ctrl Pts',(-0.832663995847618,4.35688503051531,
18.2119751887921));
#35984=CARTESIAN_POINT('Ctrl Pts',(-4.11334475517948,1.66017210678477,18.370867124276));
#35985=CARTESIAN_POINT('Ctrl Pts',(-3.62366888385615,-2.55828073504186,
18.5297590597599));
#35986=CARTESIAN_POINT('Ctrl Pts',(0.187518996969786,-4.4317731355385,18.6886509952437));
#35987=CARTESIAN_POINT('Ctrl Pts',(3.82682400979189,-2.24303243337775,18.8475429307276));
#35988=CARTESIAN_POINT('Ctrl Pts',(3.95840182287352,2.00170714836323,19.0064348662115));
#35989=CARTESIAN_POINT('Ctrl Pts',(0.461646139008639,4.41165041015396,19.1653268016953));
#35990=CARTESIAN_POINT('Ctrl Pts',(-3.45826167159393,2.77780537652842,19.3242187371792));
#35991=CARTESIAN_POINT('Ctrl Pts',(-4.20827233037425,-1.40221984463863,
19.4831106726631));
#35992=CARTESIAN_POINT('Ctrl Pts',(-1.10091424691577,-4.29694825658366,
19.6420026081469));
#35993=CARTESIAN_POINT('Ctrl Pts',(3.01555918602559,-3.25302617490586,19.8008945436308));
#35994=CARTESIAN_POINT('Ctrl Pts',(4.36792354278479,0.772670967933531,19.9597864791147));
#35995=CARTESIAN_POINT('Ctrl Pts',(1.71658033947744,4.09012572361745,20.1186784145985));
#35996=CARTESIAN_POINT('Ctrl Pts',(-2.5082074562233,3.65850677953844,20.2775703500824));
#35997=CARTESIAN_POINT('Ctrl Pts',(-4.43393276867548,-0.126557139470934,
20.4364622855663));
#35998=CARTESIAN_POINT('Ctrl Pts',(-2.29544542175872,-3.79561678758089,
20.5953542210502));
#35999=CARTESIAN_POINT('Ctrl Pts',(1.94708337032167,-3.98555427199136,20.7542461565341));
#36000=CARTESIAN_POINT('Ctrl Pts',(4.40488486902698,-0.52226988840308,20.9131380920179));
#36001=CARTESIAN_POINT('Ctrl Pts',(2.82509945345179,3.41973529030544,21.0720300275018));
#36002=CARTESIAN_POINT('Ctrl Pts',(-1.34421660681807,4.22715723558706,21.2309219629857));
#36003=CARTESIAN_POINT('Ctrl Pts',(-4.28140261453686,1.15990017936594,21.3898138984695));
#36004=CARTESIAN_POINT('Ctrl Pts',(-3.29418736642239,-2.97053955182989,
21.5487058339534));
#36005=CARTESIAN_POINT('Ctrl Pts',(0.712531667157375,-4.37813612283788,
21.7075977694373));
#36006=CARTESIAN_POINT('Ctrl Pts',(4.06613346502197,-1.7726637213475,21.8664897049211));
#36007=CARTESIAN_POINT('Ctrl Pts',(3.69265225138302,2.45765941919457,22.025381640405));
#36008=CARTESIAN_POINT('Ctrl Pts',(-0.0655703163120924,4.43525466499184,
22.1842735758889));
#36009=CARTESIAN_POINT('Ctrl Pts',(-3.76369372215058,2.34742279002442,22.3431655113728));
#36010=CARTESIAN_POINT('Ctrl Pts',(-4.0119492247608,-1.89208847597824,22.5020574468566));
#36011=CARTESIAN_POINT('Ctrl Pts',(-0.582802053840284,-4.39729181288394,
22.6609493823405));
#36012=CARTESIAN_POINT('Ctrl Pts',(3.38057590440328,-2.87184871381299,22.8198413178244));
#36013=CARTESIAN_POINT('Ctrl Pts',(4.24521650715976,1.285939018969,22.9787332533082));
#36014=CARTESIAN_POINT('Ctrl Pts',(1.21871680907285,4.26508574569377,23.1376251887921));
#36015=CARTESIAN_POINT('Ctrl Pts',(-2.92505373203667,3.33465212858728,23.296517124276));
#36016=CARTESIAN_POINT('Ctrl Pts',(-4.38733815754819,-0.652117348083053,
23.4554090597599));
#36017=CARTESIAN_POINT('Ctrl Pts',(-1.82876059391868,-4.04164014539733,
23.6143009952437));
#36018=CARTESIAN_POINT('Ctrl Pts',(2.40731317054649,-3.72558744783597,23.7731929307276));
#36019=CARTESIAN_POINT('Ctrl Pts',(4.43445972060527,0.00359092823684341,
23.9320848662115));
#36020=CARTESIAN_POINT('Ctrl Pts',(2.4014416917595,3.73295270922791,24.0909768016953));
#36021=CARTESIAN_POINT('Ctrl Pts',(-1.84187514744654,4.03377454464145,24.2498687371792));
#36022=CARTESIAN_POINT('Ctrl Pts',(-3.53121097966664,1.77942692174697,24.3557966941685));
#36023=CARTESIAN_POINT('Ctrl Pts',(-3.71226170138833,0.544051223706471,
24.4087606726631));
#36024=CARTESIAN_POINT('Ctrl Pts',(2.06798052000209,-2.90001952809568,-0.109744663668461));
#36025=CARTESIAN_POINT('Ctrl Pts',(3.0330562439233,-2.2118318183024,-0.0567806851738377));
#36026=CARTESIAN_POINT('Ctrl Pts',(4.20535745823963,0.191894718237391,0.0491472718154096));
#36027=CARTESIAN_POINT('Ctrl Pts',(2.1127408095543,3.64588036952885,0.20803920729928));
#36028=CARTESIAN_POINT('Ctrl Pts',(-1.91829660558064,3.74733746988985,0.366931142783152));
#36029=CARTESIAN_POINT('Ctrl Pts',(-4.19002106768543,0.419258972444119,
0.525823078267022));
#36030=CARTESIAN_POINT('Ctrl Pts',(-2.62161565760238,-3.29588329210025,
0.684715013750895));
#36031=CARTESIAN_POINT('Ctrl Pts',(1.35007080858346,-3.98852267764505,0.843606949234764));
#36032=CARTESIAN_POINT('Ctrl Pts',(4.08412137222898,-1.02597522411638,1.00249888471864));
#36033=CARTESIAN_POINT('Ctrl Pts',(3.07467508021171,2.87739305660463,1.16139082020251));
#36034=CARTESIAN_POINT('Ctrl Pts',(-0.753105157375175,4.14309028633234,
1.32028275568638));
#36035=CARTESIAN_POINT('Ctrl Pts',(-3.89055727921005,1.61127416982435,1.47917469117025));
#36036=CARTESIAN_POINT('Ctrl Pts',(-3.46187378548392,-2.39751806138059,
1.63806662665412));
#36037=CARTESIAN_POINT('Ctrl Pts',(0.14002328039052,-4.20867770156907,1.79695856213799));
#36038=CARTESIAN_POINT('Ctrl Pts',(3.61356992084825,-2.16211260763564,1.95585049762186));
#36039=CARTESIAN_POINT('Ctrl Pts',(3.77486292837046,1.86628713503355,2.11474243310573));
#36040=CARTESIAN_POINT('Ctrl Pts',(0.476056292737952,4.18401440521967,2.27363436858961));
#36041=CARTESIAN_POINT('Ctrl Pts',(-3.2591106302341,2.66661036613276,2.43252630407347));
#36042=CARTESIAN_POINT('Ctrl Pts',(-4.0069256010488,-1.2950519324793,2.59141823955734));
#36043=CARTESIAN_POINT('Ctrl Pts',(-1.08192930174121,-4.0696486060465,2.75031017504122));
#36044=CARTESIAN_POINT('Ctrl Pts',(2.83478038785305,-3.11394154898843,2.90920211052509));
#36045=CARTESIAN_POINT('Ctrl Pts',(4.15308572767863,0.696053577028067,3.06809404600896));
#36046=CARTESIAN_POINT('Ctrl Pts',(1.66460721884761,3.8680349362124,3.22698598149283));
#36047=CARTESIAN_POINT('Ctrl Pts',(-2.34967649317396,3.49451455708637,3.3858779169767));
#36048=CARTESIAN_POINT('Ctrl Pts',(-4.21020970411577,-0.0821329642322605,
3.54476985246057));
#36049=CARTESIAN_POINT('Ctrl Pts',(-2.21159834323779,-3.58349610344751,
3.70366178794445));
#36050=CARTESIAN_POINT('Ctrl Pts',(1.81419891355671,-3.80017024344135,3.86255372342831));
#36051=CARTESIAN_POINT('Ctrl Pts',(4.1770728542812,-0.53354844253673,4.02144565891219));
#36052=CARTESIAN_POINT('Ctrl Pts',(2.71117598399594,3.22213226793253,4.18033759439605));
#36053=CARTESIAN_POINT('Ctrl Pts',(-1.23982752232801,4.02435576039341,4.33922952987993));
#36054=CARTESIAN_POINT('Ctrl Pts',(-4.05438558157035,1.13779133682627,4.4981214653638));
#36055=CARTESIAN_POINT('Ctrl Pts',(-3.15262991786046,-2.79169055788951,
4.65701340084767));
#36056=CARTESIAN_POINT('Ctrl Pts',(0.638876015320037,-4.16226488915267,
4.81590533633154));
#36057=CARTESIAN_POINT('Ctrl Pts',(3.84477812391437,-1.7176416238867,4.97479727181542));
#36058=CARTESIAN_POINT('Ctrl Pts',(3.5264960087876,2.30139902455706,5.13368920729927));
#36059=CARTESIAN_POINT('Ctrl Pts',(-0.0242279270633424,4.21094105608648,
5.29258114278316));
#36060=CARTESIAN_POINT('Ctrl Pts',(-3.55274416312754,2.26066814937938,5.45147307826701));
#36061=CARTESIAN_POINT('Ctrl Pts',(-3.82475910651287,-1.76176881213256,
5.61036501375091));
#36062=CARTESIAN_POINT('Ctrl Pts',(-0.590939573042961,-4.16934071422273,
5.76925694923476));
#36063=CARTESIAN_POINT('Ctrl Pts',(3.18454448653674,-2.75522920707652,5.92814888471864));
#36064=CARTESIAN_POINT('Ctrl Pts',(4.04102487998468,1.1843688148564,6.0870408202025));
#36065=CARTESIAN_POINT('Ctrl Pts',(1.19343818017234,4.03835571493739,6.24593275568638));
#36066=CARTESIAN_POINT('Ctrl Pts',(-2.74807276467801,3.19072212050733,6.40482469117025));
#36067=CARTESIAN_POINT('Ctrl Pts',(-4.17065690263191,-0.581577656713809,
6.56371662665412));
#36068=CARTESIAN_POINT('Ctrl Pts',(-1.77035119231138,-3.82079418788054,
6.72260856213799));
#36069=CARTESIAN_POINT('Ctrl Pts',(2.25268632236759,-3.5578105490987,6.88150049762186));
#36070=CARTESIAN_POINT('Ctrl Pts',(4.21087605067235,-0.033681688409442,
7.04039243310573));
#36071=CARTESIAN_POINT('Ctrl Pts',(2.30931042573792,3.52132033871361,7.19928436858961));
#36072=CARTESIAN_POINT('Ctrl Pts',(-1.70900553113983,3.84862464586941,7.35817630407347));
#36073=CARTESIAN_POINT('Ctrl Pts',(-4.16082008352265,0.648218946664257,
7.51706823955734));
#36074=CARTESIAN_POINT('Ctrl Pts',(-2.79876137105901,-3.14635445525897,
7.67596017504123));
#36075=CARTESIAN_POINT('Ctrl Pts',(1.12868612378383,-4.05692977561084,7.83485211052507));
#36076=CARTESIAN_POINT('Ctrl Pts',(4.02156212899428,-1.24885932470353,7.99374404600897));
#36077=CARTESIAN_POINT('Ctrl Pts',(3.2282109052434,2.70393526577978,8.15263598149282));
#36078=CARTESIAN_POINT('Ctrl Pts',(-0.524169312226923,4.1782601764825,8.3115279169767));
#36079=CARTESIAN_POINT('Ctrl Pts',(-3.79608767697933,1.82272595826847,8.47041985246058));
#36080=CARTESIAN_POINT('Ctrl Pts',(-3.5884522490603,-2.20354760022878,8.62931178794444));
#36081=CARTESIAN_POINT('Ctrl Pts',(-0.0915849341228856,-4.21001469951135,
8.78820372342831));
#36082=CARTESIAN_POINT('Ctrl Pts',(3.48923057484898,-2.35751597360421,8.94709565891219));
#36083=CARTESIAN_POINT('Ctrl Pts',(3.87176234716024,1.65591904916041,9.10598759439605));
#36084=CARTESIAN_POINT('Ctrl Pts',(0.705375731447328,4.15151257347791,9.26487952987993));
#36085=CARTESIAN_POINT('Ctrl Pts',(-3.10756939673095,2.84176424334623,9.42377146536379));
#36086=CARTESIAN_POINT('Ctrl Pts',(-4.07206743925366,-1.07278997964659,
9.58266340084768));
#36087=CARTESIAN_POINT('Ctrl Pts',(-1.30404428944617,-4.00400799967019,
9.74155533633153));
#36088=CARTESIAN_POINT('Ctrl Pts',(2.65928640835889,-3.26508918233143,9.90044727181542));
#36089=CARTESIAN_POINT('Ctrl Pts',(4.18507327278026,0.466661838722957,10.0593392072993));
#36090=CARTESIAN_POINT('Ctrl Pts',(1.87475601684109,3.77066326361532,10.2182311427832));
#36091=CARTESIAN_POINT('Ctrl Pts',(-2.15399215108477,3.61841531382528,10.377123078267));
#36092=CARTESIAN_POINT('Ctrl Pts',(-4.20835716549627,0.149470859622617,
10.5360150137509));
#36093=CARTESIAN_POINT('Ctrl Pts',(-2.40527567651967,-3.45648094023428,
10.6949069492348));
#36094=CARTESIAN_POINT('Ctrl Pts',(1.60251940571986,-3.89416783466651,10.8537988847186));
#36095=CARTESIAN_POINT('Ctrl Pts',(4.14141994429093,-0.762399118106369,
11.0126908202025));
#36096=CARTESIAN_POINT('Ctrl Pts',(2.88422969138973,3.06819664584361,11.1715827556864));
#36097=CARTESIAN_POINT('Ctrl Pts',(-1.01669095332279,4.08643500813259,11.3304746911703));
#36098=CARTESIAN_POINT('Ctrl Pts',(-3.98569664673889,1.35898263801798,11.4893666266541));
#36099=CARTESIAN_POINT('Ctrl Pts',(-3.30134997748419,-2.61413463624678,
11.648258562138));
#36100=CARTESIAN_POINT('Ctrl Pts',(0.409066111808665,-4.19109490305693,
11.8071504976218));
#36101=CARTESIAN_POINT('Ctrl Pts',(3.74452575596225,-1.92643152829146,11.9660424331058));
#36102=CARTESIAN_POINT('Ctrl Pts',(3.6476940768864,2.10402934668408,12.1249343685896));
#36103=CARTESIAN_POINT('Ctrl Pts',(0.207328517730425,4.20590376209391,12.2838263040735));
#36104=CARTESIAN_POINT('Ctrl Pts',(-3.42307762836267,2.45258050234096,12.4427182395573));
#36105=CARTESIAN_POINT('Ctrl Pts',(-3.91583687114297,-1.54881669956688,
12.6016101750412));
#36106=CARTESIAN_POINT('Ctrl Pts',(-0.819278322583353,-4.13054410464348,
12.7605021105251));
#36107=CARTESIAN_POINT('Ctrl Pts',(3.02824364863007,-2.92614968427652,12.919394046009));
#36108=CARTESIAN_POINT('Ctrl Pts',(4.10002976510464,0.960399654058624,13.0782859814928));
#36109=CARTESIAN_POINT('Ctrl Pts',(1.4136639806759,3.9666315331777,13.2371779169767));
#36110=CARTESIAN_POINT('Ctrl Pts',(-2.56848848838443,3.33698643319039,13.3960698524606));
#36111=CARTESIAN_POINT('Ctrl Pts',(-4.19632392852339,-0.351393023781037,
13.5549617879445));
#36112=CARTESIAN_POINT('Ctrl Pts',(-1.97774271993255,-3.71768009705162,
13.7138537234283));
#36113=CARTESIAN_POINT('Ctrl Pts',(2.05366863581272,-3.67628300114927,13.8727456589122));
#36114=CARTESIAN_POINT('Ctrl Pts',(4.20265495328316,-0.265146966613851,
14.0316375943961));
#36115=CARTESIAN_POINT('Ctrl Pts',(2.49942150494934,3.38902695634851,14.1905295298799));
#36116=CARTESIAN_POINT('Ctrl Pts',(-1.49482108676428,3.93676535861929,14.3494214653638));
#36117=CARTESIAN_POINT('Ctrl Pts',(-4.11888711133529,0.876002588087538,
14.5083134008477));
#36118=CARTESIAN_POINT('Ctrl Pts',(-2.96751629424819,-2.98771796085767,
14.6672053363315));
#36119=CARTESIAN_POINT('Ctrl Pts',(0.903926727462482,-4.11284913917822,
14.8260972718154));
#36120=CARTESIAN_POINT('Ctrl Pts',(3.94681626451235,-1.46807797628081,14.9849892072993));
#36121=CARTESIAN_POINT('Ctrl Pts',(3.37199181001155,2.52235659720725,15.1438811427832));
#36122=CARTESIAN_POINT('Ctrl Pts',(-0.293653481567197,4.20075936028517,
15.302773078267));
#36123=CARTESIAN_POINT('Ctrl Pts',(-3.69013136383804,2.02867988797614,15.4616650137509));
#36124=CARTESIAN_POINT('Ctrl Pts',(-3.7041766799792,-2.00291954250747,15.6205569492348));
#36125=CARTESIAN_POINT('Ctrl Pts',(-0.322915271855557,-4.19861135346705,
15.7794488847186));
#36126=CARTESIAN_POINT('Ctrl Pts',(3.35433536373254,-2.54578982594268,15.9383408202025));
#36127=CARTESIAN_POINT('Ctrl Pts',(3.95694933917511,1.44054277876839,16.0972327556863));
#36128=CARTESIAN_POINT('Ctrl Pts',(0.932561187129547,4.10645116889506,16.2561246911703));
#36129=CARTESIAN_POINT('Ctrl Pts',(-2.94662724659887,3.00832169820004,16.4150166266541));
#36130=CARTESIAN_POINT('Ctrl Pts',(-4.12489070599933,-0.847282853491266,
16.573908562138));
#36131=CARTESIAN_POINT('Ctrl Pts',(-1.52221433425345,-3.92625458813528,
16.7328004976219));
#36132=CARTESIAN_POINT('Ctrl Pts',(2.47574768701282,-3.40635948785661,16.8916924331057));
#36133=CARTESIAN_POINT('Ctrl Pts',(4.20440035952933,0.235858404662022,17.0505843685896));
#36134=CARTESIAN_POINT('Ctrl Pts',(2.07923339936798,3.66188476623891,17.2094763040735));
#36135=CARTESIAN_POINT('Ctrl Pts',(-1.95179166425446,3.73136983822386,17.3683682395573));
#36136=CARTESIAN_POINT('Ctrl Pts',(-4.19377372735666,0.380622508521273,
17.5272601750413));
#36137=CARTESIAN_POINT('Ctrl Pts',(-2.59167669631074,-3.31900941126415,
17.6861521105251));
#36138=CARTESIAN_POINT('Ctrl Pts',(1.38599204049781,-3.97638499568851,17.845044046009));
#36139=CARTESIAN_POINT('Ctrl Pts',(4.09323862916349,-0.988943423550422,
18.0039359814928));
#36140=CARTESIAN_POINT('Ctrl Pts',(3.04855817916078,2.90497927678192,18.1628279169767));
#36141=CARTESIAN_POINT('Ctrl Pts',(-0.79047874443103,4.13615218831009,18.3217198524606));
#36142=CARTESIAN_POINT('Ctrl Pts',(-3.9049503925967,1.57606281652034,18.4806117879444));
#36143=CARTESIAN_POINT('Ctrl Pts',(-3.44008296723408,-2.42867057231101,
18.6395037234283));
#36144=CARTESIAN_POINT('Ctrl Pts',(0.178018723063364,-4.20724623768266,
18.7983956589122));
#36145=CARTESIAN_POINT('Ctrl Pts',(3.63294564614808,-2.12939369361065,18.9572875943961));
#36146=CARTESIAN_POINT('Ctrl Pts',(3.75785733321325,1.90029467017615,19.1161795298799));
#36147=CARTESIAN_POINT('Ctrl Pts',(0.438257763221198,4.18814298982299,19.2750714653638));
#36148=CARTESIAN_POINT('Ctrl Pts',(-3.2830557796519,2.63707343810004,19.4339634008477));
#36149=CARTESIAN_POINT('Ctrl Pts',(-3.99506865257438,-1.33117918840468,
19.5928553363316));
#36150=CARTESIAN_POINT('Ctrl Pts',(-1.04513863451291,-4.07925199082465,
19.7517472718154));
#36151=CARTESIAN_POINT('Ctrl Pts',(2.86278192766154,-3.08821812779751,19.9106392072993));
#36152=CARTESIAN_POINT('Ctrl Pts',(4.14663145649351,0.733525142958367,20.0695311427831));
#36153=CARTESIAN_POINT('Ctrl Pts',(1.62961323923206,3.88290770670228,20.228423078267));
#36154=CARTESIAN_POINT('Ctrl Pts',(-2.3811341557403,3.47315587080009,20.3873150137509));
#36155=CARTESIAN_POINT('Ctrl Pts',(-4.20929645733797,-0.120145375813829,
20.5462069492348));
#36156=CARTESIAN_POINT('Ctrl Pts',(-2.17915128305114,-3.60331947526336,
20.7050988847187));
#36157=CARTESIAN_POINT('Ctrl Pts',(1.8484382962994,-3.78363415795159,20.8639908202025));
#36158=CARTESIAN_POINT('Ctrl Pts',(4.18172021126871,-0.495810131935346,
21.0228827556864));
#36159=CARTESIAN_POINT('Ctrl Pts',(2.6819714554658,3.24648126020556,21.1817746911702));
#36160=CARTESIAN_POINT('Ctrl Pts',(-1.27611456830103,4.01299679193883,21.3406666266541));
#36161=CARTESIAN_POINT('Ctrl Pts',(-4.0644939375549,1.10113616299357,21.499558562138));
#36162=CARTESIAN_POINT('Ctrl Pts',(-3.12729397009587,-2.82004312294412,
21.6584504976218));
#36163=CARTESIAN_POINT('Ctrl Pts',(0.676432679244829,-4.15632663665986,
21.8173424331058));
#36164=CARTESIAN_POINT('Ctrl Pts',(3.86013096777133,-1.68285526903662,21.9762343685896));
#36165=CARTESIAN_POINT('Ctrl Pts',(3.50557143079345,2.33314703363201,22.1351263040735));
#36166=CARTESIAN_POINT('Ctrl Pts',(-0.062248327739398,4.21055138242857,
22.2940182395573));
#36167=CARTESIAN_POINT('Ctrl Pts',(-3.57301372792039,2.22849532219585,22.4529101750413));
#36168=CARTESIAN_POINT('Ctrl Pts',(-3.80869186337486,-1.79622960798394,
22.6118021105251));
#36169=CARTESIAN_POINT('Ctrl Pts',(-0.553275556609776,-4.17451184208706,
22.770694046009));
#36170=CARTESIAN_POINT('Ctrl Pts',(3.20930580605478,-2.72635225830787,22.9295859814928));
#36171=CARTESIAN_POINT('Ctrl Pts',(4.03014112673573,1.22078949756286,23.0884779169767));
#36172=CARTESIAN_POINT('Ctrl Pts',(1.15697296611493,4.04900373014777,23.2473698524606));
#36173=CARTESIAN_POINT('Ctrl Pts',(-2.77686175098751,3.16570866623898,23.4062617879444));
#36174=CARTESIAN_POINT('Ctrl Pts',(-4.16506246873653,-0.619079130483647,
23.5651537234284));
#36175=CARTESIAN_POINT('Ctrl Pts',(-1.73611010606296,-3.83687855306338,
23.7240456589121));
#36176=CARTESIAN_POINT('Ctrl Pts',(2.28535147670074,-3.53683803157065,23.8829375943961));
#36177=CARTESIAN_POINT('Ctrl Pts',(4.20979671230505,0.00340900105942339,
24.0418295298799));
#36178=CARTESIAN_POINT('Ctrl Pts',(2.27977746461109,3.54383014676541,24.2007214653638));
#36179=CARTESIAN_POINT('Ctrl Pts',(-1.74856023703795,3.82941144719509,24.3596134008477));
#36180=CARTESIAN_POINT('Ctrl Pts',(-3.35230925733317,1.68927582545165,24.4655413578369));
#36181=CARTESIAN_POINT('Ctrl Pts',(-3.52418740734158,0.51648795956872,24.5185053363315));
#36182=CARTESIAN_POINT('Ctrl Pts',(1.95761919937776,-2.74525502143746,0.));
#36183=CARTESIAN_POINT('Ctrl Pts',(2.87119200517945,-2.09379362688536,0.0529639784946237));
#36184=CARTESIAN_POINT('Ctrl Pts',(3.98093135833217,0.181653928094203,0.158891935483871));
#36185=CARTESIAN_POINT('Ctrl Pts',(1.99999077945293,3.45131172222888,0.317783870967742));
#36186=CARTESIAN_POINT('Ctrl Pts',(-1.81592342329319,3.54735439074478,0.476675806451613));
#36187=CARTESIAN_POINT('Ctrl Pts',(-3.96641342051426,0.396884499650513,
0.635567741935484));
#36188=CARTESIAN_POINT('Ctrl Pts',(-2.48170865009243,-3.119992837997,0.794459677419355));
#36189=CARTESIAN_POINT('Ctrl Pts',(1.27802196869812,-3.77566833700333,0.953351612903227));
#36190=CARTESIAN_POINT('Ctrl Pts',(3.86616524359544,-0.97122229991515,1.1122435483871));
#36191=CARTESIAN_POINT('Ctrl Pts',(2.91058978102209,2.72383605033175,1.27113548387097));
#36192=CARTESIAN_POINT('Ctrl Pts',(-0.71291441141164,3.92198718064885,1.43002741935484));
#36193=CARTESIAN_POINT('Ctrl Pts',(-3.6829310297627,1.52528576541256,1.58891935483871));
#36194=CARTESIAN_POINT('Ctrl Pts',(-3.27712496454226,-2.26957040572551,
1.74781129032258));
#36195=CARTESIAN_POINT('Ctrl Pts',(0.13255069832671,-3.98407441119242,1.90670322580645));
#36196=CARTESIAN_POINT('Ctrl Pts',(3.42072557595435,-2.04672776701011,2.06559516129032));
#36197=CARTESIAN_POINT('Ctrl Pts',(3.57341090601276,1.76668952717683,2.2244870967742));
#36198=CARTESIAN_POINT('Ctrl Pts',(0.45065073371557,3.96072731387378,2.38337903225806));
#36199=CARTESIAN_POINT('Ctrl Pts',(-3.08518261218244,2.52430213897566,2.54227096774194));
#36200=CARTESIAN_POINT('Ctrl Pts',(-3.79308915689569,-1.22593926910403,
2.70116290322581));
#36201=CARTESIAN_POINT('Ctrl Pts',(-1.02419029239979,-3.85246484135621,
2.86005483870968));
#36202=CARTESIAN_POINT('Ctrl Pts',(2.68349747959669,-2.94776072747231,3.01894677419354));
#36203=CARTESIAN_POINT('Ctrl Pts',(3.9314491981565,0.658907486316316,3.17783870967743));
#36204=CARTESIAN_POINT('Ctrl Pts',(1.57577260497388,3.66161063015511,3.33673064516129));
#36205=CARTESIAN_POINT('Ctrl Pts',(-2.22428198470617,3.30802380549044,3.49562258064516));
#36206=CARTESIAN_POINT('Ctrl Pts',(-3.98552465580058,-0.07774979799263,
3.65451451612903));
#36207=CARTESIAN_POINT('Ctrl Pts',(-2.09357261161725,-3.39225669930255,
3.8134064516129));
#36208=CARTESIAN_POINT('Ctrl Pts',(1.71738108280889,-3.59736765289132,3.97229838709678));
#36209=CARTESIAN_POINT('Ctrl Pts',(3.95415621068438,-0.505074716519562,
4.13119032258065));
#36210=CARTESIAN_POINT('Ctrl Pts',(2.56648943634972,3.05017766348832,4.29008225806451));
#36211=CARTESIAN_POINT('Ctrl Pts',(-1.17366200413909,3.8095891259482,4.44897419354839));
#36212=CARTESIAN_POINT('Ctrl Pts',(-3.83801635431,1.07707115435234,4.60786612903225));
#36213=CARTESIAN_POINT('Ctrl Pts',(-2.98438442530889,-2.6427072121746,4.76675806451613));
#36214=CARTESIAN_POINT('Ctrl Pts',(0.604781303071069,-3.94013849796468,
4.92565));
#36215=CARTESIAN_POINT('Ctrl Pts',(3.63959495745868,-1.6259767381985,5.08454193548388));
#36216=CARTESIAN_POINT('Ctrl Pts',(3.3382985122726,2.17858092584818,5.24343387096774));
#36217=CARTESIAN_POINT('Ctrl Pts',(-0.0229349622598251,3.98621697792136,
5.40232580645161));
#36218=CARTESIAN_POINT('Ctrl Pts',(-3.36314588892197,2.14002372355154,5.56121774193549));
#36219=CARTESIAN_POINT('Ctrl Pts',(-3.62064428919136,-1.6677490035023,5.72010967741935));
#36220=CARTESIAN_POINT('Ctrl Pts',(-0.559403071098495,-3.94683670951677,
5.87900161290323));
#36221=CARTESIAN_POINT('Ctrl Pts',(3.01459581839321,-2.60819168376593,6.03789354838709));
#36222=CARTESIAN_POINT('Ctrl Pts',(3.82536866943663,1.12116294553142,6.19678548387097));
#36223=CARTESIAN_POINT('Ctrl Pts',(1.12974830864147,3.82284194895142,6.35567741935484));
#36224=CARTESIAN_POINT('Ctrl Pts',(-2.60141715716711,3.02044377235149,6.51456935483871));
#36225=CARTESIAN_POINT('Ctrl Pts',(-3.94808265727831,-0.550540769460877,
6.67346129032257));
#36226=CARTESIAN_POINT('Ctrl Pts',(-1.67587337027072,-3.61689096522939,
6.83235322580646));
#36227=CARTESIAN_POINT('Ctrl Pts',(2.13246786040229,-3.36794189853266,6.99124516129032));
#36228=CARTESIAN_POINT('Ctrl Pts',(3.98615544163244,-0.0318842074478251,
7.15013709677419));
#36229=CARTESIAN_POINT('Ctrl Pts',(2.18607012156152,3.33339905069232,7.30902903225807));
#36230=CARTESIAN_POINT('Ctrl Pts',(-1.61780152532516,3.64323620318475,7.46792096774193));
#36231=CARTESIAN_POINT('Ctrl Pts',(-3.93877079686046,0.613625632889965,
7.62681290322582));
#36232=CARTESIAN_POINT('Ctrl Pts',(-2.64940067929482,-2.97844386351206,
7.78570483870967));
#36233=CARTESIAN_POINT('Ctrl Pts',(1.06845185659111,-3.84042477308012,7.94459677419355));
#36234=CARTESIAN_POINT('Ctrl Pts',(3.80694458147109,-1.18221180891932,8.10348870967742));
#36235=CARTESIAN_POINT('Ctrl Pts',(3.0559319039131,2.55963513145653,8.2623806451613));
#36236=CARTESIAN_POINT('Ctrl Pts',(-0.49619611955484,3.95528016940384,8.42127258064515));
#36237=CARTESIAN_POINT('Ctrl Pts',(-3.59350295957747,1.72545306718219,8.58016451612905));
#36238=CARTESIAN_POINT('Ctrl Pts',(-3.39694835172031,-2.08595151029096,
8.7390564516129));
#36239=CARTESIAN_POINT('Ctrl Pts',(-0.086697347329244,-3.9853400579507,
8.89794838709678));
#36240=CARTESIAN_POINT('Ctrl Pts',(3.30302181201077,-2.23170309784288,9.05684032258065));
#36241=CARTESIAN_POINT('Ctrl Pts',(3.66513912143678,1.56754809433529,9.21573225806451));
#36242=CARTESIAN_POINT('Ctrl Pts',(0.667732148006428,3.92995999802278,9.3746241935484));
#36243=CARTESIAN_POINT('Ctrl Pts',(-2.94172863602851,2.69010862968584,9.53351612903225));
#36244=CARTESIAN_POINT('Ctrl Pts',(-3.85475458938848,-1.01553870587432,
9.69240806451614));
#36245=CARTESIAN_POINT('Ctrl Pts',(-1.23445173354738,-3.79032725830928,
9.85129999999999));
#36246=CARTESIAN_POINT('Ctrl Pts',(2.51736903674626,-3.09084210861242,10.0101919354839));
#36247=CARTESIAN_POINT('Ctrl Pts',(3.96172967315432,0.441757630821415,10.1690838709677));
#36248=CARTESIAN_POINT('Ctrl Pts',(1.77470645260886,3.56943536355667,10.3279758064516));
#36249=CARTESIAN_POINT('Ctrl Pts',(-2.03904067252446,3.42531238624034,10.4868677419355));
#36250=CARTESIAN_POINT('Ctrl Pts',(-3.98377098107586,0.14149409131981,10.6457596774194));
#36251=CARTESIAN_POINT('Ctrl Pts',(-2.27691402245245,-3.27201991771136,
10.8046516129032));
#36252=CARTESIAN_POINT('Ctrl Pts',(1.51699821428175,-3.68634890174633,10.9635435483871));
#36253=CARTESIAN_POINT('Ctrl Pts',(3.92040597926993,-0.721712384018116,
11.122435483871));
#36254=CARTESIAN_POINT('Ctrl Pts',(2.73030783639792,2.90445707939446,11.2813274193548));
#36255=CARTESIAN_POINT('Ctrl Pts',(-0.962433500126168,3.86835540835836,
11.4402193548387));
#36256=CARTESIAN_POINT('Ctrl Pts',(-3.77299312207436,1.28645820309873,11.5991112903226));
#36257=CARTESIAN_POINT('Ctrl Pts',(-3.12516778435703,-2.4746268662482,11.7580032258064));
#36258=CARTESIAN_POINT('Ctrl Pts',(0.38723559847199,-3.96742994882286,11.9168951612903));
#36259=CARTESIAN_POINT('Ctrl Pts',(3.54469272874429,-1.82362421192741,12.0757870967742));
#36260=CARTESIAN_POINT('Ctrl Pts',(3.45302863798842,1.9917442187119,12.2346790322581));
#36261=CARTESIAN_POINT('Ctrl Pts',(0.196264076456207,3.98144850774605,12.3935709677419));
#36262=CARTESIAN_POINT('Ctrl Pts',(-3.24039923076088,2.32169434526269,12.5524629032258));
#36263=CARTESIAN_POINT('Ctrl Pts',(-3.70686153299603,-1.46616144497625,
12.7113548387097));
#36264=CARTESIAN_POINT('Ctrl Pts',(-0.775556132376715,-3.9101105474236,
12.8702467741936));
#36265=CARTESIAN_POINT('Ctrl Pts',(2.86663624227273,-2.76999069710151,13.0291387096774));
#36266=CARTESIAN_POINT('Ctrl Pts',(3.88122465785174,0.909146282412278,13.1880306451613));
#36267=CARTESIAN_POINT('Ctrl Pts',(1.33822138229676,3.75494545093591,13.3469225806451));
#36268=CARTESIAN_POINT('Ctrl Pts',(-2.43141670320813,3.15890243959844,13.5058145161291));
#36269=CARTESIAN_POINT('Ctrl Pts',(-3.97237991839373,-0.332640333517474,
13.6647064516129));
#36270=CARTESIAN_POINT('Ctrl Pts',(-1.87219709398698,-3.51927973437849,
13.8235983870968));
#36271=CARTESIAN_POINT('Ctrl Pts',(1.94407109338865,-3.48009186536664,13.9824903225806));
#36272=CARTESIAN_POINT('Ctrl Pts',(3.97837307717912,-0.25099694483561,14.1413822580645));
#36273=CARTESIAN_POINT('Ctrl Pts',(2.36603559757979,3.20816573115008,14.3002741935484));
#36274=CARTESIAN_POINT('Ctrl Pts',(-1.41504740048591,3.7266731359107,14.4591661290323));
#36275=CARTESIAN_POINT('Ctrl Pts',(-3.8990756495189,0.82925321034604,14.6180580645161));
#36276=CARTESIAN_POINT('Ctrl Pts',(-2.80914970711657,-2.8282732772042,14.77695));
#36277=CARTESIAN_POINT('Ctrl Pts',(0.8556871302199,-3.8933599040824,14.9358419354839));
#36278=CARTESIAN_POINT('Ctrl Pts',(3.73618765800463,-1.38973148187494,15.0947338709677));
#36279=CARTESIAN_POINT('Ctrl Pts',(3.19203969455987,2.38774671937678,15.2536258064516));
#36280=CARTESIAN_POINT('Ctrl Pts',(-0.277982160818163,3.97657864574653,
15.4125177419355));
#36281=CARTESIAN_POINT('Ctrl Pts',(-3.4932011864735,1.92041591285862,15.5714096774194));
#36282=CARTESIAN_POINT('Ctrl Pts',(-3.50649695027464,-1.89603031232498,
15.7303016129032));
#36283=CARTESIAN_POINT('Ctrl Pts',(-0.30568234557457,-3.97454527098943,
15.8891935483871));
#36284=CARTESIAN_POINT('Ctrl Pts',(3.17532551476257,-2.40992939374543,16.048085483871));
#36285=CARTESIAN_POINT('Ctrl Pts',(3.74577996379122,1.36366574731522,16.2069774193548));
#36286=CARTESIAN_POINT('Ctrl Pts',(0.882793462927545,3.88730337243608,16.3658693548387));
#36287=CARTESIAN_POINT('Ctrl Pts',(-2.78937543925498,2.84777746083178,16.5247612903226));
#36288=CARTESIAN_POINT('Ctrl Pts',(-3.90475885207616,-0.802066153551767,
16.6836532258065));
#36289=CARTESIAN_POINT('Ctrl Pts',(-1.44097876042837,-3.71672329068694,
16.8425451612903));
#36290=CARTESIAN_POINT('Ctrl Pts',(2.34362517346463,-3.22457328244272,17.0014370967742));
#36291=CARTESIAN_POINT('Ctrl Pts',(3.980025336833,0.223271417131382,17.1603290322581));
#36292=CARTESIAN_POINT('Ctrl Pts',(1.96827154957251,3.46646201691059,17.3192209677419));
#36293=CARTESIAN_POINT('Ctrl Pts',(-1.84763096082072,3.53223889907763,17.4781129032258));
#36294=CARTESIAN_POINT('Ctrl Pts',(-3.96996581307795,0.360309936766638,
17.6370048387097));
#36295=CARTESIAN_POINT('Ctrl Pts',(-2.4533674327226,-3.14188479222213,17.7958967741935));
#36296=CARTESIAN_POINT('Ctrl Pts',(1.31202620257783,-3.7641784032229,17.9547887096774));
#36297=CARTESIAN_POINT('Ctrl Pts',(3.87479594250582,-0.936166764781103,
18.1136806451613));
#36298=CARTESIAN_POINT('Ctrl Pts',(2.88586665310525,2.74995008464444,18.2725725806452));
#36299=CARTESIAN_POINT('Ctrl Pts',(-0.748293493014444,3.91541934610488,
18.431464516129));
#36300=CARTESIAN_POINT('Ctrl Pts',(-3.69655603001392,1.49195352625591,18.5903564516129));
#36301=CARTESIAN_POINT('Ctrl Pts',(-3.25649705061201,-2.29906040958017,
18.7492483870968));
#36302=CARTESIAN_POINT('Ctrl Pts',(0.168518449156949,-3.98271933982683,
18.9081403225806));
#36303=CARTESIAN_POINT('Ctrl Pts',(3.43906728250426,-2.01575495384355,19.0670322580645));
#36304=CARTESIAN_POINT('Ctrl Pts',(3.55731284355299,1.79888219198906,19.2259241935484));
#36305=CARTESIAN_POINT('Ctrl Pts',(0.41486938743375,3.96463556949202,19.3848161290323));
#36306=CARTESIAN_POINT('Ctrl Pts',(-3.10784988770987,2.49634149967166,19.5437080645161));
#36307=CARTESIAN_POINT('Ctrl Pts',(-3.78186497477451,-1.26013853217073,
19.7026));
#36308=CARTESIAN_POINT('Ctrl Pts',(-0.989363022110038,-3.86155572506565,
19.8614919354839));
#36309=CARTESIAN_POINT('Ctrl Pts',(2.71000466929749,-2.92341008068914,20.0203838709678));
#36310=CARTESIAN_POINT('Ctrl Pts',(3.92533937020224,0.694379317983201,20.1792758064516));
#36311=CARTESIAN_POINT('Ctrl Pts',(1.54264613898669,3.6756896897871,20.3381677419355));
#36312=CARTESIAN_POINT('Ctrl Pts',(-2.25406085525731,3.28780496206174,20.4970596774194));
#36313=CARTESIAN_POINT('Ctrl Pts',(-3.98466014600046,-0.113733612156729,
20.6559516129032));
#36314=CARTESIAN_POINT('Ctrl Pts',(-2.06285714434356,-3.41102216294582,
20.8148435483871));
#36315=CARTESIAN_POINT('Ctrl Pts',(1.74979322227715,-3.58171404391184,20.9737354838709));
#36316=CARTESIAN_POINT('Ctrl Pts',(3.95855555351044,-0.46935037546761,21.1326274193549));
#36317=CARTESIAN_POINT('Ctrl Pts',(2.53884345747981,3.07322723010567,21.2915193548387));
#36318=CARTESIAN_POINT('Ctrl Pts',(-1.20801252978399,3.79883634829061,21.4504112903226));
#36319=CARTESIAN_POINT('Ctrl Pts',(-3.84758526057294,1.0423721466212,21.6093032258064));
#36320=CARTESIAN_POINT('Ctrl Pts',(-2.96040057376934,-2.66954669405833,
21.7681951612904));
#36321=CARTESIAN_POINT('Ctrl Pts',(0.640333691332285,-3.93451715048184,
21.9270870967742));
#36322=CARTESIAN_POINT('Ctrl Pts',(3.6541284705207,-1.59304681672573,22.0859790322581));
#36323=CARTESIAN_POINT('Ctrl Pts',(3.31849061020388,2.20863464806944,22.2448709677419));
#36324=CARTESIAN_POINT('Ctrl Pts',(-0.058926339166703,3.98584809986529,
22.4037629032258));
#36325=CARTESIAN_POINT('Ctrl Pts',(-3.3823337336902,2.1095678543673,22.5626548387097));
#36326=CARTESIAN_POINT('Ctrl Pts',(-3.60543450198892,-1.70037073998966,
22.7215467741936));
#36327=CARTESIAN_POINT('Ctrl Pts',(-0.52374905937927,-3.95173187129016,
22.8804387096774));
#36328=CARTESIAN_POINT('Ctrl Pts',(3.03803570770629,-2.58085580280275,23.0393306451613));
#36329=CARTESIAN_POINT('Ctrl Pts',(3.81506574631169,1.15563997615671,23.1982225806452));
#36330=CARTESIAN_POINT('Ctrl Pts',(1.095229123157,3.83292171460177,23.357114516129));
#36331=CARTESIAN_POINT('Ctrl Pts',(-2.62866976993836,2.99676520389069,23.5160064516129));
#36332=CARTESIAN_POINT('Ctrl Pts',(-3.94278677992486,-0.586040912884242,
23.6748983870968));
#36333=CARTESIAN_POINT('Ctrl Pts',(-1.64345961820725,-3.63211696072943,
23.8337903225806));
#36334=CARTESIAN_POINT('Ctrl Pts',(2.163389782855,-3.34808861530533,23.9926822580645));
#36335=CARTESIAN_POINT('Ctrl Pts',(3.98513370400483,0.0032270738820094,
24.1515741935484));
#36336=CARTESIAN_POINT('Ctrl Pts',(2.15811323746268,3.35470758430291,24.3104661290323));
#36337=CARTESIAN_POINT('Ctrl Pts',(-1.65524532662936,3.62504834974875,24.4693580645161));
#36338=CARTESIAN_POINT('Ctrl Pts',(-3.1734075349997,1.59912472915632,24.5752860215054));
#36339=CARTESIAN_POINT('Ctrl Pts',(-3.33611311329483,0.488924695430968,
24.62825));
#36340=CARTESIAN_POINT('',(1.95761919937778,-2.74525502143744,0.));
#36341=CARTESIAN_POINT('Ctrl Pts',(1.95761919937776,-2.74525502143746,0.));
#36342=CARTESIAN_POINT('Ctrl Pts',(2.87119200517945,-2.09379362688536,0.0529639784946237));
#36343=CARTESIAN_POINT('Ctrl Pts',(3.98093135833217,0.181653928094203,0.158891935483871));
#36344=CARTESIAN_POINT('Ctrl Pts',(1.99999077945293,3.45131172222888,0.317783870967742));
#36345=CARTESIAN_POINT('Ctrl Pts',(-1.81592342329319,3.54735439074478,0.476675806451613));
#36346=CARTESIAN_POINT('Ctrl Pts',(-3.32105516281529,1.34233496093003,0.58788455216069));
#36347=CARTESIAN_POINT('Ctrl Pts',(-3.3766520624322,0.1136195821916,0.646129319375144));
#36348=CARTESIAN_POINT('Ctrl Pts',(-3.37589447807987,0.0021436428109594,
0.651410108094974));
#36349=CARTESIAN_POINT('Ctrl Pts',(1.73118107496478,3.54876586530513,2.39391839684799E-16));
#36350=CARTESIAN_POINT('Ctrl Pts',(1.81301063452785,3.50205269354806,2.06920727311338E-16));
#36351=CARTESIAN_POINT('Ctrl Pts',(1.89292240658196,3.4522795469799,5.6760153975772E-16));
#36352=CARTESIAN_POINT('Ctrl Pts',(1.97072352421092,3.39943606703627,2.9316826744008E-16));
#36353=CARTESIAN_POINT('Ctrl Pts',(2.07158749034463,3.33092801556019,-4.87384004076243E-17));
#36354=CARTESIAN_POINT('Ctrl Pts',(2.16890551010069,3.25726040082769,-6.1331688516479E-17));
#36355=CARTESIAN_POINT('Ctrl Pts',(2.26249391432527,3.17884397520376,-1.04083408558608E-17));
#36356=CARTESIAN_POINT('Ctrl Pts',(2.31703211703773,3.13314717171513,1.92670006623856E-17));
#36357=CARTESIAN_POINT('Ctrl Pts',(2.37030307443948,3.08583698417059,-9.57318163015451E-16));
#36358=CARTESIAN_POINT('Ctrl Pts',(2.42226407127706,3.03698980450436,-1.02695629777827E-15));
#36359=CARTESIAN_POINT('Ctrl Pts',(2.45441149625484,3.00676884764696,-1.07004028094122E-15));
#36360=CARTESIAN_POINT('Ctrl Pts',(2.48605741280453,2.97595951290433,-8.19532942944583E-16));
#36361=CARTESIAN_POINT('Ctrl Pts',(2.51719072732778,2.9445793777147,-8.39606162372775E-16));
#36362=CARTESIAN_POINT('Ctrl Pts',(2.53181221876951,2.92984196908534,-8.49033375972473E-16));
#36363=CARTESIAN_POINT('Ctrl Pts',(2.54632072268487,2.91497845934833,-6.96615474306211E-16));
#36364=CARTESIAN_POINT('Ctrl Pts',(2.56070494112922,2.90000148244637,-7.07767178198537E-16));
#36365=CARTESIAN_POINT('Ctrl Pts',(2.64790074151672,2.80921243517189,-7.75367774667319E-16));
#36366=CARTESIAN_POINT('Ctrl Pts',(2.73062866917384,2.71416182380689,-8.593918943852E-16));
#36367=CARTESIAN_POINT('Ctrl Pts',(2.80868748257388,2.61529981528879,-7.7715611723761E-16));
#36368=CARTESIAN_POINT('Ctrl Pts',(2.87698894429891,2.52879555783546,-7.05199812233468E-16));
#36369=CARTESIAN_POINT('Ctrl Pts',(2.94171511816388,2.43937213712426,-7.20848724153807E-16));
#36370=CARTESIAN_POINT('Ctrl Pts',(3.00269897791456,2.3473133317077,-6.24500451351651E-16));
#36371=CARTESIAN_POINT('Ctrl Pts',(3.02937941655548,2.30703760433796,-5.82348082000707E-16));
#36372=CARTESIAN_POINT('Ctrl Pts',(3.05534314365639,2.26625728440317,-1.08606649764317E-16));
#36373=CARTESIAN_POINT('Ctrl Pts',(3.08057418911428,2.22499554197223,-6.93889390390723E-17));
#36374=CARTESIAN_POINT('Ctrl Pts',(3.09523937783659,2.20101273710704,-4.6594198725879E-17));
#36375=CARTESIAN_POINT('Ctrl Pts',(3.10965701779078,2.17686728558595,-1.5350788780052E-16));
#36376=CARTESIAN_POINT('Ctrl Pts',(3.12382377516257,2.1525637049523,-1.66533453693773E-16));
#36377=CARTESIAN_POINT('Ctrl Pts',(3.1333468514065,2.13622652592816,-1.75289406369904E-16));
#36378=CARTESIAN_POINT('Ctrl Pts',(3.14275743380374,2.11981622896702,-6.17919290773945E-16));
#36379=CARTESIAN_POINT('Ctrl Pts',(3.15204614385832,2.10334928089744,-6.10622663543836E-16));
#36380=CARTESIAN_POINT('Ctrl Pts',(3.21133027918083,1.99825085797653,-5.64052770246931E-16));
#36381=CARTESIAN_POINT('Ctrl Pts',(3.26572921710173,1.89071971149897,-2.93721959998899E-16));
#36382=CARTESIAN_POINT('Ctrl Pts',(3.3150665440347,1.78114320161924,-3.46944695195361E-16));
#36383=CARTESIAN_POINT('Ctrl Pts',(3.36416434269629,1.67209867580975,-3.99909038813826E-16));
#36384=CARTESIAN_POINT('Ctrl Pts',(3.40824985101865,1.5610277430108,-6.74639111044964E-16));
#36385=CARTESIAN_POINT('Ctrl Pts',(3.44710068203266,1.44829560050515,-7.21644966006352E-16));
#36386=CARTESIAN_POINT('Ctrl Pts',(3.48485757303191,1.33873770674576,-7.67327256340457E-16));
#36387=CARTESIAN_POINT('Ctrl Pts',(3.51767049623361,1.22761008128266,-7.45739296926402E-16));
#36388=CARTESIAN_POINT('Ctrl Pts',(3.54528704260767,1.11524410687019,-6.10622663543836E-16));
#36389=CARTESIAN_POINT('Ctrl Pts',(3.56429882714017,1.03788911593903,-5.17605662582399E-16));
#36390=CARTESIAN_POINT('Ctrl Pts',(3.58084694549942,0.959947166702576,1.01128139593754E-16));
#36391=CARTESIAN_POINT('Ctrl Pts',(3.59483483174014,0.881527990398642,1.38777878078145E-16));
#36392=CARTESIAN_POINT('Ctrl Pts',(3.60174616248926,0.842781545425996,1.5738038819335E-16));
#36393=CARTESIAN_POINT('Ctrl Pts',(3.60803228263339,0.803918629301433,-8.2431208915498E-16));
#36394=CARTESIAN_POINT('Ctrl Pts',(3.6136804381616,0.764952740225288,-8.60422844084496E-16));
#36395=CARTESIAN_POINT('Ctrl Pts',(3.61598402562173,0.749060590478247,-8.75150533826084E-16));
#36396=CARTESIAN_POINT('Ctrl Pts',(3.6181800809526,0.733160977259198,-9.56453568707426E-16));
#36397=CARTESIAN_POINT('Ctrl Pts',(3.62026800126996,0.71725566677106,-9.43689570931383E-16));
#36398=CARTESIAN_POINT('Ctrl Pts',(3.63517124652415,0.603726074153541,-8.52582172005361E-16));
#36399=CARTESIAN_POINT('Ctrl Pts',(3.64457137343043,0.489891978911761,1.54068630345449E-16));
#36400=CARTESIAN_POINT('Ctrl Pts',(3.64826597516095,0.3760806489335,1.38777878078145E-16));
#36401=CARTESIAN_POINT('Ctrl Pts',(3.65049038519446,0.307558225463841,1.29571770019922E-16));
#36402=CARTESIAN_POINT('Ctrl Pts',(3.65064564728474,0.239043959798587,2.28153843810054E-16));
#36403=CARTESIAN_POINT('Ctrl Pts',(3.64867842117138,0.170609648189261,1.38777878078145E-16));
#36404=CARTESIAN_POINT('Ctrl Pts',(3.64536397368567,0.0553092612588858,
-9.22057312926959E-18));
#36405=CARTESIAN_POINT('Ctrl Pts',(3.63602703897368,-0.0597651999246838,
-3.71059406415836E-16));
#36406=CARTESIAN_POINT('Ctrl Pts',(3.62088618085986,-0.174255990612961,
-4.44089209850063E-16));
#36407=CARTESIAN_POINT('Ctrl Pts',(3.60564019443288,-0.289541731204713,
-5.17626084943432E-16));
#36408=CARTESIAN_POINT('Ctrl Pts',(3.58450894234823,-0.404236478340693,
2.06881119674206E-16));
#36409=CARTESIAN_POINT('Ctrl Pts',(3.55766829556208,-0.517952337059044,
1.66533453693773E-16));
#36410=CARTESIAN_POINT('Ctrl Pts',(3.55209090522836,-0.541582085487224,
1.58149353116006E-16));
#36411=CARTESIAN_POINT('Ctrl Pts',(3.54626683911464,-0.565169464342046,
2.72822796152711E-16));
#36412=CARTESIAN_POINT('Ctrl Pts',(3.54019745029697,-0.588710821151176,
2.77555756156289E-16));
#36413=CARTESIAN_POINT('Ctrl Pts',(3.53607649256559,-0.604694792398417,
2.80769313353732E-16));
#36414=CARTESIAN_POINT('Ctrl Pts',(3.53184170988113,-0.62066020100356,-1.61867697048363E-17));
#36415=CARTESIAN_POINT('Ctrl Pts',(3.52749592285427,-0.636597072708719,
-2.77555756156289E-17));
#36416=CARTESIAN_POINT('Ctrl Pts',(3.49747618222011,-0.7466854760641,-1.07670341512578E-16));
#36417=CARTESIAN_POINT('Ctrl Pts',(3.46222700262188,-0.855189606000695,
-1.99543722780696E-16));
#36418=CARTESIAN_POINT('Ctrl Pts',(3.42199607778626,-0.961778490999782,
-2.77555756156289E-16));
#36419=CARTESIAN_POINT('Ctrl Pts',(3.38156991618782,-1.0688846414842,-3.55946374337476E-16));
#36420=CARTESIAN_POINT('Ctrl Pts',(3.33611303054141,-1.17405769074672,1.35240542225809E-16));
#36421=CARTESIAN_POINT('Ctrl Pts',(3.28582849960376,-1.27693996092432,1.11022302462516E-16));
#36422=CARTESIAN_POINT('Ctrl Pts',(3.23598893769955,-1.3789118233987,8.70183704900679E-17));
#36423=CARTESIAN_POINT('Ctrl Pts',(3.18140622212873,-1.47863395215989,2.26466381867324E-16));
#36424=CARTESIAN_POINT('Ctrl Pts',(3.1222390297712,-1.57572584500942,2.22044604925031E-16));
#36425=CARTESIAN_POINT('Ctrl Pts',(3.08604888850041,-1.6351129678129,2.19339985594059E-16));
#36426=CARTESIAN_POINT('Ctrl Pts',(3.04814284654775,-1.69351537716898,-1.98475779326559E-16));
#36427=CARTESIAN_POINT('Ctrl Pts',(3.00855126708734,-1.75083831899302,-2.22044604925031E-16));
#36428=CARTESIAN_POINT('Ctrl Pts',(2.9875142347103,-1.78129693164588,-2.34567928166019E-16));
#36429=CARTESIAN_POINT('Ctrl Pts',(2.96600124729196,-1.81145066683922,-9.64459754115302E-17));
#36430=CARTESIAN_POINT('Ctrl Pts',(2.94401641708542,-1.8412845286552,-1.11022302462516E-16));
#36431=CARTESIAN_POINT('Ctrl Pts',(2.93430327275808,-1.85446546309672,-1.17462287082754E-16));
#36432=CARTESIAN_POINT('Ctrl Pts',(2.92449763119146,-1.86758436264681,1.18006511135168E-16));
#36433=CARTESIAN_POINT('Ctrl Pts',(2.91460943608169,-1.8806275411502,1.11022302462516E-16));
#36434=CARTESIAN_POINT('Ctrl Pts',(2.8471863415804,-1.96956302907997,6.34001675707856E-17));
#36435=CARTESIAN_POINT('Ctrl Pts',(2.77582498992288,-2.05512251526362,-2.18484873575661E-16));
#36436=CARTESIAN_POINT('Ctrl Pts',(2.70071126790977,-2.13697549169768,-1.66533453693773E-16));
#36437=CARTESIAN_POINT('Ctrl Pts',(2.6265626894838,-2.21777673120304,-1.1524956270538E-16));
#36438=CARTESIAN_POINT('Ctrl Pts',(2.54875698937316,-2.29496666804747,3.16111469076589E-16));
#36439=CARTESIAN_POINT('Ctrl Pts',(2.46744030034225,-2.36818969290806,1.66533453693773E-16));
#36440=CARTESIAN_POINT('Ctrl Pts',(2.38865944095536,-2.43912928592605,2.1619971139621E-17));
#36441=CARTESIAN_POINT('Ctrl Pts',(2.30658261909198,-2.50634586230322,1.27495535944492E-16));
#36442=CARTESIAN_POINT('Ctrl Pts',(2.22131994895062,-2.56947408053004,1.66533453693773E-16));
#36443=CARTESIAN_POINT('Ctrl Pts',(2.13653932671254,-2.63224539197476,2.05350663525179E-16));
#36444=CARTESIAN_POINT('Ctrl Pts',(2.04860838319626,-2.69097492590926,9.78571983200637E-17));
#36445=CARTESIAN_POINT('Ctrl Pts',(1.95761919937776,-2.74525502143746,5.55111512312578E-17));
#36446=CARTESIAN_POINT('Ctrl Pts',(0.349418900843865,3.91916189049794,24.058));
#36447=CARTESIAN_POINT('Ctrl Pts',(0.983708099956935,3.86349481221817,24.0324107126756));
#36448=CARTESIAN_POINT('Ctrl Pts',(1.60505772607221,3.66267070559658,24.0068214253513));
#36449=CARTESIAN_POINT('Ctrl Pts',(2.13605939111367,3.32170193071062,23.9812321380269));
#36450=CARTESIAN_POINT('Ctrl Pts',(3.23511152224044,2.61597446626503,23.9282681595323));
#36451=CARTESIAN_POINT('Ctrl Pts',(3.94711712557296,1.30987366083964,23.8753041810376));
#36452=CARTESIAN_POINT('Ctrl Pts',(3.94814528315368,0.00380497154103099,
23.822340202543));
#36453=CARTESIAN_POINT('Ctrl Pts',(3.94917344073441,-1.30226371775762,23.7693762240484));
#36454=CARTESIAN_POINT('Ctrl Pts',(3.23922415256329,-2.60830029092949,23.7164122455538));
#36455=CARTESIAN_POINT('Ctrl Pts',(2.14246851744994,-3.3166627231204,23.6634482670591));
#36456=CARTESIAN_POINT('Ctrl Pts',(1.04571288233662,-4.0250251553113,23.6104842885645));
#36457=CARTESIAN_POINT('Ctrl Pts',(-0.437849099718904,-4.13571344652128,
23.5575203100699));
#36458=CARTESIAN_POINT('Ctrl Pts',(-1.62766388484424,-3.59751656345146,
23.5045563315753));
#36459=CARTESIAN_POINT('Ctrl Pts',(-2.81747866996957,-3.05931968038165,
23.4515923530806));
#36460=CARTESIAN_POINT('Ctrl Pts',(-3.71354625816471,-1.87223762303205,
23.398628374586));
#36461=CARTESIAN_POINT('Ctrl Pts',(-3.90551869671661,-0.580571401587583,
23.3456643960914));
#36462=CARTESIAN_POINT('Ctrl Pts',(-3.93389711745665,-0.389630203130338,
23.3378349697575));
#36463=CARTESIAN_POINT('Ctrl Pts',(-3.94688938557907,-0.196403592096446,
23.3300055434235));
#36464=CARTESIAN_POINT('Ctrl Pts',(-3.94525314071248,-0.00295827654940184,
23.3221761170896));
#36465=CARTESIAN_POINT('Origin',(0.,0.,-1.84858989190503));
#36466=CARTESIAN_POINT('',(-1.95761919937781,-2.74525502143742,0.));
#36467=CARTESIAN_POINT('Ctrl Pts',(-1.96186193197216,-2.74910310536277,
-1.68972908581866E-15));
#36468=CARTESIAN_POINT('Ctrl Pts',(-1.11318069597017,-3.34796943221813,
0.0492202025162847));
#36469=CARTESIAN_POINT('Ctrl Pts',(1.27289724729396,-3.73216471134832,0.15142869376082));
#36470=CARTESIAN_POINT('Ctrl Pts',(3.84885445708067,-1.03979978230375,0.306625473733605));
#36471=CARTESIAN_POINT('Ctrl Pts',(2.95737874714596,2.67433718082728,0.465590339918353));
#36472=CARTESIAN_POINT('Ctrl Pts',(-0.647631800440264,3.93376542742361,
0.624555206103101));
#36473=CARTESIAN_POINT('Ctrl Pts',(-3.06550566908991,2.04752208664245,0.752221723431987));
#36474=CARTESIAN_POINT('Ctrl Pts',(-3.36890345256199,0.462673372879177,
0.826899952032626));
#36475=CARTESIAN_POINT('Ctrl Pts',(-3.36692593843476,0.00163208592380858,
0.848589891905015));
#36476=CARTESIAN_POINT('Origin',(0.,0.,0.));
#36477=CARTESIAN_POINT('Ctrl Pts',(-1.47719995289048,3.03093687853778,-0.329233991005386));
#36478=CARTESIAN_POINT('Ctrl Pts',(-2.48630564145415,2.53912496184525,-0.276245702277136));
#36479=CARTESIAN_POINT('Ctrl Pts',(-3.95706612649723,0.476768711041013,
-0.170269124820638));
#36480=CARTESIAN_POINT('Ctrl Pts',(-2.54025446427213,-3.07629710463389,
-0.0113042586358904));
#36481=CARTESIAN_POINT('Ctrl Pts',(1.21035452671364,-3.79753374264191,0.147660607548857));
#36482=CARTESIAN_POINT('Ctrl Pts',(3.84885445708067,-1.03979978230375,0.306625473733605));
#36483=CARTESIAN_POINT('Ctrl Pts',(2.95737874714596,2.67433718082728,0.465590339918353));
#36484=CARTESIAN_POINT('Ctrl Pts',(-0.647631800440264,3.93376542742361,
0.624555206103101));
#36485=CARTESIAN_POINT('Ctrl Pts',(-3.65826453346399,1.58509620284767,0.783520072287847));
#36486=CARTESIAN_POINT('Ctrl Pts',(-3.31298624479799,-2.21807698161905,
0.942484938472596));
#36487=CARTESIAN_POINT('Ctrl Pts',(0.0716483833591926,-3.98622915634864,
1.10144980465734));
#36488=CARTESIAN_POINT('Ctrl Pts',(3.39051798866077,-2.09756782602768,1.26041467084209));
#36489=CARTESIAN_POINT('Ctrl Pts',(3.59899177492058,1.71542482386315,1.41937953702684));
#36490=CARTESIAN_POINT('Ctrl Pts',(0.505790215469384,3.95468340129096,1.57834440321159));
#36491=CARTESIAN_POINT('Ctrl Pts',(-3.05141119286119,2.56598394358578,1.73730926939633));
#36492=CARTESIAN_POINT('Ctrl Pts',(-3.80929264538726,-1.17672126473752,
1.89627413558108));
#36493=CARTESIAN_POINT('Ctrl Pts',(-1.07258002819951,-3.83991470812214,
2.05523900176583));
#36494=CARTESIAN_POINT('Ctrl Pts',(2.6481020123777,-2.98042525524821,2.21420386795058));
#36495=CARTESIAN_POINT('Ctrl Pts',(3.9394520872816,0.613266379946328,2.37316873413532));
#36496=CARTESIAN_POINT('Ctrl Pts',(1.61680281711694,3.64435532093595,2.53213360032008));
#36497=CARTESIAN_POINT('Ctrl Pts',(-2.18907900650795,3.33216312280983,2.69109846650482));
#36498=CARTESIAN_POINT('Ctrl Pts',(-3.98672992391563,-0.0369098299799313,
2.85006333268957));
#36499=CARTESIAN_POINT('Ctrl Pts',(-2.12700963248002,-3.37212213291773,
3.00902819887431));
#36500=CARTESIAN_POINT('Ctrl Pts',(1.68400001564517,-3.61379602896036,3.16799306505907));
#36501=CARTESIAN_POINT('Ctrl Pts',(3.95013122707835,-0.540223147458982,
3.32695793124381));
#36502=CARTESIAN_POINT('Ctrl Pts',(2.59246639543577,3.02894300530038,3.48592279742856));
#36503=CARTESIAN_POINT('Ctrl Pts',(-1.14349143614182,3.81939852540782,3.6448876636133));
#36504=CARTESIAN_POINT('Ctrl Pts',(-3.83042595833975,1.10599038526397,3.80385252979806));
#36505=CARTESIAN_POINT('Ctrl Pts',(-3.00338040757504,-2.62203811565132,
3.9628173959828));
#36506=CARTESIAN_POINT('Ctrl Pts',(0.57892500607099,-3.94464492605495,4.12178226216755));
#36507=CARTESIAN_POINT('Ctrl Pts',(3.63013258458704,-1.64848875417016,4.2807471283523));
#36508=CARTESIAN_POINT('Ctrl Pts',(3.35110647594949,2.15996831943484,4.43971199453705));
#36509=CARTESIAN_POINT('Ctrl Pts',(-0.00217860669321579,3.9869001753454,
4.59867686072179));
#36510=CARTESIAN_POINT('Ctrl Pts',(-3.35346506555395,2.15630466503255,4.75764172690654));
#36511=CARTESIAN_POINT('Ctrl Pts',(-3.6283288127004,-1.65245507692285,4.91660659309129));
#36512=CARTESIAN_POINT('Ctrl Pts',(-0.574613628296617,-3.94527526701846,
5.07557145927603));
#36513=CARTESIAN_POINT('Ctrl Pts',(3.0062441927532,-2.61875420913902,5.2345363254608));
#36514=CARTESIAN_POINT('Ctrl Pts',(3.8292149534867,1.11017592945447,5.39350119164552));
#36515=CARTESIAN_POINT('Ctrl Pts',(1.13931660104628,3.82064594498541,5.55246605783029));
#36516=CARTESIAN_POINT('Ctrl Pts',(-2.59577512563926,3.02610793784054,5.71143092401502));
#36517=CARTESIAN_POINT('Ctrl Pts',(-3.94953846664522,-0.544539856061292,
5.87039579019978));
#36518=CARTESIAN_POINT('Ctrl Pts',(-1.68004955900417,-3.61563427819245,
6.02936065638453));
#36519=CARTESIAN_POINT('Ctrl Pts',(2.13069369871068,-3.3697955600636,6.18832552256926));
#36520=CARTESIAN_POINT('Ctrl Pts',(3.98676787287831,-0.032552759256669,
6.34729038875402));
#36521=CARTESIAN_POINT('Ctrl Pts',(2.18543605335013,3.3345534950076,6.50625525493876));
#36522=CARTESIAN_POINT('Ctrl Pts',(-1.62078473268592,3.64258625218979,6.66522012112352));
#36523=CARTESIAN_POINT('Ctrl Pts',(-3.94011990490355,0.608960498992104,
6.82418498730826));
#36524=CARTESIAN_POINT('Ctrl Pts',(-2.64484328742837,-2.98331723745481,
6.98314985349301));
#36525=CARTESIAN_POINT('Ctrl Pts',(1.07677617223565,-3.83874078693202,7.14211471967776));
#36526=CARTESIAN_POINT('Ctrl Pts',(3.81057598656871,-1.17255635469506,7.3010795858625));
#36527=CARTESIAN_POINT('Ctrl Pts',(3.04860581952888,2.56931514444696,7.46004445204726));
#36528=CARTESIAN_POINT('Ctrl Pts',(-0.510113381387115,3.95413228059959,
7.619009318232));
#36529=CARTESIAN_POINT('Ctrl Pts',(-3.60086158473341,1.71148286638841,7.77797418441675));
#36530=CARTESIAN_POINT('Ctrl Pts',(-3.38822891354565,-2.10125738160825,
7.93693905060149));
#36531=CARTESIAN_POINT('Ctrl Pts',(-0.0672816548149041,-3.98633301836102,
8.09590391678625));
#36532=CARTESIAN_POINT('Ctrl Pts',(3.31538886833258,-2.21440159096907,8.25486878297098));
#36533=CARTESIAN_POINT('Ctrl Pts',(3.65656725922866,1.58899138861319,8.41383364915575));
#36534=CARTESIAN_POINT('Ctrl Pts',(0.643261156248369,3.93466553079316,8.57279851534047));
#36535=CARTESIAN_POINT('Ctrl Pts',(-2.96016388101437,2.67073165104392,8.73176338152524));
#36536=CARTESIAN_POINT('Ctrl Pts',(-3.84797530194499,-1.04329469948394,
8.89072824770997));
#36537=CARTESIAN_POINT('Ctrl Pts',(-1.20570712414377,-3.80021684712055,
9.04969311389473));
#36538=CARTESIAN_POINT('Ctrl Pts',(2.54266018034211,-3.07087234538534,9.20865798007948));
#36539=CARTESIAN_POINT('Ctrl Pts',(3.95842601916979,0.47564819468749,9.36762284626423));
#36540=CARTESIAN_POINT('Ctrl Pts',(1.74278629094578,3.58581562527152,9.52658771244896));
#36541=CARTESIAN_POINT('Ctrl Pts',(-2.07166160205713,3.40640513751843,9.68555257863373));
#36542=CARTESIAN_POINT('Ctrl Pts',(-3.98559564477585,0.102005444431573,
9.84451744481845));
#36543=CARTESIAN_POINT('Ctrl Pts',(-2.24319907973156,-3.29597263991092,
10.0034823110032));
#36544=CARTESIAN_POINT('Ctrl Pts',(1.55707745747673,-3.67027077281332,10.1624471771879));
#36545=CARTESIAN_POINT('Ctrl Pts',(3.928912558612,-0.677512997019795,10.3214120433727));
#36546=CARTESIAN_POINT('Ctrl Pts',(2.69641733534343,2.93678588051791,10.4803769095574));
#36547=CARTESIAN_POINT('Ctrl Pts',(-1.00973405207762,3.8569177977272,10.6393417757422));
#36548=CARTESIAN_POINT('Ctrl Pts',(-3.7895693127859,1.2387663936115,10.7983066419269));
#36549=CARTESIAN_POINT('Ctrl Pts',(-3.0929058256244,-2.51581225614482,10.9572715081117));
#36550=CARTESIAN_POINT('Ctrl Pts',(0.441146911493231,-3.96241935650807,
11.1162363742964));
#36551=CARTESIAN_POINT('Ctrl Pts',(3.57049754163045,-1.77395745708877,11.2752012404812));
#36552=CARTESIAN_POINT('Ctrl Pts',(3.42432285260543,2.04190860605321,11.4341661066659));
#36553=CARTESIAN_POINT('Ctrl Pts',(0.136721492950909,3.98455580808139,11.5931309728507));
#36554=CARTESIAN_POINT('Ctrl Pts',(-3.27630628322196,2.27182633422323,11.7520958390354));
#36555=CARTESIAN_POINT('Ctrl Pts',(-3.683695752997,-1.52504536119478,11.9110607052202));
#36556=CARTESIAN_POINT('Ctrl Pts',(-0.711713421966334,-3.92286142494773,
12.0700255714049));
#36557=CARTESIAN_POINT('Ctrl Pts',(2.91318501009988,-2.72189839106446,12.2289904375897));
#36558=CARTESIAN_POINT('Ctrl Pts',(3.86556759564105,0.976096776902648,12.3879553037744));
#36559=CARTESIAN_POINT('Ctrl Pts',(1.27173165426137,3.77863419159615,12.5469201699592));
#36560=CARTESIAN_POINT('Ctrl Pts',(-2.48877340931887,3.11470458814592,12.7058850361439));
#36561=CARTESIAN_POINT('Ctrl Pts',(-3.96611198956382,-0.406612150074322,
12.8648499023287));
#36562=CARTESIAN_POINT('Ctrl Pts',(-1.80499399926681,-3.5549084962852,13.0238147685134));
#36563=CARTESIAN_POINT('Ctrl Pts',(2.01200065152342,-3.44198069904803,13.1827796346982));
#36564=CARTESIAN_POINT('Ctrl Pts',(3.98321358718988,-0.171427165804589,
13.3417445008829));
#36565=CARTESIAN_POINT('Ctrl Pts',(2.30028118194861,3.25639129072706,13.5007093670677));
#36566=CARTESIAN_POINT('Ctrl Pts',(-1.49289753065309,3.69684118097057,13.6596742332524));
#36567=CARTESIAN_POINT('Ctrl Pts',(-3.91651258901516,0.74585983564986,13.8186390994372));
#36568=CARTESIAN_POINT('Ctrl Pts',(-2.74717288447362,-2.88936306080816,
13.9776039656219));
#36569=CARTESIAN_POINT('Ctrl Pts',(0.942385426660244,-3.87392403926152,
14.1365688318067));
#36570=CARTESIAN_POINT('Ctrl Pts',(3.76741231340739,-1.30460040439068,14.2955336979914));
#36571=CARTESIAN_POINT('Ctrl Pts',(3.1362669786623,2.46154569181692,14.4544985641762));
#36572=CARTESIAN_POINT('Ctrl Pts',(-0.372046531241306,3.96950363810656,
14.6134634303609));
#36573=CARTESIAN_POINT('Ctrl Pts',(-3.53904967227374,1.83589356214594,14.7724282965457));
#36574=CARTESIAN_POINT('Ctrl Pts',(-3.45937733680892,-1.98194000815431,
14.9313931627304));
#36575=CARTESIAN_POINT('Ctrl Pts',(-0.206119829211681,-3.98156908396121,
15.0903580289152));
#36576=CARTESIAN_POINT('Ctrl Pts',(3.23622917375625,-2.32856146349605,15.2493228950999));
#36577=CARTESIAN_POINT('Ctrl Pts',(3.70970605913983,1.46063640552025,15.4082877612846));
#36578=CARTESIAN_POINT('Ctrl Pts',(0.779949646731194,3.90986653262151,15.5672526274694));
#36579=CARTESIAN_POINT('Ctrl Pts',(-2.86532184046814,2.77223889751338,15.7262174936541));
#36580=CARTESIAN_POINT('Ctrl Pts',(-3.88198649442593,-0.908602559673156,
15.8851823598389));
#36581=CARTESIAN_POINT('Ctrl Pts',(-1.33737014962086,-3.75590452983738,
16.0441472260236));
#36582=CARTESIAN_POINT('Ctrl Pts',(2.43413116992486,-3.15759136082396,16.2031120922084));
#36583=CARTESIAN_POINT('Ctrl Pts',(3.97259404474729,0.337452678146523,16.3620769583931));
#36584=CARTESIAN_POINT('Ctrl Pts',(1.86665380078734,3.52292227310739,16.5210418245779));
#36585=CARTESIAN_POINT('Ctrl Pts',(-1.95172895721992,3.47651144567355,16.6800066907626));
#36586=CARTESIAN_POINT('Ctrl Pts',(-3.97962242319515,0.240796850378547,
16.8389715569474));
#36587=CARTESIAN_POINT('Ctrl Pts',(-2.35666503270154,-3.21582146239366,
16.9979364231321));
#36588=CARTESIAN_POINT('Ctrl Pts',(1.42826443406275,-3.7222894112013,17.1569012893169));
#36589=CARTESIAN_POINT('Ctrl Pts',(3.90292376012977,-0.813980268166524,
17.3158661555016));
#36590=CARTESIAN_POINT('Ctrl Pts',(2.79709452794753,2.84106317354542,17.4748310216864));
#36591=CARTESIAN_POINT('Ctrl Pts',(-0.87475073969136,3.88975434928213,17.6337958878711));
#36592=CARTESIAN_POINT('Ctrl Pts',(-3.74411171420101,1.37003840308681,17.7927607540559));
#36593=CARTESIAN_POINT('Ctrl Pts',(-3.1786761163436,-2.40653192410502,17.9517256202406));
#36594=CARTESIAN_POINT('Ctrl Pts',(0.302833216085013,-3.97538297495793,
18.1106904864254));
#36595=CARTESIAN_POINT('Ctrl Pts',(3.5065275226793,-1.89727238082542,18.2696553526101));
#36596=CARTESIAN_POINT('Ctrl Pts',(3.49338172535042,1.92136979140851,18.4286202187948));
#36597=CARTESIAN_POINT('Ctrl Pts',(0.275455597698851,3.97737375262188,18.5875850849796));
#36598=CARTESIAN_POINT('Ctrl Pts',(-3.19516970536172,2.38458975681184,18.7465499511644));
#36599=CARTESIAN_POINT('Ctrl Pts',(-3.73459028221552,-1.3957840729596,18.9055148173491));
#36600=CARTESIAN_POINT('Ctrl Pts',(-0.847949117405149,-3.89568479841959,
19.0644796835338));
#36601=CARTESIAN_POINT('Ctrl Pts',(2.81658890100978,-2.82173788950715,19.2234445497186));
#36602=CARTESIAN_POINT('Ctrl Pts',(3.89722701433046,0.840832535700663,19.3824094159033));
#36603=CARTESIAN_POINT('Ctrl Pts',(1.40260268563389,3.73203476143841,19.5413742820881));
#36604=CARTESIAN_POINT('Ctrl Pts',(-2.3787500488546,3.19951964512964,19.7003391482728));
#36605=CARTESIAN_POINT('Ctrl Pts',(-3.97787021705804,-0.268190772315832,
19.8593040144576));
#36606=CARTESIAN_POINT('Ctrl Pts',(-1.92774697870435,-3.4898666651324,20.0182688806423));
#36607=CARTESIAN_POINT('Ctrl Pts',(1.89086481476229,-3.50998689564495,20.1772337468271));
#36608=CARTESIAN_POINT('Ctrl Pts',(3.97482324267393,-0.310093440809367,
20.3361986130118));
#36609=CARTESIAN_POINT('Ctrl Pts',(2.41233351706024,3.17427546962878,20.4951634791965));
#36610=CARTESIAN_POINT('Ctrl Pts',(-1.36319778790607,3.74660773920425,20.6541283453813));
#36611=CARTESIAN_POINT('Ctrl Pts',(-3.88815019533756,0.881853615583829,
20.813093211566));
#36612=CARTESIAN_POINT('Ctrl Pts',(-2.84616711491744,-2.79190087828212,
20.9720580777508));
#36613=CARTESIAN_POINT('Ctrl Pts',(0.806850527235046,-3.9044039261228,21.1310229439355));
#36614=CARTESIAN_POINT('Ctrl Pts',(3.71967457752779,-1.43506051902692,21.2899878101203));
#36615=CARTESIAN_POINT('Ctrl Pts',(3.22012038549849,2.35078763921597,21.448952676305));
#36616=CARTESIAN_POINT('Ctrl Pts',(-0.233528014234224,3.98005560769136,
21.6079175424898));
#36617=CARTESIAN_POINT('Ctrl Pts',(-3.47294089147738,1.95807523322667,21.7668824086745));
#36618=CARTESIAN_POINT('Ctrl Pts',(-3.52632583653101,-1.86021624962628,
21.9258472748593));
#36619=CARTESIAN_POINT('Ctrl Pts',(-0.344707483447601,-3.97197126386073,
22.0848121410441));
#36620=CARTESIAN_POINT('Ctrl Pts',(3.15313982968432,-2.43989387002868,22.2437770072288));
#36621=CARTESIAN_POINT('Ctrl Pts',(3.75834184644668,1.33050740634341,22.4027418734136));
#36622=CARTESIAN_POINT('Ctrl Pts',(0.915689325102905,3.88032175554439,22.5617067395983));
#36623=CARTESIAN_POINT('Ctrl Pts',(-2.76699741760937,2.87037799557025,22.720671605783));
#36624=CARTESIAN_POINT('Ctrl Pts',(-3.91129134187434,-0.7728027958352,22.8796364719677));
#36625=CARTESIAN_POINT('Ctrl Pts',(-1.46739644894177,-3.70704069007233,
23.0386013381526));
#36626=CARTESIAN_POINT('Ctrl Pts',(2.32262200499063,-3.24046036848089,23.1975662043372));
#36627=CARTESIAN_POINT('Ctrl Pts',(3.98198637087808,0.198816238648098,23.3565310705221));
#36628=CARTESIAN_POINT('Ctrl Pts',(1.98816433058814,3.45581133218519,23.5154959367067));
#36629=CARTESIAN_POINT('Ctrl Pts',(-1.82925354411967,3.5422830008711,23.6744608028915));
#36630=CARTESIAN_POINT('Ctrl Pts',(-3.96914826399699,0.379513463839679,
23.8334256690762));
#36631=CARTESIAN_POINT('Ctrl Pts',(-2.46663759784563,-3.13218185614485,
23.992390535261));
#36632=CARTESIAN_POINT('Ctrl Pts',(1.29650641132588,-3.76899081084458,24.1513554014457));
#36633=CARTESIAN_POINT('Ctrl Pts',(3.87454091099827,-0.951014904317504,
24.3103202676305));
#36634=CARTESIAN_POINT('Ctrl Pts',(2.88961752940844,2.74513957150359,24.4692851338152));
#36635=CARTESIAN_POINT('Ctrl Pts',(0.478408881098333,3.52136284087264,24.5752617112718));
#36636=CARTESIAN_POINT('Ctrl Pts',(-0.624728334461281,3.3133687646595,24.62825));
#36637=CARTESIAN_POINT('Ctrl Pts',(-1.56047750639987,3.20180677844002,-0.219489327336924));
#36638=CARTESIAN_POINT('Ctrl Pts',(-2.62647180561611,2.68226882971724,-0.166501038608675));
#36639=CARTESIAN_POINT('Ctrl Pts',(-4.1801468173981,0.503646678216414,-0.0605244611521764));
#36640=CARTESIAN_POINT('Ctrl Pts',(-2.683462008154,-3.24972419975438,0.0984404050325707));
#36641=CARTESIAN_POINT('Ctrl Pts',(1.27858859595154,-4.01162075153852,0.257405271217319));
#36642=CARTESIAN_POINT('Ctrl Pts',(4.06583468536472,-1.09841878093043,0.416370137402066));
#36643=CARTESIAN_POINT('Ctrl Pts',(3.12410178716573,2.82510367472183,0.575335003586814));
#36644=CARTESIAN_POINT('Ctrl Pts',(-0.684142221260432,4.15553253500754,
0.734299869771561));
#36645=CARTESIAN_POINT('Ctrl Pts',(-3.86450020240029,1.67445643711512,0.89326473595631));
#36646=CARTESIAN_POINT('Ctrl Pts',(-3.49975675527435,-2.3431216813317,1.05222960214106));
#36647=CARTESIAN_POINT('Ctrl Pts',(0.0756875806712427,-4.21095392107594,
1.2111944683258));
#36648=CARTESIAN_POINT('Ctrl Pts',(3.58165937251524,-2.21581878895911,1.37015933451055));
#36649=CARTESIAN_POINT('Ctrl Pts',(3.80188592579657,1.81213236997502,1.5291242006953));
#36650=CARTESIAN_POINT('Ctrl Pts',(0.534304277936582,4.17762976540319,1.68808906688005));
#36651=CARTESIAN_POINT('Ctrl Pts',(-3.22343533786296,2.71064199393843,1.8470539330648));
#36652=CARTESIAN_POINT('Ctrl Pts',(-4.02404256565933,-1.24305924958384,
2.00601879924955));
#36653=CARTESIAN_POINT('Ctrl Pts',(-1.1330470222017,-4.05639095560061,2.16498366543429));
#36654=CARTESIAN_POINT('Ctrl Pts',(2.79738949143739,-3.14844754849901,2.32394853161904));
#36655=CARTESIAN_POINT('Ctrl Pts',(4.1615397818786,0.647839440737169,2.48291339780379));
#36656=CARTESIAN_POINT('Ctrl Pts',(1.70795052048174,3.84980685419155,2.64187826398853));
#36657=CARTESIAN_POINT('Ctrl Pts',(-2.31248893740054,3.52001473505691,2.80084313017328));
#36658=CARTESIAN_POINT('Ctrl Pts',(-4.21148291955221,-0.0389906317936465,
2.95980799635803));
#36659=CARTESIAN_POINT('Ctrl Pts',(-2.2469203853454,-3.56222644534663,3.11877286254278));
#36660=CARTESIAN_POINT('Ctrl Pts',(1.77893597955331,-3.81752477372836,3.27773772872752));
#36661=CARTESIAN_POINT('Ctrl Pts',(4.17282096111768,-0.570678375934639,
3.43670259491227));
#36662=CARTESIAN_POINT('Ctrl Pts',(2.73861740129298,3.19970050005065,3.59566746109702));
#36663=CARTESIAN_POINT('Ctrl Pts',(-1.20795608026431,4.03471816744471,3.75463232728177));
#36664=CARTESIAN_POINT('Ctrl Pts',(-4.04636727494025,1.16834089733205,3.91359719346651));
#36665=CARTESIAN_POINT('Ctrl Pts',(-3.17269680384994,-2.76985623536663,
4.07256205965127));
#36666=CARTESIAN_POINT('Ctrl Pts',(0.611562062467236,-4.1670253683656,4.23152692583601));
#36667=CARTESIAN_POINT('Ctrl Pts',(3.83478230717035,-1.74142276094858,4.39049179202076));
#36668=CARTESIAN_POINT('Ctrl Pts',(3.5400260249384,2.28173712733952,4.54945665820551));
#36669=CARTESIAN_POINT('Ctrl Pts',(-0.00230142624457838,4.21166276895315,
4.70842152439025));
#36670=CARTESIAN_POINT('Ctrl Pts',(-3.54251758068034,2.27786693341294,4.867386390575));
#36671=CARTESIAN_POINT('Ctrl Pts',(-3.83287684714762,-1.74561268623704,
5.02635125675975));
#36672=CARTESIAN_POINT('Ctrl Pts',(-0.607007629585367,-4.16769124497425,
5.18531612294449));
#36673=CARTESIAN_POINT('Ctrl Pts',(3.17572203570494,-2.76638719772175,5.34428098912925));
#36674=CARTESIAN_POINT('Ctrl Pts',(4.04508799935564,1.17276240272716,5.50324585531399));
#36675=CARTESIAN_POINT('Ctrl Pts',(1.20354588769234,4.03603591064399,5.66221072149874));
#36676=CARTESIAN_POINT('Ctrl Pts',(-2.74211266207147,3.19670560488322,5.82117558768349));
#36677=CARTESIAN_POINT('Ctrl Pts',(-4.17219478365215,-0.575238440171331,
5.98014045386823));
#36678=CARTESIAN_POINT('Ctrl Pts',(-1.77476281483295,-3.81946665476637,
6.13910532005299));
#36679=CARTESIAN_POINT('Ctrl Pts',(2.2508121418228,-3.55976871130813,6.29807018623772));
#36680=CARTESIAN_POINT('Ctrl Pts',(4.21152300789809,-0.0343879300103317,
6.45703505242249));
#36681=CARTESIAN_POINT('Ctrl Pts',(2.30864061175677,3.52253986514459,6.61599991860723));
#36682=CARTESIAN_POINT('Ctrl Pts',(-1.71215691763581,3.84793805370841,6.77496478479197));
#36683=CARTESIAN_POINT('Ctrl Pts',(-4.16224524790261,0.643290814560192,
6.93392965097673));
#36684=CARTESIAN_POINT('Ctrl Pts',(-2.79394705497301,-3.1515025669977,7.09289451716147));
#36685=CARTESIAN_POINT('Ctrl Pts',(1.13747972501166,-4.05515085428062,7.25185938334622));
#36686=CARTESIAN_POINT('Ctrl Pts',(4.02539825555276,-1.23865954159255,7.41082424953096));
#36687=CARTESIAN_POINT('Ctrl Pts',(3.22047181083767,2.71416099216412,7.56978911571571));
#36688=CARTESIAN_POINT('Ctrl Pts',(-0.538871163521626,4.1770475751313,7.72875398190046));
#36689=CARTESIAN_POINT('Ctrl Pts',(-3.80386114665173,1.80796818356375,7.8877188480852));
#36690=CARTESIAN_POINT('Ctrl Pts',(-3.57924125016108,-2.21971634425003,
8.04668371426996));
#36691=CARTESIAN_POINT('Ctrl Pts',(-0.0710746766045851,-4.21106363833782,
8.2056485804547));
#36692=CARTESIAN_POINT('Ctrl Pts',(3.50229482737133,-2.33923908952323,8.36461344663945));
#36693=CARTESIAN_POINT('Ctrl Pts',(3.86270724386325,1.6785712150492,8.5235783128242));
#36694=CARTESIAN_POINT('Ctrl Pts',(0.679525180800456,4.15648338195204,8.68254317900894));
#36695=CARTESIAN_POINT('Ctrl Pts',(-3.12704393372178,2.82129488220555,8.8415080451937));
#36696=CARTESIAN_POINT('Ctrl Pts',(-4.06490596761654,-1.10211072502764,
9.00047291137844));
#36697=CARTESIAN_POINT('Ctrl Pts',(-1.27367919478393,-4.0144551167699,9.15943777756319));
#36698=CARTESIAN_POINT('Ctrl Pts',(2.68600334712891,-3.24399361821161,9.31840264374794));
#36699=CARTESIAN_POINT('Ctrl Pts',(4.18158337439399,0.502462992445402,9.47736750993269));
#36700=CARTESIAN_POINT('Ctrl Pts',(1.84103634728762,3.7879669670882,9.63633237611743));
#36701=CARTESIAN_POINT('Ctrl Pts',(-2.18845209448917,3.59844216375801,9.79529724230219));
#36702=CARTESIAN_POINT('Ctrl Pts',(-4.21028469511404,0.107756029408409,
9.95426210848692));
#36703=CARTESIAN_POINT('Ctrl Pts',(-2.36966004463275,-3.48178400373378,
10.1132269746717));
#36704=CARTESIAN_POINT('Ctrl Pts',(1.64485812726998,-3.87718329679412,10.2721918408564));
#36705=CARTESIAN_POINT('Ctrl Pts',(4.15040608438235,-0.71570797851312,10.4311567070412));
#36706=CARTESIAN_POINT('Ctrl Pts',(2.84842860401989,3.1023479920194,10.5901215732259));
#36707=CARTESIAN_POINT('Ctrl Pts',(-1.06665808689608,4.07435259905726,10.7490864394107));
#36708=CARTESIAN_POINT('Ctrl Pts',(-4.00320732475952,1.30860218965774,10.9080513055954));
#36709=CARTESIAN_POINT('Ctrl Pts',(-3.26726924195739,-2.657641863823,11.0670161717801));
#36710=CARTESIAN_POINT('Ctrl Pts',(0.466016689924724,-4.18580183722271,
11.2259810379649));
#36711=CARTESIAN_POINT('Ctrl Pts',(3.77178532227006,-1.87396479649261,11.3849459041496));
#36712=CARTESIAN_POINT('Ctrl Pts',(3.61736999495961,2.15702176515476,11.5439107703344));
#36713=CARTESIAN_POINT('Ctrl Pts',(0.144429204708414,4.20918623734002,11.7028756365191));
#36714=CARTESIAN_POINT('Ctrl Pts',(-3.4610089507791,2.39990116846763,11.8618405027039));
#36715=CARTESIAN_POINT('Ctrl Pts',(-3.89136511392694,-1.61102021275272,
12.0208053688886));
#36716=CARTESIAN_POINT('Ctrl Pts',(-0.751836461819641,-4.14401381639395,
12.1797702350734));
#36717=CARTESIAN_POINT('Ctrl Pts',(3.07741661604235,-2.87534616126336,12.3387351012581));
#36718=CARTESIAN_POINT('Ctrl Pts',(4.08349003170681,1.03112450108435,12.4976999674429));
#36719=CARTESIAN_POINT('Ctrl Pts',(1.34342587594075,3.99165573310602,12.6566648336276));
#36720=CARTESIAN_POINT('Ctrl Pts',(-2.62907869457274,3.29029691570976,12.8156296998124));
#36721=CARTESIAN_POINT('Ctrl Pts',(-4.18970264348228,-0.429535021835278,
12.9745945659971));
#36722=CARTESIAN_POINT('Ctrl Pts',(-1.90675103226963,-3.75531744020717,
13.1335594321819));
#36723=CARTESIAN_POINT('Ctrl Pts',(2.12542774146498,-3.63602330735055,13.2925242983666));
#36724=CARTESIAN_POINT('Ctrl Pts',(4.2077683483767,-0.181091419411761,13.4514891645514));
#36725=CARTESIAN_POINT('Ctrl Pts',(2.42996016605737,3.43997124510655,13.6104540307361));
#36726=CARTESIAN_POINT('Ctrl Pts',(-1.577060039425,3.90525161901692,13.7694188969209));
#36727=CARTESIAN_POINT('Ctrl Pts',(-4.13730706309004,0.787907888963343,
13.9283837631056));
#36728=CARTESIAN_POINT('Ctrl Pts',(-2.90204551118784,-3.05225169780932,
14.0873486292903));
#36729=CARTESIAN_POINT('Ctrl Pts',(0.995512664202879,-4.09231757213405,
14.2463134954751));
#36730=CARTESIAN_POINT('Ctrl Pts',(3.97980121844884,-1.37814761089607,14.4052783616599));
#36731=CARTESIAN_POINT('Ctrl Pts',(3.3130748919202,2.60031600701019,14.5642432278446));
#36732=CARTESIAN_POINT('Ctrl Pts',(-0.393020756736522,4.19328549714417,
14.7232080940294));
#36733=CARTESIAN_POINT('Ctrl Pts',(-3.73856457063159,1.9393925665021,14.8821729602141));
#36734=CARTESIAN_POINT('Ctrl Pts',(-3.65440068534852,-2.09367242106057,
15.0411378263989));
#36735=CARTESIAN_POINT('Ctrl Pts',(-0.217739891257386,-4.20603113582635,
15.2001026925836));
#36736=CARTESIAN_POINT('Ctrl Pts',(3.41867248324782,-2.45983475625287,15.3590675587684));
#36737=CARTESIAN_POINT('Ctrl Pts',(3.91884175823025,1.5429801844924,15.5180324249531));
#36738=CARTESIAN_POINT('Ctrl Pts',(0.823919522517587,4.13028633343982,15.6769972911379));
#36739=CARTESIAN_POINT('Ctrl Pts',(-3.02685514706235,2.92852462760477,15.8359621573226));
#36740=CARTESIAN_POINT('Ctrl Pts',(-4.10083455042517,-0.95982527880059,
15.9949270235073));
#36741=CARTESIAN_POINT('Ctrl Pts',(-1.41276475952385,-3.96764468041594,
16.1538918896921));
#36742=CARTESIAN_POINT('Ctrl Pts',(2.57135598390867,-3.3356014419895,16.3128567558768));
#36743=CARTESIAN_POINT('Ctrl Pts',(4.196550126309,0.356476665661734,16.4718216220616));
#36744=CARTESIAN_POINT('Ctrl Pts',(1.97188692205462,3.72152798490289,16.6307864882463));
#36745=CARTESIAN_POINT('Ctrl Pts',(-2.06175821382304,3.67250073431153,16.7897513544311));
#36746=CARTESIAN_POINT('Ctrl Pts',(-4.20397473152436,0.254371839027192,
16.9487162206158));
#36747=CARTESIAN_POINT('Ctrl Pts',(-2.48952267189958,-3.39711428154593,
17.1076810868006));
#36748=CARTESIAN_POINT('Ctrl Pts',(1.50878323424311,-3.93213450022406,17.2666459529853));
#36749=CARTESIAN_POINT('Ctrl Pts',(4.1229521602399,-0.859868629593263,17.4256108191701));
#36750=CARTESIAN_POINT('Ctrl Pts',(2.95478150103885,3.00122889112179,17.5845756853548));
#36751=CARTESIAN_POINT('Ctrl Pts',(-0.924065053159552,4.10904032023471,
17.7435405515396));
#36752=CARTESIAN_POINT('Ctrl Pts',(-3.95518704155557,1.44727469476127,17.9025054177243));
#36753=CARTESIAN_POINT('Ctrl Pts',(-3.35787485639895,-2.54220082301716,
18.0614702839091));
#36754=CARTESIAN_POINT('Ctrl Pts',(0.319905521907667,-4.1994962832271,18.2204351500938));
#36755=CARTESIAN_POINT('Ctrl Pts',(3.70420897591159,-2.00423163296111,18.3794000162786));
#36756=CARTESIAN_POINT('Ctrl Pts',(3.69032208064376,2.02968754169158,18.5383648824633));
#36757=CARTESIAN_POINT('Ctrl Pts',(0.290984482757316,4.20159929152924,18.6973297486481));
#36758=CARTESIAN_POINT('Ctrl Pts',(-3.37529827603299,2.51902166000967,18.8562946148328));
#36759=CARTESIAN_POINT('Ctrl Pts',(-3.94512883622391,-1.47447178385209,
19.0152594810176));
#36760=CARTESIAN_POINT('Ctrl Pts',(-0.895752482047657,-4.11530510007291,
19.1742243472023));
#36761=CARTESIAN_POINT('Ctrl Pts',(2.9753748747426,-2.98081413888224,19.333189213387));
#36762=CARTESIAN_POINT('Ctrl Pts',(4.1169342588298,0.888234701092859,19.4921540795718));
#36763=CARTESIAN_POINT('Ctrl Pts',(1.48167479769069,3.94242924726034,19.6511189457566));
#36764=CARTESIAN_POINT('Ctrl Pts',(-2.5128527369107,3.37989344485135,19.8100838119413));
#36765=CARTESIAN_POINT('Ctrl Pts',(-4.20212374428449,-0.283310100845846,
19.9690486781261));
#36766=CARTESIAN_POINT('Ctrl Pts',(-2.03642424467465,-3.68660885793949,
20.1280135443108));
#36767=CARTESIAN_POINT('Ctrl Pts',(1.9974628385994,-3.70786337197934,20.2869784104955));
#36768=CARTESIAN_POINT('Ctrl Pts',(4.1989049958817,-0.327575043797077,20.4459432766802));
#36769=CARTESIAN_POINT('Ctrl Pts',(2.54832948237039,3.35322612201562,20.6049081428651));
#36770=CARTESIAN_POINT('Ctrl Pts',(-1.44004843801888,3.95782378065465,20.7638730090497));
#36771=CARTESIAN_POINT('Ctrl Pts',(-4.10734573167046,0.931568355633416,
20.9228378752345));
#36772=CARTESIAN_POINT('Ctrl Pts',(-3.00662056859199,-2.94929505794555,
21.0818027414192));
#36773=CARTESIAN_POINT('Ctrl Pts',(0.852336947556435,-4.12451577099776,
21.240767607604));
#36774=CARTESIAN_POINT('Ctrl Pts',(3.92937225458326,-1.51596245036574,21.3997324737888));
#36775=CARTESIAN_POINT('Ctrl Pts',(3.4016555576228,2.48331393874026,21.5586973399735));
#36776=CARTESIAN_POINT('Ctrl Pts',(-0.246693220246651,4.20443233691565,
21.7176622061583));
#36777=CARTESIAN_POINT('Ctrl Pts',(-3.66872888914082,2.0684622628846,21.876627072343));
#36778=CARTESIAN_POINT('Ctrl Pts',(-3.72512342515035,-1.96508645217684,
22.0355919385278));
#36779=CARTESIAN_POINT('Ctrl Pts',(-0.364140462606384,-4.19589223597873,
22.1945568047125));
#36780=CARTESIAN_POINT('Ctrl Pts',(3.33089895455792,-2.57744355781532,22.3535216708973));
#36781=CARTESIAN_POINT('Ctrl Pts',(3.97021940141924,1.4055151272072,22.512486537082));
#36782=CARTESIAN_POINT('Ctrl Pts',(0.967311562579962,4.09907596143147,22.6714514032667));
#36783=CARTESIAN_POINT('Ctrl Pts',(-2.92298765783001,3.03219634429854,22.8304162694515));
#36784=CARTESIAN_POINT('Ctrl Pts',(-4.13179146670604,-0.816369765937287,
22.9893811356362));
#36785=CARTESIAN_POINT('Ctrl Pts',(-1.5501213272205,-3.91602612824874,23.148346001821));
#36786=CARTESIAN_POINT('Ctrl Pts',(2.45356045914115,-3.42314221273843,23.3073108680058));
#36787=CARTESIAN_POINT('Ctrl Pts',(4.20647194740789,0.210024558767638,23.4662757341905));
#36788=CARTESIAN_POINT('Ctrl Pts',(2.10024764138301,3.65063364623366,23.6252406003752));
#36789=CARTESIAN_POINT('Ctrl Pts',(-1.93237821563391,3.74198017901762,23.78420546656));
#36790=CARTESIAN_POINT('Ctrl Pts',(-4.19291008872147,0.400908639713182,
23.9431703327447));
#36791=CARTESIAN_POINT('Ctrl Pts',(-2.60569497064129,-3.30875946949763,
24.1021351989295));
#36792=CARTESIAN_POINT('Ctrl Pts',(1.36959731674678,-3.98146870411307,24.2611000651142));
#36793=CARTESIAN_POINT('Ctrl Pts',(4.09296922018457,-1.00462863103577,24.420064931299));
#36794=CARTESIAN_POINT('Ctrl Pts',(3.05252051214689,2.89989756964007,24.5790297974837));
#36795=CARTESIAN_POINT('Ctrl Pts',(0.505379313311694,3.71988063924714,24.6850063749402));
#36796=CARTESIAN_POINT('Ctrl Pts',(-0.659947566089433,3.50016083979823,
24.7379946636685));
#36797=CARTESIAN_POINT('Ctrl Pts',(-1.64375505990927,3.37267667834226,-0.109744663668463));
#36798=CARTESIAN_POINT('Ctrl Pts',(-2.76663796977808,2.82541269758923,-0.0567563749402136));
#36799=CARTESIAN_POINT('Ctrl Pts',(-4.40322750829897,0.530524645391819,
0.0492202025162849));
#36800=CARTESIAN_POINT('Ctrl Pts',(-2.82666955203587,-3.42315129487488,
0.208185068701033));
#36801=CARTESIAN_POINT('Ctrl Pts',(1.34682266518943,-4.22570776043514,0.36714993488578));
#36802=CARTESIAN_POINT('Ctrl Pts',(4.28281491364878,-1.15703777955712,0.526114801070528));
#36803=CARTESIAN_POINT('Ctrl Pts',(3.29082482718549,2.97587016861638,0.685079667255276));
#36804=CARTESIAN_POINT('Ctrl Pts',(-0.720652642080601,4.37729964259146,
0.844044533440024));
#36805=CARTESIAN_POINT('Ctrl Pts',(-4.07073587133658,1.76381667138256,1.00300939962477));
#36806=CARTESIAN_POINT('Ctrl Pts',(-3.68652726575071,-2.46816638104435,
1.16197426580952));
#36807=CARTESIAN_POINT('Ctrl Pts',(0.0797267779832985,-4.43567868580324,
1.32093913199426));
#36808=CARTESIAN_POINT('Ctrl Pts',(3.7728007563697,-2.33406975189055,1.47990399817901));
#36809=CARTESIAN_POINT('Ctrl Pts',(4.00478007667258,1.90883991608689,1.63886886436376));
#36810=CARTESIAN_POINT('Ctrl Pts',(0.562818340403771,4.40057612951542,1.79783373054851));
#36811=CARTESIAN_POINT('Ctrl Pts',(-3.39545948286473,2.85530004429109,1.95679859673326));
#36812=CARTESIAN_POINT('Ctrl Pts',(-4.23879248593139,-1.30939723443016,
2.11576346291801));
#36813=CARTESIAN_POINT('Ctrl Pts',(-1.19351401620389,-4.27286720307909,
2.27472832910275));
#36814=CARTESIAN_POINT('Ctrl Pts',(2.94667697049707,-3.31646984174982,2.4336931952875));
#36815=CARTESIAN_POINT('Ctrl Pts',(4.3836274764756,0.682412501528009,2.59265806147225));
#36816=CARTESIAN_POINT('Ctrl Pts',(1.79909822384654,4.05525838744716,2.751622927657));
#36817=CARTESIAN_POINT('Ctrl Pts',(-2.43589886829313,3.70786634730399,2.91058779384175));
#36818=CARTESIAN_POINT('Ctrl Pts',(-4.43623591518879,-0.041071433607366,
3.06955266002649));
#36819=CARTESIAN_POINT('Ctrl Pts',(-2.36683113821078,-3.75233075777553,
3.22851752621124));
#36820=CARTESIAN_POINT('Ctrl Pts',(1.87387194346144,-4.02125351849637,3.38748239239599));
#36821=CARTESIAN_POINT('Ctrl Pts',(4.39551069515703,-0.601133604410289,
3.54644725858073));
#36822=CARTESIAN_POINT('Ctrl Pts',(2.88476840715019,3.37045799480092,3.70541212476548));
#36823=CARTESIAN_POINT('Ctrl Pts',(-1.27242072438679,4.25003780948162,3.86437699095023));
#36824=CARTESIAN_POINT('Ctrl Pts',(-4.26230859154076,1.23069140940013,4.02334185713497));
#36825=CARTESIAN_POINT('Ctrl Pts',(-3.34201320012482,-2.91767435508194,
4.18230672331973));
#36826=CARTESIAN_POINT('Ctrl Pts',(0.64419911886348,-4.38940581067625,4.34127158950447));
#36827=CARTESIAN_POINT('Ctrl Pts',(4.03943202975366,-1.834356767727,4.50023645568922));
#36828=CARTESIAN_POINT('Ctrl Pts',(3.72894557392732,2.40350593524421,4.65920132187397));
#36829=CARTESIAN_POINT('Ctrl Pts',(-0.00242424579594498,4.43642536256088,
4.81816618805872));
#36830=CARTESIAN_POINT('Ctrl Pts',(-3.73157009580673,2.39942920179332,4.97713105424346));
#36831=CARTESIAN_POINT('Ctrl Pts',(-4.03742488159485,-1.83877029555123,
5.13609592042822));
#36832=CARTESIAN_POINT('Ctrl Pts',(-0.639401630874114,-4.39010722293004,
5.29506078661295));
#36833=CARTESIAN_POINT('Ctrl Pts',(3.34519987865668,-2.91402018630447,5.45402565279771));
#36834=CARTESIAN_POINT('Ctrl Pts',(4.26096104522458,1.23534887599985,5.61299051898245));
#36835=CARTESIAN_POINT('Ctrl Pts',(1.26777517433839,4.25142587630257,5.77195538516721));
#36836=CARTESIAN_POINT('Ctrl Pts',(-2.88845019850368,3.3673032719259,5.93092025135195));
#36837=CARTESIAN_POINT('Ctrl Pts',(-4.39485110065909,-0.605937024281373,
6.0898851175367));
#36838=CARTESIAN_POINT('Ctrl Pts',(-1.86947607066172,-4.02329903134028,
6.24884998372145));
#36839=CARTESIAN_POINT('Ctrl Pts',(2.37093058493492,-3.74974186255266,6.40781484990618));
#36840=CARTESIAN_POINT('Ctrl Pts',(4.43627814291787,-0.0362231007639915,
6.56677971609095));
#36841=CARTESIAN_POINT('Ctrl Pts',(2.43184517016341,3.71052623528157,6.72574458227568));
#36842=CARTESIAN_POINT('Ctrl Pts',(-1.80352910258568,4.05328985522703,6.88470944846044));
#36843=CARTESIAN_POINT('Ctrl Pts',(-4.38437059090167,0.677621130128278,
7.04367431464518));
#36844=CARTESIAN_POINT('Ctrl Pts',(-2.94305082251765,-3.31968789654059,
7.20263918082993));
#36845=CARTESIAN_POINT('Ctrl Pts',(1.19818327778767,-4.27156092162922,7.36160404701468));
#36846=CARTESIAN_POINT('Ctrl Pts',(4.2402205245368,-1.30476272849002,7.52056891319943));
#36847=CARTESIAN_POINT('Ctrl Pts',(3.39233780214647,2.85900683988128,7.67953377938417));
#36848=CARTESIAN_POINT('Ctrl Pts',(-0.567628945656141,4.39996286966301,
7.83849864556892));
#36849=CARTESIAN_POINT('Ctrl Pts',(-4.00686070857005,1.90445350073909,7.99746351175367));
#36850=CARTESIAN_POINT('Ctrl Pts',(-3.77025358677652,-2.33817530689181,
8.15642837793842));
#36851=CARTESIAN_POINT('Ctrl Pts',(-0.0748676983942658,-4.43579425831462,
8.31539324412316));
#36852=CARTESIAN_POINT('Ctrl Pts',(3.68920078641008,-2.4640765880774,8.47435811030792));
#36853=CARTESIAN_POINT('Ctrl Pts',(4.06884722849785,1.76815104148521,8.63332297649266));
#36854=CARTESIAN_POINT('Ctrl Pts',(0.715789205352545,4.37830123311092,8.79228784267741));
#36855=CARTESIAN_POINT('Ctrl Pts',(-3.29392398642918,2.97185811336718,8.95125270886215));
#36856=CARTESIAN_POINT('Ctrl Pts',(-4.28183663328808,-1.16092675057133,
9.1102175750469));
#36857=CARTESIAN_POINT('Ctrl Pts',(-1.34165126542409,-4.22869338641924,
9.26918244123165));
#36858=CARTESIAN_POINT('Ctrl Pts',(2.82934651391571,-3.41711489103788,9.42814730741641));
#36859=CARTESIAN_POINT('Ctrl Pts',(4.40474072961818,0.529277790203311,9.58711217360113));
#36860=CARTESIAN_POINT('Ctrl Pts',(1.93928640362945,3.99011830890487,9.74607703978591));
#36861=CARTESIAN_POINT('Ctrl Pts',(-2.30524258692121,3.79047918999758,9.90504190597063));
#36862=CARTESIAN_POINT('Ctrl Pts',(-4.43497374545224,0.113506614385248,
10.0640067721554));
#36863=CARTESIAN_POINT('Ctrl Pts',(-2.49612100953394,-3.66759536755666,
10.2229716383401));
#36864=CARTESIAN_POINT('Ctrl Pts',(1.73263879706324,-4.08409582077491,10.3819365045249));
#36865=CARTESIAN_POINT('Ctrl Pts',(4.3718996101527,-0.753902960006452,10.5409013707096));
#36866=CARTESIAN_POINT('Ctrl Pts',(3.00043987269634,3.26791010352089,10.6998662368944));
#36867=CARTESIAN_POINT('Ctrl Pts',(-1.12358212171453,4.29178740038732,10.8588311030791));
#36868=CARTESIAN_POINT('Ctrl Pts',(-4.21684533673315,1.37843798570399,11.0177959692639));
#36869=CARTESIAN_POINT('Ctrl Pts',(-3.44163265829037,-2.79947147150118,
11.1767608354486));
#36870=CARTESIAN_POINT('Ctrl Pts',(0.490886468356214,-4.40918431793734,
11.3357257016334));
#36871=CARTESIAN_POINT('Ctrl Pts',(3.97307310290967,-1.97397213589646,11.4946905678181));
#36872=CARTESIAN_POINT('Ctrl Pts',(3.8104171373138,2.27213492425632,11.6536554340029));
#36873=CARTESIAN_POINT('Ctrl Pts',(0.152136916465922,4.43381666659865,11.8126203001876));
#36874=CARTESIAN_POINT('Ctrl Pts',(-3.64571161833625,2.52797600271203,11.9715851663724));
#36875=CARTESIAN_POINT('Ctrl Pts',(-4.09903447485687,-1.69699506431066,
12.1305500325571));
#36876=CARTESIAN_POINT('Ctrl Pts',(-0.791959501672948,-4.36516620784018,
12.2895148987418));
#36877=CARTESIAN_POINT('Ctrl Pts',(3.24164822198482,-3.02879393146226,12.4484797649266));
#36878=CARTESIAN_POINT('Ctrl Pts',(4.30141246777259,1.08615222526604,12.6074446311113));
#36879=CARTESIAN_POINT('Ctrl Pts',(1.41512009762014,4.2046772746159,12.7664094972961));
#36880=CARTESIAN_POINT('Ctrl Pts',(-2.76938397982661,3.4658892432736,12.9253743634808));
#36881=CARTESIAN_POINT('Ctrl Pts',(-4.41329329740075,-0.452457893596237,
13.0843392296656));
#36882=CARTESIAN_POINT('Ctrl Pts',(-2.00850806527244,-3.95572638412914,
13.2433040958503));
#36883=CARTESIAN_POINT('Ctrl Pts',(2.23885483140653,-3.83006591565308,13.4022689620351));
#36884=CARTESIAN_POINT('Ctrl Pts',(4.43232310956353,-0.19075567301893,13.5612338282198));
#36885=CARTESIAN_POINT('Ctrl Pts',(2.55963915016612,3.62355119948605,13.7201986944046));
#36886=CARTESIAN_POINT('Ctrl Pts',(-1.66122254819691,4.11366205706328,13.8791635605893));
#36887=CARTESIAN_POINT('Ctrl Pts',(-4.35810153716492,0.829955942276827,
14.0381284267741));
#36888=CARTESIAN_POINT('Ctrl Pts',(-3.05691813790205,-3.21514033481048,
14.1970932929588));
#36889=CARTESIAN_POINT('Ctrl Pts',(1.04863990174551,-4.31071110500657,14.3560581591436));
#36890=CARTESIAN_POINT('Ctrl Pts',(4.19219012349031,-1.45169481740146,14.5150230253283));
#36891=CARTESIAN_POINT('Ctrl Pts',(3.48988280517811,2.73908632220345,14.6739878915131));
#36892=CARTESIAN_POINT('Ctrl Pts',(-0.413994982231739,4.41706735618179,
14.8329527576978));
#36893=CARTESIAN_POINT('Ctrl Pts',(-3.93807946898943,2.04289157085825,14.9919176238826));
#36894=CARTESIAN_POINT('Ctrl Pts',(-3.84942403388813,-2.20540483396684,
15.1508824900673));
#36895=CARTESIAN_POINT('Ctrl Pts',(-0.229359953303091,-4.4304931876915,
15.3098473562521));
#36896=CARTESIAN_POINT('Ctrl Pts',(3.60111579273939,-2.5911080490097,15.4688122224368));
#36897=CARTESIAN_POINT('Ctrl Pts',(4.12797745732068,1.62532396346455,15.6277770886216));
#36898=CARTESIAN_POINT('Ctrl Pts',(0.867889398303981,4.35070613425814,15.7867419548063));
#36899=CARTESIAN_POINT('Ctrl Pts',(-3.18838845365656,3.08481035769615,15.9457068209911));
#36900=CARTESIAN_POINT('Ctrl Pts',(-4.31968260642442,-1.01104799792802,
16.1046716871758));
#36901=CARTESIAN_POINT('Ctrl Pts',(-1.48815936942683,-4.1793848309945,16.2636365533605));
#36902=CARTESIAN_POINT('Ctrl Pts',(2.70858079789248,-3.51361152315505,16.4226014195453));
#36903=CARTESIAN_POINT('Ctrl Pts',(4.42050620787071,0.375500653176939,16.5815662857301));
#36904=CARTESIAN_POINT('Ctrl Pts',(2.07712004332191,3.92013369669841,16.7405311519148));
#36905=CARTESIAN_POINT('Ctrl Pts',(-2.17178747042617,3.8684900229495,16.8994960180995));
#36906=CARTESIAN_POINT('Ctrl Pts',(-4.42832703985357,0.267946827675841,
17.0584608842843));
#36907=CARTESIAN_POINT('Ctrl Pts',(-2.62238031109761,-3.57840710069821,
17.217425750469));
#36908=CARTESIAN_POINT('Ctrl Pts',(1.58930203442347,-4.14197958924682,17.3763906166538));
#36909=CARTESIAN_POINT('Ctrl Pts',(4.34298056035004,-0.905756991020003,
17.5353554828385));
#36910=CARTESIAN_POINT('Ctrl Pts',(3.11246847413016,3.16139460869816,17.6943203490233));
#36911=CARTESIAN_POINT('Ctrl Pts',(-0.973379366627741,4.32832629118729,
17.853285215208));
#36912=CARTESIAN_POINT('Ctrl Pts',(-4.16626236891013,1.52451098643573,18.0122500813928));
#36913=CARTESIAN_POINT('Ctrl Pts',(-3.53707359645429,-2.67786972192929,
18.1712149475776));
#36914=CARTESIAN_POINT('Ctrl Pts',(0.336977827730321,-4.42360959149628,
18.3301798137622));
#36915=CARTESIAN_POINT('Ctrl Pts',(3.90189042914389,-2.11119088509681,18.489144679947));
#36916=CARTESIAN_POINT('Ctrl Pts',(3.88726243593711,2.13800529197465,18.6481095461317));
#36917=CARTESIAN_POINT('Ctrl Pts',(0.306513367815784,4.42582483043659,18.8070744123165));
#36918=CARTESIAN_POINT('Ctrl Pts',(-3.55542684670427,2.6534535632075,18.9660392785013));
#36919=CARTESIAN_POINT('Ctrl Pts',(-4.15566739023229,-1.5531594947446,19.125004144686));
#36920=CARTESIAN_POINT('Ctrl Pts',(-0.943555846690173,-4.33492540172624,
19.2839690108708));
#36921=CARTESIAN_POINT('Ctrl Pts',(3.13416084847543,-3.13989038825732,19.4429338770555));
#36922=CARTESIAN_POINT('Ctrl Pts',(4.33664150332913,0.935636866485059,19.6018987432403));
#36923=CARTESIAN_POINT('Ctrl Pts',(1.5607469097475,4.15282373308227,19.760863609425));
#36924=CARTESIAN_POINT('Ctrl Pts',(-2.6469554249668,3.56026724457307,19.9198284756097));
#36925=CARTESIAN_POINT('Ctrl Pts',(-4.42637727151094,-0.298429429375862,
20.0787933417945));
#36926=CARTESIAN_POINT('Ctrl Pts',(-2.14510151064494,-3.88335105074656,
20.2377582079792));
#36927=CARTESIAN_POINT('Ctrl Pts',(2.10406086243651,-3.90573984831374,20.396723074164));
#36928=CARTESIAN_POINT('Ctrl Pts',(4.42298674908946,-0.345056646784782,
20.5556879403487));
#36929=CARTESIAN_POINT('Ctrl Pts',(2.68432544768054,3.53217677440245,20.7146528065335));
#36930=CARTESIAN_POINT('Ctrl Pts',(-1.51689908813168,4.16903982210505,20.8736176727182));
#36931=CARTESIAN_POINT('Ctrl Pts',(-4.32654126800335,0.981283095682997,
21.032582538903));
#36932=CARTESIAN_POINT('Ctrl Pts',(-3.16707402226655,-3.10668923760898,
21.1915474050877));
#36933=CARTESIAN_POINT('Ctrl Pts',(0.897823367877824,-4.34462761587273,
21.3505122712725));
#36934=CARTESIAN_POINT('Ctrl Pts',(4.13906993163872,-1.59686438170456,21.5094771374572));
#36935=CARTESIAN_POINT('Ctrl Pts',(3.58319072974711,2.61584023826454,21.668442003642));
#36936=CARTESIAN_POINT('Ctrl Pts',(-0.25985842625908,4.42880906613994,21.8274068698267));
#36937=CARTESIAN_POINT('Ctrl Pts',(-3.86451688680425,2.17884929254253,21.9863717360115));
#36938=CARTESIAN_POINT('Ctrl Pts',(-3.92392101376968,-2.0699566547274,22.1453366021962));
#36939=CARTESIAN_POINT('Ctrl Pts',(-0.383573441765164,-4.41981320809673,
22.304301468381));
#36940=CARTESIAN_POINT('Ctrl Pts',(3.50865807943151,-2.71499324560195,22.4632663345657));
#36941=CARTESIAN_POINT('Ctrl Pts',(4.1820969563918,1.48052284807099,22.6222312007505));
#36942=CARTESIAN_POINT('Ctrl Pts',(1.01893380005702,4.31783016731854,22.7811960669352));
#36943=CARTESIAN_POINT('Ctrl Pts',(-3.07897789805066,3.19401469302683,22.9401609331199));
#36944=CARTESIAN_POINT('Ctrl Pts',(-4.35229159153774,-0.859936736039379,
23.0991257993047));
#36945=CARTESIAN_POINT('Ctrl Pts',(-1.63284620549922,-4.12501156642513,
23.2580906654894));
#36946=CARTESIAN_POINT('Ctrl Pts',(2.58449891329166,-3.60582405699598,23.4170555316742));
#36947=CARTESIAN_POINT('Ctrl Pts',(4.43095752393771,0.221232878887186,23.5760203978589));
#36948=CARTESIAN_POINT('Ctrl Pts',(2.21233095217787,3.84545596028211,23.7349852640437));
#36949=CARTESIAN_POINT('Ctrl Pts',(-2.03550288714815,3.94167735716416,23.8939501302284));
#36950=CARTESIAN_POINT('Ctrl Pts',(-4.41667191344595,0.422303815586678,
24.0529149964132));
#36951=CARTESIAN_POINT('Ctrl Pts',(-2.74475234343696,-3.48533708285041,
24.2118798625979));
#36952=CARTESIAN_POINT('Ctrl Pts',(1.44268822216767,-4.19394659738156,24.3708447287827));
#36953=CARTESIAN_POINT('Ctrl Pts',(4.31139752937088,-1.05824235775403,24.5298095949674));
#36954=CARTESIAN_POINT('Ctrl Pts',(3.21542349488533,3.05465556777655,24.6887744611522));
#36955=CARTESIAN_POINT('Ctrl Pts',(0.532349745525053,3.91839843762163,24.7947510386087));
#36956=CARTESIAN_POINT('Ctrl Pts',(-0.695166797717585,3.68695291493697,
24.8477393273369));
#36957=CARTESIAN_POINT('Ctrl Pts',(-1.72703261341866,3.5435465782445,-1.38777878078145E-15));
#36958=CARTESIAN_POINT('Ctrl Pts',(-2.90680413394004,2.96855656546122,0.0529882887282479));
#36959=CARTESIAN_POINT('Ctrl Pts',(-4.62630819919985,0.557402612567225,
0.158964866184747));
#36960=CARTESIAN_POINT('Ctrl Pts',(-2.96987709591773,-3.59657838999538,
0.317929732369494));
#36961=CARTESIAN_POINT('Ctrl Pts',(1.41505673442732,-4.43979476933175,0.476894598554242));
#36962=CARTESIAN_POINT('Ctrl Pts',(4.49979514193284,-1.21565677818381,0.635859464738989));
#36963=CARTESIAN_POINT('Ctrl Pts',(3.45754786720525,3.12663666251093,0.794824330923737));
#36964=CARTESIAN_POINT('Ctrl Pts',(-0.757163062900767,4.59906675017539,
0.953789197108486));
#36965=CARTESIAN_POINT('Ctrl Pts',(-4.27697154027288,1.85317690565,1.11275406329323));
#36966=CARTESIAN_POINT('Ctrl Pts',(-3.87329777622707,-2.593211080757,1.27171892947798));
#36967=CARTESIAN_POINT('Ctrl Pts',(0.0837659752953463,-4.66040345053054,
1.43068379566273));
#36968=CARTESIAN_POINT('Ctrl Pts',(3.96394214022417,-2.45232071482198,1.58964866184748));
#36969=CARTESIAN_POINT('Ctrl Pts',(4.20767422754857,2.00554746219876,1.74861352803222));
#36970=CARTESIAN_POINT('Ctrl Pts',(0.591332402870964,4.62352249362764,1.90757839421698));
#36971=CARTESIAN_POINT('Ctrl Pts',(-3.5674836278665,2.99995809464374,2.06654326040171));
#36972=CARTESIAN_POINT('Ctrl Pts',(-4.45354240620347,-1.37573521927647,
2.22550812658647));
#36973=CARTESIAN_POINT('Ctrl Pts',(-1.25398101020607,-4.48934345055757,
2.38447299277121));
#36974=CARTESIAN_POINT('Ctrl Pts',(3.09596444955676,-3.48449213500062,2.54343785895597));
#36975=CARTESIAN_POINT('Ctrl Pts',(4.60571517107261,0.716985562318844,2.70240272514071));
#36976=CARTESIAN_POINT('Ctrl Pts',(1.89024592721134,4.26070992070277,2.86136759132546));
#36977=CARTESIAN_POINT('Ctrl Pts',(-2.55930879918572,3.89571795955106,3.0203324575102));
#36978=CARTESIAN_POINT('Ctrl Pts',(-4.66098891082537,-0.0431522354210798,
3.17929732369495));
#36979=CARTESIAN_POINT('Ctrl Pts',(-2.48674189107617,-3.94243507020443,
3.3382621898797));
#36980=CARTESIAN_POINT('Ctrl Pts',(1.96880790736958,-4.22498226326438,3.49722705606445));
#36981=CARTESIAN_POINT('Ctrl Pts',(4.61820042919637,-0.631588832885941,
3.65619192224919));
#36982=CARTESIAN_POINT('Ctrl Pts',(3.0309194130074,3.54121548955118,3.81515678843395));
#36983=CARTESIAN_POINT('Ctrl Pts',(-1.33688536850928,4.46535745151852,3.97412165461869));
#36984=CARTESIAN_POINT('Ctrl Pts',(-4.47824990814127,1.29304192146821,4.13308652080344));
#36985=CARTESIAN_POINT('Ctrl Pts',(-3.51132959639971,-3.06549247479725,
4.29205138698818));
#36986=CARTESIAN_POINT('Ctrl Pts',(0.676836175259727,-4.61178625298691,
4.45101625317294));
#36987=CARTESIAN_POINT('Ctrl Pts',(4.24408175233697,-1.92729077450542,4.60998111935768));
#36988=CARTESIAN_POINT('Ctrl Pts',(3.91786512291623,2.52527474314889,4.76894598554243));
#36989=CARTESIAN_POINT('Ctrl Pts',(-0.00254706534730991,4.66118795616863,
4.92791085172718));
#36990=CARTESIAN_POINT('Ctrl Pts',(-3.92062261093312,2.52099147017371,5.08687571791192));
#36991=CARTESIAN_POINT('Ctrl Pts',(-4.24197291604209,-1.93192790486543,
5.24584058409668));
#36992=CARTESIAN_POINT('Ctrl Pts',(-0.671795632162863,-4.61252320088583,
5.40480545028142));
#36993=CARTESIAN_POINT('Ctrl Pts',(3.51467772160843,-3.0616531748872,5.56377031646618));
#36994=CARTESIAN_POINT('Ctrl Pts',(4.47683409109351,1.29793534927254,5.72273518265091));
#36995=CARTESIAN_POINT('Ctrl Pts',(1.33200446098445,4.46681584196115,5.88170004883567));
#36996=CARTESIAN_POINT('Ctrl Pts',(-3.03478773493588,3.53790093896858,6.04066491502041));
#36997=CARTESIAN_POINT('Ctrl Pts',(-4.61750741766603,-0.636635608391419,
6.19962978120516));
#36998=CARTESIAN_POINT('Ctrl Pts',(-1.96418932649049,-4.22713140791419,
6.35859464738991));
#36999=CARTESIAN_POINT('Ctrl Pts',(2.49104902804703,-3.93971501379719,6.51755951357465));
#37000=CARTESIAN_POINT('Ctrl Pts',(4.66103327793766,-0.0380582715176506,
6.6765243797594));
#37001=CARTESIAN_POINT('Ctrl Pts',(2.55504972857005,3.89851260541856,6.83548924594414));
#37002=CARTESIAN_POINT('Ctrl Pts',(-1.89490128753556,4.25864165674564,6.9944541121289));
#37003=CARTESIAN_POINT('Ctrl Pts',(-4.60649593390074,0.711951445696367,
7.15341897831364));
#37004=CARTESIAN_POINT('Ctrl Pts',(-3.09215459006229,-3.48787322608348,
7.3123838444984));
#37005=CARTESIAN_POINT('Ctrl Pts',(1.25888683056368,-4.48797098897782,7.47134871068314));
#37006=CARTESIAN_POINT('Ctrl Pts',(4.45504279352084,-1.3708659153875,7.63031357686789));
#37007=CARTESIAN_POINT('Ctrl Pts',(3.56420379345526,3.00385268759844,7.78927844305264));
#37008=CARTESIAN_POINT('Ctrl Pts',(-0.596386727790659,4.62287816419472,
7.94824330923738));
#37009=CARTESIAN_POINT('Ctrl Pts',(-4.20986027048837,2.00093881791443,8.10720817542214));
#37010=CARTESIAN_POINT('Ctrl Pts',(-3.96126592339197,-2.45663426953358,
8.26617304160689));
#37011=CARTESIAN_POINT('Ctrl Pts',(-0.0786607201839425,-4.66052487829143,
8.42513790779162));
#37012=CARTESIAN_POINT('Ctrl Pts',(3.87610674544883,-2.58891408663156,8.58410277397638));
#37013=CARTESIAN_POINT('Ctrl Pts',(4.27498721313245,1.85773086792121,8.74306764016112));
#37014=CARTESIAN_POINT('Ctrl Pts',(0.752053229904626,4.60011908426979,8.90203250634587));
#37015=CARTESIAN_POINT('Ctrl Pts',(-3.46080403913657,3.12242134452881,9.06099737253062));
#37016=CARTESIAN_POINT('Ctrl Pts',(-4.49876729895963,-1.21974277611503,
9.21996223871536));
#37017=CARTESIAN_POINT('Ctrl Pts',(-1.40962333606424,-4.44293165606859,
9.37892710490011));
#37018=CARTESIAN_POINT('Ctrl Pts',(2.97268968070251,-3.59023616386415,9.53789197108486));
#37019=CARTESIAN_POINT('Ctrl Pts',(4.62789808484238,0.556092587961218,9.69685683726961));
#37020=CARTESIAN_POINT('Ctrl Pts',(2.03753645997128,4.19226965072155,9.85582170345435));
#37021=CARTESIAN_POINT('Ctrl Pts',(-2.42203307935326,3.98251621623715,10.0147865696391));
#37022=CARTESIAN_POINT('Ctrl Pts',(-4.65966279579043,0.119257199362087,
10.1737514358238));
#37023=CARTESIAN_POINT('Ctrl Pts',(-2.62258197443514,-3.85340673137953,
10.3327163020086));
#37024=CARTESIAN_POINT('Ctrl Pts',(1.82041946685649,-4.2910083447557,10.4916811681933));
#37025=CARTESIAN_POINT('Ctrl Pts',(4.59339313592305,-0.792097941499782,
10.6506460343781));
#37026=CARTESIAN_POINT('Ctrl Pts',(3.15245114137279,3.43347221502238,10.8096109005628));
#37027=CARTESIAN_POINT('Ctrl Pts',(-1.18050615653299,4.50922220171738,10.9685757667476));
#37028=CARTESIAN_POINT('Ctrl Pts',(-4.43048334870678,1.44827378175024,11.1275406329323));
#37029=CARTESIAN_POINT('Ctrl Pts',(-3.61599607462336,-2.94130107917936,
11.2865054991171));
#37030=CARTESIAN_POINT('Ctrl Pts',(0.515756246787712,-4.63256679865198,
11.4454703653018));
#37031=CARTESIAN_POINT('Ctrl Pts',(4.17436088354928,-2.07397947530031,11.6044352314866));
#37032=CARTESIAN_POINT('Ctrl Pts',(4.00346427966798,2.38724808335786,11.7634000976713));
#37033=CARTESIAN_POINT('Ctrl Pts',(0.159844628223428,4.6584470958573,11.9223649638561));
#37034=CARTESIAN_POINT('Ctrl Pts',(-3.83041428589339,2.65605083695643,12.0813298300408));
#37035=CARTESIAN_POINT('Ctrl Pts',(-4.3067038357868,-1.7829699158686,12.2402946962256));
#37036=CARTESIAN_POINT('Ctrl Pts',(-0.832082541526254,-4.58631859928641,
12.3992595624103));
#37037=CARTESIAN_POINT('Ctrl Pts',(3.40587982792729,-3.18224170166115,12.5582244285951));
#37038=CARTESIAN_POINT('Ctrl Pts',(4.51933490383836,1.14117994944773,12.7171892947798));
#37039=CARTESIAN_POINT('Ctrl Pts',(1.48681431929952,4.41769881612578,12.8761541609645));
#37040=CARTESIAN_POINT('Ctrl Pts',(-2.90968926508048,3.64148157083744,13.0351190271493));
#37041=CARTESIAN_POINT('Ctrl Pts',(-4.63688395131922,-0.475380765357195,
13.1940838933341));
#37042=CARTESIAN_POINT('Ctrl Pts',(-2.11026509827526,-4.1561353280511,13.3530487595188));
#37043=CARTESIAN_POINT('Ctrl Pts',(2.35228192134809,-4.0241085239556,13.5120136257036));
#37044=CARTESIAN_POINT('Ctrl Pts',(4.65687787075036,-0.200419926626097,
13.6709784918883));
#37045=CARTESIAN_POINT('Ctrl Pts',(2.68931813427488,3.80713115386554,13.829943358073));
#37046=CARTESIAN_POINT('Ctrl Pts',(-1.74538505696882,4.32207249510964,13.9889082242578));
#37047=CARTESIAN_POINT('Ctrl Pts',(-4.57889601123979,0.872003995590307,
14.1478730904425));
#37048=CARTESIAN_POINT('Ctrl Pts',(-3.21179076461628,-3.37802897181164,
14.3068379566273));
#37049=CARTESIAN_POINT('Ctrl Pts',(1.10176713928815,-4.5291046378791,14.465802822812));
#37050=CARTESIAN_POINT('Ctrl Pts',(4.40457902853176,-1.52524202390685,14.6247676889968));
#37051=CARTESIAN_POINT('Ctrl Pts',(3.66669071843603,2.87785663739672,14.7837325551815));
#37052=CARTESIAN_POINT('Ctrl Pts',(-0.434969207726955,4.6408492152194,14.9426974213663));
#37053=CARTESIAN_POINT('Ctrl Pts',(-4.13759436734728,2.14639057521441,15.101662287551));
#37054=CARTESIAN_POINT('Ctrl Pts',(-4.04444738242773,-2.3171372468731,15.2606271537358));
#37055=CARTESIAN_POINT('Ctrl Pts',(-0.240980015348797,-4.65495523955664,
15.4195920199205));
#37056=CARTESIAN_POINT('Ctrl Pts',(3.78355910223096,-2.72238134176653,15.5785568861053));
#37057=CARTESIAN_POINT('Ctrl Pts',(4.33711315641111,1.7076677424367,15.73752175229));
#37058=CARTESIAN_POINT('Ctrl Pts',(0.911859274090375,4.57112593507645,15.8964866184748));
#37059=CARTESIAN_POINT('Ctrl Pts',(-3.34992176025076,3.24109608778754,16.0554514846595));
#37060=CARTESIAN_POINT('Ctrl Pts',(-4.53853066242366,-1.06227071705545,
16.2144163508443));
#37061=CARTESIAN_POINT('Ctrl Pts',(-1.56355397932982,-4.39112498157307,
16.373381217029));
#37062=CARTESIAN_POINT('Ctrl Pts',(2.8458056118763,-3.69162160432059,16.5323460832138));
#37063=CARTESIAN_POINT('Ctrl Pts',(4.64446228943243,0.394524640692141,16.6913109493985));
#37064=CARTESIAN_POINT('Ctrl Pts',(2.18235316458919,4.11873940849393,16.8502758155833));
#37065=CARTESIAN_POINT('Ctrl Pts',(-2.2818167270293,4.06447931158747,17.009240681768));
#37066=CARTESIAN_POINT('Ctrl Pts',(-4.65267934818278,0.281521816324489,
17.1682055479527));
#37067=CARTESIAN_POINT('Ctrl Pts',(-2.75523795029565,-3.75969991985049,
17.3271704141375));
#37068=CARTESIAN_POINT('Ctrl Pts',(1.66982083460383,-4.35182467826958,17.4861352803222));
#37069=CARTESIAN_POINT('Ctrl Pts',(4.56300896046017,-0.95164535244674,17.645100146507));
#37070=CARTESIAN_POINT('Ctrl Pts',(3.27015544722148,3.32156032627453,17.8040650126917));
#37071=CARTESIAN_POINT('Ctrl Pts',(-1.02269368009593,4.54761226213988,17.9630298788765));
#37072=CARTESIAN_POINT('Ctrl Pts',(-4.37733769626469,1.6017472781102,18.1219947450612));
#37073=CARTESIAN_POINT('Ctrl Pts',(-3.71627233650965,-2.81353862084143,
18.280959611246));
#37074=CARTESIAN_POINT('Ctrl Pts',(0.354050133552978,-4.64772289976546,
18.4399244774307));
#37075=CARTESIAN_POINT('Ctrl Pts',(4.09957188237618,-2.21815013723249,18.5988893436155));
#37076=CARTESIAN_POINT('Ctrl Pts',(4.08420279123045,2.24632304225772,18.7578542098002));
#37077=CARTESIAN_POINT('Ctrl Pts',(0.322042252874243,4.65005036934395,18.916819075985));
#37078=CARTESIAN_POINT('Ctrl Pts',(-3.73555541737554,2.78788546640533,19.0757839421697));
#37079=CARTESIAN_POINT('Ctrl Pts',(-4.36620594424068,-1.63184720563709,
19.2347488083544));
#37080=CARTESIAN_POINT('Ctrl Pts',(-0.991359211332678,-4.55454570337957,
19.3937136745392));
#37081=CARTESIAN_POINT('Ctrl Pts',(3.29294682220825,-3.29896663763241,19.5526785407239));
#37082=CARTESIAN_POINT('Ctrl Pts',(4.55634874782847,0.983039031877256,19.7116434069087));
#37083=CARTESIAN_POINT('Ctrl Pts',(1.63981902180431,4.3632182189042,19.8706082730935));
#37084=CARTESIAN_POINT('Ctrl Pts',(-2.7810581130229,3.74064104429479,20.0295731392782));
#37085=CARTESIAN_POINT('Ctrl Pts',(-4.65063079873739,-0.313548757905883,
20.188538005463));
#37086=CARTESIAN_POINT('Ctrl Pts',(-2.25377877661524,-4.08009324355364,
20.3475028716477));
#37087=CARTESIAN_POINT('Ctrl Pts',(2.21065888627362,-4.10361632464813,20.5064677378324));
#37088=CARTESIAN_POINT('Ctrl Pts',(4.64706850229723,-0.362538249772487,
20.6654326040172));
#37089=CARTESIAN_POINT('Ctrl Pts',(2.82032141299069,3.71112742678928,20.824397470202));
#37090=CARTESIAN_POINT('Ctrl Pts',(-1.59374973824449,4.38025586355546,20.9833623363867));
#37091=CARTESIAN_POINT('Ctrl Pts',(-4.54573680433624,1.03099783573258,21.1423272025715));
#37092=CARTESIAN_POINT('Ctrl Pts',(-3.32752747594111,-3.2640834172724,21.3012920687562));
#37093=CARTESIAN_POINT('Ctrl Pts',(0.943309788199209,-4.5647394607477,21.4602569349409));
#37094=CARTESIAN_POINT('Ctrl Pts',(4.34876760869419,-1.67776631304337,21.6192218011257));
#37095=CARTESIAN_POINT('Ctrl Pts',(3.76472590187142,2.74836653778883,21.7781866673104));
#37096=CARTESIAN_POINT('Ctrl Pts',(-0.273023632271506,4.65318579536423,
21.9371515334952));
#37097=CARTESIAN_POINT('Ctrl Pts',(-4.06030488446768,2.28923632220046,22.0961163996799));
#37098=CARTESIAN_POINT('Ctrl Pts',(-4.12271860238902,-2.17482685727795,
22.2550812658647));
#37099=CARTESIAN_POINT('Ctrl Pts',(-0.403006420923942,-4.64373418021473,
22.4140461320495));
#37100=CARTESIAN_POINT('Ctrl Pts',(3.68641720430509,-2.85254293338859,22.5730109982341));
#37101=CARTESIAN_POINT('Ctrl Pts',(4.39397451136436,1.55553056893478,22.7319758644189));
#37102=CARTESIAN_POINT('Ctrl Pts',(1.07055603753408,4.53658437320562,22.8909407306037));
#37103=CARTESIAN_POINT('Ctrl Pts',(-3.2349681382713,3.35583304175512,23.0499055967884));
#37104=CARTESIAN_POINT('Ctrl Pts',(-4.57279171636944,-0.903503706141469,
23.2088704629732));
#37105=CARTESIAN_POINT('Ctrl Pts',(-1.71557108377795,-4.33399700460152,
23.3678353291579));
#37106=CARTESIAN_POINT('Ctrl Pts',(2.71543736744218,-3.78850590125353,23.5268001953427));
#37107=CARTESIAN_POINT('Ctrl Pts',(4.65544310046753,0.232441199006727,23.6857650615274));
#37108=CARTESIAN_POINT('Ctrl Pts',(2.32441426297274,4.04027827433057,23.8447299277122));
#37109=CARTESIAN_POINT('Ctrl Pts',(-2.13862755866238,4.14137453531068,24.0036947938969));
#37110=CARTESIAN_POINT('Ctrl Pts',(-4.64043373817043,0.443698991460186,
24.1626596600816));
#37111=CARTESIAN_POINT('Ctrl Pts',(-2.88380971623262,-3.66191469620319,
24.3216245262664));
#37112=CARTESIAN_POINT('Ctrl Pts',(1.51577912758857,-4.40642449065004,24.4805893924511));
#37113=CARTESIAN_POINT('Ctrl Pts',(4.52982583855719,-1.1118560844723,24.6395542586359));
#37114=CARTESIAN_POINT('Ctrl Pts',(3.37832647762378,3.20941356591303,24.7985191248206));
#37115=CARTESIAN_POINT('Ctrl Pts',(0.559320177738415,4.11691623599613,24.9044957022771));
#37116=CARTESIAN_POINT('Ctrl Pts',(-0.730386029345736,3.8737449900757,24.9574839910054));
#37117=CARTESIAN_POINT('Ctrl Pts',(-3.94350653563855,-0.00347714007584369,
23.1778238829104));
#37118=CARTESIAN_POINT('Ctrl Pts',(-3.94586355936157,-0.259474013504655,
23.1881727429313));
#37119=CARTESIAN_POINT('Ctrl Pts',(-3.92307523690983,-0.515053183369563,
23.1985216029522));
#37120=CARTESIAN_POINT('Ctrl Pts',(-3.87361768125451,-0.765363131235343,
23.2088704629732));
#37121=CARTESIAN_POINT('Ctrl Pts',(-3.62038483883896,-2.0470014722948,23.2618587517014));
#37122=CARTESIAN_POINT('Ctrl Pts',(-2.66797796130846,-3.19049923844816,
23.3148470404297));
#37123=CARTESIAN_POINT('Ctrl Pts',(-1.45327311400651,-3.67133293763351,
23.3678353291579));
#37124=CARTESIAN_POINT('Ctrl Pts',(-0.238568266704596,-4.15216663681884,
23.4208236178862));
#37125=CARTESIAN_POINT('Ctrl Pts',(1.23843455036875,-3.9703362690362,23.4738119066144));
#37126=CARTESIAN_POINT('Ctrl Pts',(2.30027024774299,-3.20926323510153,23.5268001953427));
#37127=CARTESIAN_POINT('Ctrl Pts',(3.36210594511727,-2.44819020116684,23.5797884840709));
#37128=CARTESIAN_POINT('Ctrl Pts',(4.00877452279241,-1.10787450108007,23.6327767727992));
#37129=CARTESIAN_POINT('Ctrl Pts',(3.94360400538084,0.196922861517294,23.6857650615274));
#37130=CARTESIAN_POINT('Ctrl Pts',(3.87843348796927,1.50172022411466,23.7387533502557));
#37131=CARTESIAN_POINT('Ctrl Pts',(3.10142387547099,2.77099924922264,23.7917416389839));
#37132=CARTESIAN_POINT('Ctrl Pts',(1.96907876561599,3.42248813860663,23.8447299277122));
#37133=CARTESIAN_POINT('Ctrl Pts',(0.836733655761017,4.07397702799061,23.8977182164404));
#37134=CARTESIAN_POINT('Ctrl Pts',(-0.650946951450773,4.10767578165063,
23.9507065051686));
#37135=CARTESIAN_POINT('Ctrl Pts',(-1.81175495164127,3.50824590117222,24.0036947938969));
#37136=CARTESIAN_POINT('Ctrl Pts',(-2.20830746798924,3.30347006620307,24.0217965292646));
#37137=CARTESIAN_POINT('Ctrl Pts',(-2.56671309215799,3.02480645592577,24.0398982646323));
#37138=CARTESIAN_POINT('Ctrl Pts',(-2.87170785494343,2.69478584831398,24.058));
#37139=CARTESIAN_POINT('Ctrl Pts',(-1.96186193197213,-2.74910310536279,
1.04083408558608E-17));
#37140=CARTESIAN_POINT('Ctrl Pts',(-2.03089214936932,-2.70842374984998,
4.0844089957036E-17));
#37141=CARTESIAN_POINT('Ctrl Pts',(-2.0982520786512,-2.66519645821488,9.07751022854637E-17));
#37142=CARTESIAN_POINT('Ctrl Pts',(-2.16378064478676,-2.619448737651,1.42247325030098E-16));
#37143=CARTESIAN_POINT('Ctrl Pts',(-2.25130095090051,-2.55834783549675,
1.98311708005797E-16));
#37144=CARTESIAN_POINT('Ctrl Pts',(-2.33555581159229,-2.49275291176235,
1.14301651927622E-16));
#37145=CARTESIAN_POINT('Ctrl Pts',(-2.41645347142118,-2.4230636931251,1.90819582357449E-16));
#37146=CARTESIAN_POINT('Ctrl Pts',(-2.46698855966785,-2.37953028534638,
2.38618744594068E-16));
#37147=CARTESIAN_POINT('Ctrl Pts',(-2.51621317497323,-2.33439817262585,
-8.87118969308996E-17));
#37148=CARTESIAN_POINT('Ctrl Pts',(-2.56410004332752,-2.28775595645186,
-9.0205620750794E-17));
#37149=CARTESIAN_POINT('Ctrl Pts',(-2.58450501257648,-2.26788134323446,
-9.08421081566083E-17));
#37150=CARTESIAN_POINT('Ctrl Pts',(-2.60466703883067,-2.24773246660606,
1.20223089018126E-16));
#37151=CARTESIAN_POINT('Ctrl Pts',(-2.62458377340069,-2.22731585490721,
1.31838984174237E-16));
#37152=CARTESIAN_POINT('Ctrl Pts',(-2.6428539078105,-2.20858717031188,1.42494544454281E-16));
#37153=CARTESIAN_POINT('Ctrl Pts',(-2.66092072754138,-2.18962968712113,
4.62480998826576E-16));
#37154=CARTESIAN_POINT('Ctrl Pts',(-2.67876242915531,-2.17047018454057,
4.44089209850063E-16));
#37155=CARTESIAN_POINT('Ctrl Pts',(-2.75353668750271,-2.09017304546908,
3.67009545019966E-16));
#37156=CARTESIAN_POINT('Ctrl Pts',(-2.82442308955658,-2.00626812836577,
4.38199731939201E-16));
#37157=CARTESIAN_POINT('Ctrl Pts',(-2.89132427090349,-1.91917015947591,
2.28983498828939E-16));
#37158=CARTESIAN_POINT('Ctrl Pts',(-2.9553640840902,-1.83579737674842,2.87154585004375E-17));
#37159=CARTESIAN_POINT('Ctrl Pts',(-3.01575243661163,-1.74949800545801,
1.64657856526806E-16));
#37160=CARTESIAN_POINT('Ctrl Pts',(-3.07237914628982,-1.6606009570442,2.22044604925031E-16));
#37161=CARTESIAN_POINT('Ctrl Pts',(-3.09715333177403,-1.62170849836315,
2.47151307349255E-16));
#37162=CARTESIAN_POINT('Ctrl Pts',(-3.12120717339458,-1.58231843772374,
3.74830717982145E-16));
#37163=CARTESIAN_POINT('Ctrl Pts',(-3.14452974084395,-1.54245667505035,
4.16333634234434E-16));
#37164=CARTESIAN_POINT('Ctrl Pts',(-3.1552141693008,-1.52419538574881,4.35346761344512E-16));
#37165=CARTESIAN_POINT('Ctrl Pts',(-3.1657451101877,-1.50583508811633,6.65859873947159E-18));
#37166=CARTESIAN_POINT('Ctrl Pts',(-3.17612143314624,-1.48737821330264,
4.16333634234434E-17));
#37167=CARTESIAN_POINT('Ctrl Pts',(-3.1851701035806,-1.47128289918176,7.21331002193362E-17));
#37168=CARTESIAN_POINT('Ctrl Pts',(-3.19410146294443,-1.45511349134961,
1.2766348924177E-16));
#37169=CARTESIAN_POINT('Ctrl Pts',(-3.20290718418031,-1.4388859283946,1.2490009027033E-16));
#37170=CARTESIAN_POINT('Ctrl Pts',(-3.25753999780039,-1.33820622270319,
1.07755298047126E-16));
#37171=CARTESIAN_POINT('Ctrl Pts',(-3.30741231186542,-1.23516335787123,
5.68363615759287E-16));
#37172=CARTESIAN_POINT('Ctrl Pts',(-3.35241796906181,-1.13019103593447,
4.71844785465692E-16));
#37173=CARTESIAN_POINT('Ctrl Pts',(-3.39804200535616,-1.0237763911033,3.73999783509847E-16));
#37174=CARTESIAN_POINT('Ctrl Pts',(-3.43866526602443,-0.915378183946712,
-6.22512805566231E-17));
#37175=CARTESIAN_POINT('Ctrl Pts',(-3.47413966247048,-0.805410191460158,
-1.66533453693773E-16));
#37176=CARTESIAN_POINT('Ctrl Pts',(-3.50939387582959,-0.696124750178875,
-2.70168366465852E-16));
#37177=CARTESIAN_POINT('Ctrl Pts',(-3.53956336356882,-0.585288114116654,
-7.73645964354313E-17));
#37178=CARTESIAN_POINT('Ctrl Pts',(-3.56445901023683,-0.473280938901883,
-1.38777878078145E-16));
#37179=CARTESIAN_POINT('Ctrl Pts',(-3.58104437402115,-0.39866228078212,
-1.79691120092537E-16));
#37180=CARTESIAN_POINT('Ctrl Pts',(-3.59528821670414,-0.323523611696084,
-9.85603223433227E-18));
#37181=CARTESIAN_POINT('Ctrl Pts',(-3.60712230450606,-0.24797391740747,
-2.77555756156289E-17));
#37182=CARTESIAN_POINT('Ctrl Pts',(-3.61048639425725,-0.226497318913744,
-3.28438994009322E-17));
#37183=CARTESIAN_POINT('Ctrl Pts',(-3.613655686349,-0.204987494839638,2.70286722177284E-16));
#37184=CARTESIAN_POINT('Ctrl Pts',(-3.61662845468875,-0.183446929103701,
2.77555756156289E-16));
#37185=CARTESIAN_POINT('Ctrl Pts',(-3.61934694140478,-0.163748878291719,
2.84203018926811E-16));
#37186=CARTESIAN_POINT('Ctrl Pts',(-3.62190130092961,-0.144022588989176,
-9.4234710418247E-17));
#37187=CARTESIAN_POINT('Ctrl Pts',(-3.62428757941211,-0.124293547804644,
-8.32667268468867E-17));
#37188=CARTESIAN_POINT('Ctrl Pts',(-3.63845233765523,-0.007183537050793,
-1.81616534692129E-17));
#37189=CARTESIAN_POINT('Ctrl Pts',(-3.64672404198312,0.110194833970378,
2.72159498670366E-16));
#37190=CARTESIAN_POINT('Ctrl Pts',(-3.64895596115005,0.227419084314086,
2.4980018054066E-16));
#37191=CARTESIAN_POINT('Ctrl Pts',(-3.6502760977502,0.296754939123098,2.36575080521473E-16));
#37192=CARTESIAN_POINT('Ctrl Pts',(-3.64948239134564,0.366037414325706,
-3.91023963353986E-16));
#37193=CARTESIAN_POINT('Ctrl Pts',(-3.64653656430167,0.435182446792325,
-3.33066907387547E-16));
#37194=CARTESIAN_POINT('Ctrl Pts',(-3.64171075252927,0.548454851010284,
-2.38122486414389E-16));
#37195=CARTESIAN_POINT('Ctrl Pts',(-3.63111244226456,0.661358405661847,
1.01745842338307E-16));
#37196=CARTESIAN_POINT('Ctrl Pts',(-3.61501201454962,0.773605457518614,
8.32667268468867E-17));
#37197=CARTESIAN_POINT('Ctrl Pts',(-3.5986111375463,0.887947146080084,6.44427734916789E-17));
#37198=CARTESIAN_POINT('Ctrl Pts',(-3.57650072189919,1.00160829055033,1.76269981291295E-16));
#37199=CARTESIAN_POINT('Ctrl Pts',(-3.5489124899874,1.11428362811214,1.66533453693773E-16));
#37200=CARTESIAN_POINT('Ctrl Pts',(-3.53981806230419,1.1514269184982,1.63323819005896E-16));
#37201=CARTESIAN_POINT('Ctrl Pts',(-3.53012795001213,1.18846302772386,5.91487372108521E-17));
#37202=CARTESIAN_POINT('Ctrl Pts',(-3.51984924725713,1.22538078979166,5.55111512312578E-17));
#37203=CARTESIAN_POINT('Ctrl Pts',(-3.51512490385872,1.24234909694735,5.38392276706252E-17));
#37204=CARTESIAN_POINT('Ctrl Pts',(-3.51027554782375,1.25929445386572,-8.56270895207211E-17));
#37205=CARTESIAN_POINT('Ctrl Pts',(-3.5053071420154,1.27619828084334,-8.32667268468867E-17));
#37206=CARTESIAN_POINT('Ctrl Pts',(-3.4726474677456,1.38731510670219,-6.77509499438615E-17));
#37207=CARTESIAN_POINT('Ctrl Pts',(-3.43480620738079,1.4967920748245,-3.16991689118145E-16));
#37208=CARTESIAN_POINT('Ctrl Pts',(-3.3920889732967,1.60433756714027,-2.77555756156289E-16));
#37209=CARTESIAN_POINT('Ctrl Pts',(-3.34803513046651,1.71524812390167,-2.36885885322814E-16));
#37210=CARTESIAN_POINT('Ctrl Pts',(-3.29879531544834,1.82410515487266,-4.90905898233538E-17));
#37211=CARTESIAN_POINT('Ctrl Pts',(-3.2446494755425,1.93058787890887,-2.77555756156289E-17));
#37212=CARTESIAN_POINT('Ctrl Pts',(-3.19007975249465,2.03790420773747,-6.25353928999361E-18));
#37213=CARTESIAN_POINT('Ctrl Pts',(-3.13052656738101,2.14280969706861,3.27691398306138E-16));
#37214=CARTESIAN_POINT('Ctrl Pts',(-3.06622468325314,2.24496360523417,3.33066907387547E-16));
#37215=CARTESIAN_POINT('Ctrl Pts',(-3.02442954901331,2.31136191319685,3.36560897131582E-16));
#37216=CARTESIAN_POINT('Ctrl Pts',(-2.98062715064349,2.37659746123392,-1.92345692100733E-16));
#37217=CARTESIAN_POINT('Ctrl Pts',(-2.93487136195522,2.44057147262401,-2.22044604925031E-16));
#37218=CARTESIAN_POINT('Ctrl Pts',(-2.91011088425382,2.47519063509293,-2.38115998071626E-16));
#37219=CARTESIAN_POINT('Ctrl Pts',(-2.88477824351069,2.50944029002795,-9.06967170124101E-17));
#37220=CARTESIAN_POINT('Ctrl Pts',(-2.85888104291211,2.54330410738954,-1.11022302462516E-16));
#37221=CARTESIAN_POINT('Ctrl Pts',(-2.84939469288667,2.55570869233558,-1.1846772565866E-16));
#37222=CARTESIAN_POINT('Ctrl Pts',(-2.83983467756884,2.56805870725536,-6.92597506618051E-18));
#37223=CARTESIAN_POINT('Ctrl Pts',(-2.83020669950388,2.58034686246535,0.));
#37224=CARTESIAN_POINT('Ctrl Pts',(-2.75399123609851,2.67762039564213,5.48262984856848E-17));
#37225=CARTESIAN_POINT('Ctrl Pts',(-2.67342730379929,2.77114184208896,-1.37750122974287E-16));
#37226=CARTESIAN_POINT('Ctrl Pts',(-2.58880471591903,2.86057864451344,-1.11022302462516E-16));
#37227=CARTESIAN_POINT('Ctrl Pts',(-2.5041872730583,2.95001000921607,-8.42961069915503E-17));
#37228=CARTESIAN_POINT('Ctrl Pts',(-2.41551123635495,3.03535802102991,-2.67279349305171E-16));
#37229=CARTESIAN_POINT('Ctrl Pts',(-2.3230183042847,3.11627005080055,-3.33066907387547E-16));
#37230=CARTESIAN_POINT('Ctrl Pts',(-2.23098883090374,3.19677665085427,-3.98524820655353E-16));
#37231=CARTESIAN_POINT('Ctrl Pts',(-2.13518016460462,3.27289238327565,-7.81735663884996E-17));
#37232=CARTESIAN_POINT('Ctrl Pts',(-2.0357894675403,3.34423830723631,-2.22044604925031E-16));
#37233=CARTESIAN_POINT('Ctrl Pts',(-1.93639877047599,3.41558423119697,-3.65915643461563E-16));
#37234=CARTESIAN_POINT('Ctrl Pts',(-1.83342562767619,3.48216116641753,-4.77297284244418E-18));
#37235=CARTESIAN_POINT('Ctrl Pts',(-1.72703261341869,3.54354657824449,0.));
#37236=CARTESIAN_POINT('Origin',(0.,0.,0.));
#37237=CARTESIAN_POINT('Origin',(-1.73205080756888,-3.,-8.));
#37238=CARTESIAN_POINT('',(-1.73205080756888,-3.,-8.));
#37239=CARTESIAN_POINT('',(1.73205080756888,-3.,-8.));
#37240=CARTESIAN_POINT('',(-0.86602540378444,-3.,-8.));
#37241=CARTESIAN_POINT('',(-1.73205080756888,-3.,-4.));
#37242=CARTESIAN_POINT('',(-1.73205080756888,-3.,-8.));
#37243=CARTESIAN_POINT('',(1.73205080756888,-3.,-4.));
#37244=CARTESIAN_POINT('',(-1.73205080756888,-3.,-4.));
#37245=CARTESIAN_POINT('',(1.73205080756888,-3.,-8.));
#37246=CARTESIAN_POINT('Origin',(-3.46410161513775,4.24230095489963E-16,
-8.));
#37247=CARTESIAN_POINT('',(-3.46410161513775,4.24230095489963E-16,-8.));
#37248=CARTESIAN_POINT('',(-3.03108891324554,-0.749999999999999,-8.));
#37249=CARTESIAN_POINT('',(-3.46410161513775,5.55111512312578E-16,-4.));
#37250=CARTESIAN_POINT('',(-3.46410161513775,4.24230095489963E-16,-8.));
#37251=CARTESIAN_POINT('',(-3.46410161513775,4.24230095489963E-16,-4.));
#37252=CARTESIAN_POINT('Origin',(-1.73205080756888,3.,-8.));
#37253=CARTESIAN_POINT('',(-1.73205080756888,3.,-8.));
#37254=CARTESIAN_POINT('',(-2.1650635094611,2.25,-8.));
#37255=CARTESIAN_POINT('',(-1.73205080756888,3.,-4.));
#37256=CARTESIAN_POINT('',(-1.73205080756888,3.,-8.));
#37257=CARTESIAN_POINT('',(-1.73205080756888,3.,-4.));
#37258=CARTESIAN_POINT('Origin',(1.73205080756888,3.,-8.));
#37259=CARTESIAN_POINT('',(1.73205080756888,3.,-8.));
#37260=CARTESIAN_POINT('',(0.866025403784439,3.,-8.));
#37261=CARTESIAN_POINT('',(1.73205080756888,3.,-4.));
#37262=CARTESIAN_POINT('',(1.73205080756888,3.,-8.));
#37263=CARTESIAN_POINT('',(1.73205080756888,3.,-4.));
#37264=CARTESIAN_POINT('Origin',(3.46410161513775,0.,-8.));
#37265=CARTESIAN_POINT('',(3.46410161513775,0.,-8.));
#37266=CARTESIAN_POINT('',(3.03108891324554,0.75,-8.));
#37267=CARTESIAN_POINT('',(3.46410161513775,0.,-4.));
#37268=CARTESIAN_POINT('',(3.46410161513775,0.,-8.));
#37269=CARTESIAN_POINT('',(3.46410161513775,0.,-4.));
#37270=CARTESIAN_POINT('Origin',(1.73205080756888,-3.,-8.));
#37271=CARTESIAN_POINT('',(2.1650635094611,-2.25,-8.));
#37272=CARTESIAN_POINT('',(1.73205080756888,-3.,-4.));
#37273=CARTESIAN_POINT('Origin',(0.,5.55111512312578E-16,-4.));
#37274=CARTESIAN_POINT('Origin',(0.,0.,0.));
#37275=CARTESIAN_POINT('',(-6.5,-7.9602041944578E-16,0.));
#37276=CARTESIAN_POINT('Origin',(0.,0.,0.));
#37277=CARTESIAN_POINT('Origin',(0.,0.,-8.));
#37278=CARTESIAN_POINT('',(-6.5,-7.9602041944578E-16,-8.));
#37279=CARTESIAN_POINT('',(-6.5,-7.9602041944578E-16,-8.));
#37280=CARTESIAN_POINT('Origin',(0.,0.,-8.));
#37281=CARTESIAN_POINT('Origin',(0.,0.,-8.));
#37282=CARTESIAN_POINT('Origin',(0.,0.,25.));
#97435=UNCERTAINTY_MEASURE_WITH_UNIT(LENGTH_MEASURE(0.01),#97476,
'DISTANCE_ACCURACY_VALUE',
'Maximum model space distance between geometric entities at asserted c
onnectivities');
#97452=UNCERTAINTY_MEASURE_WITH_UNIT(LENGTH_MEASURE(0.01),#97476,
'DISTANCE_ACCURACY_VALUE',
'Maximum model space distance between geometric entities at asserted c
onnectivities');
#97458=(
GEOMETRIC_REPRESENTATION_CONTEXT(3)
GLOBAL_UNCERTAINTY_ASSIGNED_CONTEXT((#97435))
GLOBAL_UNIT_ASSIGNED_CONTEXT((#97476,#97478,#97479))
REPRESENTATION_CONTEXT('','3D')
);
#97475=(
GEOMETRIC_REPRESENTATION_CONTEXT(3)
GLOBAL_UNCERTAINTY_ASSIGNED_CONTEXT((#97452))
GLOBAL_UNIT_ASSIGNED_CONTEXT((#97476,#97478,#97479))
REPRESENTATION_CONTEXT('','3D')
);
#97476=(
LENGTH_UNIT()
NAMED_UNIT(*)
SI_UNIT(.MILLI.,.METRE.)
);
#97478=(
NAMED_UNIT(*)
PLANE_ANGLE_UNIT()
SI_UNIT($,.RADIAN.)
);
#97479=(
NAMED_UNIT(*)
SI_UNIT($,.STERADIAN.)
SOLID_ANGLE_UNIT()
);
#97485=SHAPE_DEFINITION_REPRESENTATION(#97507,#97608);
#97507=PRODUCT_DEFINITION_SHAPE('',$,#97631);
#97608=SHAPE_REPRESENTATION('',(#22177),#97458);
#97625=PRODUCT_DEFINITION_CONTEXT('part definition',#97693,'design');
#97631=PRODUCT_DEFINITION('Socket head cap screw M8x25',
'Socket head cap screw M8x25',#97653,#97625);
#97653=PRODUCT_DEFINITION_FORMATION('',$,#97700);
#97693=APPLICATION_CONTEXT(
'Core Data for Automotive Mechanical Design Process');
#97694=PRODUCT_CONTEXT('part definition',#97693,'mechanical');
#97700=PRODUCT('Socket head cap screw M8x25',
'Socket head cap screw M8x25',$,(#97694));
#97720=PRESENTATION_STYLE_ASSIGNMENT((#97727));
#97727=SURFACE_STYLE_USAGE(.BOTH.,#97734);
#97734=SURFACE_SIDE_STYLE('',(#97741));
#97741=SURFACE_STYLE_FILL_AREA(#97748);
#97748=FILL_AREA_STYLE('Dark gray',(#97755));
#97755=FILL_AREA_STYLE_COLOUR('Dark gray',#97762);
#97762=COLOUR_RGB('Dark gray',0.250980392156863,0.282352941176471,0.32156862745098);
ENDSEC;
END-ISO-10303-21;
